ISO-10303-21;
HEADER;
/* Generated by software containing ST-Developer
 * from STEP Tools, Inc. (www.steptools.com) 
 */

FILE_DESCRIPTION(
/* description */ (''),
/* implementation_level */ '2;1');

FILE_NAME(
/* name */ 'ISO 1207 - M2 x 4 - 4.8.step',
/* time_stamp */ '2026-10-15T12:29:06-07:00',
/* author */ (''),
/* organization */ (''),
/* preprocessor_version */ 'ST-DEVELOPER v20.2',
/* originating_system */ 'Autodesk Translation Framework v15.15.0.0',
/* authorisation */ '');

FILE_SCHEMA (('AUTOMOTIVE_DESIGN { 1 0 10303 214 3 1 1 }'));
ENDSEC;

DATA;
#10=MECHANICAL_DESIGN_GEOMETRIC_PRESENTATION_REPRESENTATION('',(#1751),#135282);
#99=TOROIDAL_SURFACE('',#34180,1.06675,0.1);
#284=(
BOUNDED_CURVE()
B_SPLINE_CURVE(2,(#135195,#135196,#135197),.UNSPECIFIED.,.F.,.F.)
B_SPLINE_CURVE_WITH_KNOTS((3,3),(0.231010318517618,0.279990879997656),
 .UNSPECIFIED.)
CURVE()
GEOMETRIC_REPRESENTATION_ITEM()
RATIONAL_B_SPLINE_CURVE((1.22678406090041,1.21136642152085,1.17921561612836))
REPRESENTATION_ITEM('')
);
#285=(
BOUNDED_CURVE()
B_SPLINE_CURVE(2,(#135200,#135201,#135202),.UNSPECIFIED.,.F.,.F.)
B_SPLINE_CURVE_WITH_KNOTS((3,3),(0.0917701333748426,0.140750694854882),
 .UNSPECIFIED.)
CURVE()
GEOMETRIC_REPRESENTATION_ITEM()
RATIONAL_B_SPLINE_CURVE((1.17921561612829,1.21136642152077,1.22678406090031))
REPRESENTATION_ITEM('')
);
#286=(
BOUNDED_CURVE()
B_SPLINE_CURVE(2,(#135207,#135208,#135209),.UNSPECIFIED.,.F.,.F.)
B_SPLINE_CURVE_WITH_KNOTS((3,3),(0.231010318517594,0.279990879997634),
 .UNSPECIFIED.)
CURVE()
GEOMETRIC_REPRESENTATION_ITEM()
RATIONAL_B_SPLINE_CURVE((1.22678406090031,1.21136642152077,1.17921561612829))
REPRESENTATION_ITEM('')
);
#287=(
BOUNDED_CURVE()
B_SPLINE_CURVE(2,(#135213,#135214,#135215),.UNSPECIFIED.,.F.,.F.)
B_SPLINE_CURVE_WITH_KNOTS((3,3),(0.0917701333748425,0.140750694854882),
 .UNSPECIFIED.)
CURVE()
GEOMETRIC_REPRESENTATION_ITEM()
RATIONAL_B_SPLINE_CURVE((1.17921561612829,1.21136642152077,1.22678406090031))
REPRESENTATION_ITEM('')
);
#615=B_SPLINE_SURFACE_WITH_KNOTS('',3,3,((#134384,#134385,#134386,#134387,
#134388,#134389,#134390,#134391,#134392,#134393,#134394,#134395,#134396,
#134397,#134398,#134399,#134400,#134401,#134402,#134403,#134404,#134405,
#134406,#134407,#134408,#134409,#134410,#134411,#134412,#134413,#134414,
#134415,#134416,#134417,#134418,#134419,#134420,#134421,#134422,#134423,
#134424,#134425,#134426,#134427,#134428,#134429,#134430,#134431,#134432,
#134433,#134434,#134435,#134436,#134437,#134438,#134439,#134440,#134441,
#134442,#134443,#134444,#134445,#134446,#134447,#134448,#134449,#134450,
#134451,#134452,#134453,#134454,#134455),(#134456,#134457,#134458,#134459,
#134460,#134461,#134462,#134463,#134464,#134465,#134466,#134467,#134468,
#134469,#134470,#134471,#134472,#134473,#134474,#134475,#134476,#134477,
#134478,#134479,#134480,#134481,#134482,#134483,#134484,#134485,#134486,
#134487,#134488,#134489,#134490,#134491,#134492,#134493,#134494,#134495,
#134496,#134497,#134498,#134499,#134500,#134501,#134502,#134503,#134504,
#134505,#134506,#134507,#134508,#134509,#134510,#134511,#134512,#134513,
#134514,#134515,#134516,#134517,#134518,#134519,#134520,#134521,#134522,
#134523,#134524,#134525,#134526,#134527),(#134528,#134529,#134530,#134531,
#134532,#134533,#134534,#134535,#134536,#134537,#134538,#134539,#134540,
#134541,#134542,#134543,#134544,#134545,#134546,#134547,#134548,#134549,
#134550,#134551,#134552,#134553,#134554,#134555,#134556,#134557,#134558,
#134559,#134560,#134561,#134562,#134563,#134564,#134565,#134566,#134567,
#134568,#134569,#134570,#134571,#134572,#134573,#134574,#134575,#134576,
#134577,#134578,#134579,#134580,#134581,#134582,#134583,#134584,#134585,
#134586,#134587,#134588,#134589,#134590,#134591,#134592,#134593,#134594,
#134595,#134596,#134597,#134598,#134599),(#134600,#134601,#134602,#134603,
#134604,#134605,#134606,#134607,#134608,#134609,#134610,#134611,#134612,
#134613,#134614,#134615,#134616,#134617,#134618,#134619,#134620,#134621,
#134622,#134623,#134624,#134625,#134626,#134627,#134628,#134629,#134630,
#134631,#134632,#134633,#134634,#134635,#134636,#134637,#134638,#134639,
#134640,#134641,#134642,#134643,#134644,#134645,#134646,#134647,#134648,
#134649,#134650,#134651,#134652,#134653,#134654,#134655,#134656,#134657,
#134658,#134659,#134660,#134661,#134662,#134663,#134664,#134665,#134666,
#134667,#134668,#134669,#134670,#134671)),.UNSPECIFIED.,.F.,.F.,.F.,(4,
4),(4,1,1,1,1,1,1,1,1,1,1,1,1,1,1,1,1,1,1,1,1,1,1,1,1,1,1,1,1,1,1,1,1,1,
1,1,1,1,1,1,1,1,1,1,1,1,1,1,1,1,1,1,1,1,1,1,1,1,1,1,1,1,1,1,1,1,1,1,1,4),
(-0.000148463654747345,0.0266708891660514),(8.30910520973557,9.29917567257901,
10.2890599933927,11.2789443142064,12.2688286350201,13.2587129558338,14.2485972766475,
15.2384815974612,16.2283659182749,17.2182502390886,18.2081345599023,19.198018880716,
20.1879032015297,21.1777875223434,22.1676718431571,23.1575561639708,24.1474404847846,
25.1373248055983,26.127209126412,27.1170934472257,28.1069777680394,29.0968620888531,
30.0867464096668,31.0766307304805,32.0665150512942,33.0563993721079,34.0462836929216,
35.0361680137353,36.026052334549,37.0159366553627,38.0058209761764,38.9957052969901,
39.9855896178038,40.9754739386175,41.9653582594312,42.9552425802449,43.9451269010586,
44.9350112218723,45.924895542686,46.9147798634997,47.9046641843134,48.8945485051271,
49.8844328259408,50.8743171467545,51.8642014675682,52.8540857883819,53.8439701091956,
54.8338544300093,55.823738750823,56.8136230716368,57.8035073924505,58.7933917132642,
59.7832760340779,60.7731603548916,61.7630446757053,62.752928996519,63.7428133173327,
64.7326976381464,65.7225819589601,66.7124662797738,67.7023506005875,68.6922349214012,
69.6821192422149,70.6720035630286,71.6618878838423,72.651772204656,73.6416565254697,
74.6315408462834,75.6214251670971,76.6114579515656),.UNSPECIFIED.);
#616=B_SPLINE_SURFACE_WITH_KNOTS('',3,3,((#134879,#134880,#134881,#134882,
#134883,#134884,#134885,#134886,#134887,#134888,#134889,#134890,#134891,
#134892,#134893,#134894,#134895,#134896,#134897,#134898,#134899,#134900,
#134901,#134902,#134903,#134904,#134905,#134906,#134907,#134908,#134909,
#134910,#134911,#134912,#134913,#134914,#134915,#134916,#134917,#134918,
#134919,#134920,#134921,#134922,#134923,#134924,#134925,#134926,#134927,
#134928,#134929,#134930,#134931,#134932,#134933,#134934,#134935,#134936,
#134937,#134938,#134939,#134940,#134941,#134942,#134943,#134944,#134945,
#134946,#134947,#134948),(#134949,#134950,#134951,#134952,#134953,#134954,
#134955,#134956,#134957,#134958,#134959,#134960,#134961,#134962,#134963,
#134964,#134965,#134966,#134967,#134968,#134969,#134970,#134971,#134972,
#134973,#134974,#134975,#134976,#134977,#134978,#134979,#134980,#134981,
#134982,#134983,#134984,#134985,#134986,#134987,#134988,#134989,#134990,
#134991,#134992,#134993,#134994,#134995,#134996,#134997,#134998,#134999,
#135000,#135001,#135002,#135003,#135004,#135005,#135006,#135007,#135008,
#135009,#135010,#135011,#135012,#135013,#135014,#135015,#135016,#135017,
#135018),(#135019,#135020,#135021,#135022,#135023,#135024,#135025,#135026,
#135027,#135028,#135029,#135030,#135031,#135032,#135033,#135034,#135035,
#135036,#135037,#135038,#135039,#135040,#135041,#135042,#135043,#135044,
#135045,#135046,#135047,#135048,#135049,#135050,#135051,#135052,#135053,
#135054,#135055,#135056,#135057,#135058,#135059,#135060,#135061,#135062,
#135063,#135064,#135065,#135066,#135067,#135068,#135069,#135070,#135071,
#135072,#135073,#135074,#135075,#135076,#135077,#135078,#135079,#135080,
#135081,#135082,#135083,#135084,#135085,#135086,#135087,#135088),(#135089,
#135090,#135091,#135092,#135093,#135094,#135095,#135096,#135097,#135098,
#135099,#135100,#135101,#135102,#135103,#135104,#135105,#135106,#135107,
#135108,#135109,#135110,#135111,#135112,#135113,#135114,#135115,#135116,
#135117,#135118,#135119,#135120,#135121,#135122,#135123,#135124,#135125,
#135126,#135127,#135128,#135129,#135130,#135131,#135132,#135133,#135134,
#135135,#135136,#135137,#135138,#135139,#135140,#135141,#135142,#135143,
#135144,#135145,#135146,#135147,#135148,#135149,#135150,#135151,#135152,
#135153,#135154,#135155,#135156,#135157,#135158)),.UNSPECIFIED.,.F.,.F.,
 .F.,(4,4),(4,1,1,1,1,1,1,1,1,1,1,1,1,1,1,1,1,1,1,1,1,1,1,1,1,1,1,1,1,1,
1,1,1,1,1,1,1,1,1,1,1,1,1,1,1,1,1,1,1,1,1,1,1,1,1,1,1,1,1,1,1,1,1,1,1,1,
1,4),(-0.000394127981503626,0.0264020341717739),(13.6815980460861,14.6704625085889,
15.6590677938146,16.6476730790403,17.6362783642661,18.6248836494918,19.6134889347175,
20.6020942199433,21.590699505169,22.5793047903947,23.5679100756204,24.5565153608462,
25.5451206460719,26.5337259312976,27.5223312165234,28.5109365017491,29.4995417869748,
30.4881470722005,31.4767523574263,32.465357642652,33.4539629278777,34.4425682131035,
35.4311734983292,36.4197787835549,37.4083840687806,38.3969893540064,39.3855946392321,
40.3741999244578,41.3628052096836,42.3514104949093,43.340015780135,44.3286210653607,
45.3172263505865,46.3058316358122,47.2944369210379,48.2830422062637,49.2716474914894,
50.2602527767151,51.2488580619408,52.2374633471666,53.2260686323923,54.214673917618,
55.2032792028438,56.1918844880695,57.1804897732952,58.1690950585209,59.1577003437467,
60.1463056289724,61.1349109141981,62.1235161994239,63.1121214846496,64.1007267698753,
65.089332055101,66.0779373403268,67.0665426255525,68.0551479107782,69.0437531960039,
70.0323584812297,71.0209637664554,72.0095690516811,72.9981743369069,73.9867796221326,
74.9753849073583,75.963990192584,76.9525954778098,77.9412007630355,78.9298060482612,
79.9185965318092),.UNSPECIFIED.);
#1649=B_SPLINE_CURVE_WITH_KNOTS('',3,(#126911,#126912,#126913,#126914,#126915,
#126916,#126917,#126918,#126919,#126920,#126921,#126922,#126923,#126924,
#126925,#126926,#126927,#126928,#126929,#126930,#126931,#126932,#126933,
#126934,#126935,#126936,#126937,#126938,#126939,#126940,#126941,#126942,
#126943,#126944,#126945,#126946,#126947,#126948,#126949,#126950,#126951,
#126952,#126953,#126954,#126955,#126956,#126957,#126958,#126959,#126960,
#126961,#126962),.UNSPECIFIED.,.F.,.F.,(4,3,3,3,3,3,3,3,3,3,3,3,3,3,3,3,
3,4),(-4.09157007060746,-4.04267459647314,-3.91804643852106,-3.79360664990601,
-3.66929160873361,-3.54503793099914,-3.42067389293025,-3.29626244717563,
-3.17156478702648,-3.05406931124741,-2.92480942306547,-2.79577237913115,
-2.66690816470504,-2.53816707784842,-2.40945958659725,-2.28078154682162,
-2.15200653753529,-2.0654640260217),.UNSPECIFIED.);
#1650=B_SPLINE_CURVE_WITH_KNOTS('',3,(#126965,#126966,#126967,#126968,#126969,
#126970,#126971,#126972,#126973,#126974,#126975,#126976,#126977,#126978,
#126979,#126980,#126981,#126982,#126983,#126984,#126985,#126986,#126987,
#126988,#126989,#126990,#126991,#126992),.UNSPECIFIED.,.F.,.F.,(4,3,3,3,
3,3,3,3,3,4),(0.,0.128770504077986,0.257463953946973,0.386129758592228,
0.514817261654237,0.643692750510219,0.772663027875016,0.901926079013672,
0.989884320813703,1.11548660900397),.UNSPECIFIED.);
#1651=B_SPLINE_CURVE_WITH_KNOTS('',3,(#126997,#126998,#126999,#127000,#127001,
#127002,#127003,#127004,#127005,#127006,#127007,#127008,#127009,#127010,
#127011,#127012,#127013,#127014,#127015,#127016,#127017,#127018,#127019,
#127020,#127021,#127022,#127023,#127024,#127025,#127026,#127027,#127028,
#127029,#127030,#127031,#127032,#127033,#127034,#127035,#127036,#127037,
#127038,#127039,#127040,#127041,#127042,#127043,#127044,#127045,#127046,
#127047,#127048,#127049,#127050,#127051,#127052,#127053,#127054,#127055,
#127056,#127057,#127058,#127059,#127060,#127061,#127062,#127063,#127064,
#127065,#127066,#127067,#127068,#127069,#127070,#127071,#127072,#127073,
#127074,#127075,#127076,#127077,#127078,#127079,#127080,#127081,#127082,
#127083,#127084,#127085,#127086,#127087,#127088,#127089,#127090,#127091,
#127092,#127093,#127094,#127095,#127096,#127097,#127098,#127099,#127100,
#127101,#127102,#127103,#127104,#127105,#127106,#127107,#127108,#127109,
#127110,#127111,#127112,#127113,#127114,#127115,#127116,#127117,#127118,
#127119,#127120,#127121,#127122,#127123,#127124,#127125,#127126,#127127,
#127128,#127129,#127130,#127131,#127132,#127133,#127134,#127135,#127136,
#127137,#127138,#127139,#127140,#127141,#127142,#127143,#127144,#127145,
#127146,#127147,#127148,#127149,#127150,#127151,#127152,#127153,#127154,
#127155,#127156,#127157,#127158,#127159,#127160,#127161,#127162,#127163,
#127164,#127165,#127166,#127167,#127168,#127169,#127170,#127171,#127172,
#127173,#127174,#127175,#127176,#127177,#127178,#127179,#127180,#127181,
#127182,#127183,#127184,#127185,#127186,#127187,#127188,#127189),
 .UNSPECIFIED.,.F.,.F.,(4,3,3,3,3,3,3,3,3,3,3,3,3,3,3,3,3,3,3,3,3,3,3,3,
3,3,3,3,3,3,3,3,3,3,3,3,3,3,3,3,3,3,3,3,3,3,3,3,3,3,3,3,3,3,3,3,3,3,3,3,
3,3,3,3,4),(-10.3747553770227,-10.2366360171358,-10.1065918341442,-10.097621507011,
-9.97435184766567,-9.97430630782751,-9.85805755748757,-9.84843734717473,
-9.72275709682591,-9.59720432091665,-9.47171800663457,-9.34614035145364,
-9.22052340584574,-9.09465137971492,-8.98574649523054,-8.98570102260178,
-8.86943094769939,-8.85978588593879,-8.73405959725147,-8.60846101885127,
-8.48292923617449,-8.35730705327952,-8.23164602820857,-8.10573130030452,
-7.9971408564736,-7.99709573737606,-7.88075327220879,-7.87117390366413,
-7.74544034467922,-7.61983394815419,-7.49429382402376,-7.36866257916642,
-7.24299208158905,-7.11706734697963,-7.00853658425701,-7.00849045215032,
-6.89238358877969,-6.88275794584282,-6.75721440838983,-6.63179830794794,
-6.50644833672224,-6.38100523841909,-6.25552208387502,-6.12978064259321,
-6.0199304705395,-6.0198851669246,-5.90354891647336,-5.89377144736946,-5.7678473942784,
-5.64205230085332,-5.51632568434797,-5.39051310093208,-5.26466383335606,
-5.13856714447721,-5.03132314697593,-5.03127988169887,-4.91519179536761,
-4.90623388686583,-4.78137263497701,-4.65663321639741,-4.53195294699382,
-4.40718096255982,-4.28235977243278,-4.15730670558814,-4.09157124239226),
 .UNSPECIFIED.);
#1652=B_SPLINE_CURVE_WITH_KNOTS('',3,(#127190,#127191,#127192,#127193,#127194,
#127195,#127196,#127197,#127198,#127199,#127200,#127201,#127202,#127203,
#127204,#127205,#127206,#127207,#127208,#127209,#127210,#127211,#127212,
#127213,#127214,#127215,#127216,#127217,#127218,#127219,#127220,#127221,
#127222,#127223,#127224,#127225,#127226,#127227,#127228,#127229,#127230,
#127231,#127232,#127233,#127234,#127235,#127236,#127237,#127238,#127239,
#127240,#127241,#127242,#127243,#127244,#127245,#127246,#127247,#127248,
#127249,#127250,#127251,#127252,#127253,#127254,#127255,#127256,#127257,
#127258,#127259,#127260,#127261,#127262,#127263,#127264,#127265,#127266,
#127267,#127268,#127269,#127270,#127271,#127272,#127273,#127274,#127275,
#127276,#127277,#127278,#127279,#127280,#127281,#127282,#127283,#127284,
#127285,#127286,#127287,#127288,#127289,#127290,#127291,#127292,#127293,
#127294,#127295,#127296,#127297,#127298,#127299,#127300,#127301,#127302,
#127303,#127304,#127305,#127306,#127307,#127308,#127309,#127310,#127311,
#127312,#127313,#127314,#127315,#127316,#127317,#127318,#127319,#127320,
#127321,#127322,#127323,#127324,#127325,#127326,#127327,#127328,#127329,
#127330,#127331,#127332,#127333,#127334,#127335,#127336,#127337,#127338,
#127339,#127340,#127341,#127342,#127343,#127344,#127345,#127346,#127347,
#127348,#127349,#127350,#127351,#127352,#127353,#127354,#127355,#127356,
#127357,#127358,#127359,#127360,#127361,#127362,#127363,#127364,#127365),
 .UNSPECIFIED.,.F.,.F.,(4,2,2,2,2,2,2,2,2,2,2,2,2,2,2,2,2,2,2,2,2,2,2,2,
2,2,2,2,2,2,2,2,2,2,2,2,2,2,2,2,2,2,2,2,2,2,2,2,2,2,2,2,2,2,2,2,2,2,2,2,
2,2,2,2,2,2,2,2,2,2,2,2,2,2,2,2,2,2,2,2,2,2,2,2,2,2,2,4),(0.000261646384316517,
0.0104924062465661,0.0260785968740954,0.0314686564231903,0.0343533113436317,
0.0368068389339,0.039813369304345,0.0456471493868944,0.0699359697100838,
0.0772288638425005,0.0818877276898668,0.0837832704086861,0.0851993880928992,
0.0869287609772795,0.0901709616532053,0.103770211934126,0.118549793829608,
0.127379387968971,0.130950725410799,0.133610817884919,0.136496694037172,
0.141284992766288,0.157275839707537,0.169927706991005,0.176474951605186,
0.17871844945781,0.180248987572319,0.181937634491626,0.185026125922963,
0.201953413384733,0.220518120216993,0.224785518830655,0.227548278686829,
0.230193218108385,0.233974595353628,0.244051689035776,0.245270298020942,
0.261852191084533,0.271911101446268,0.274414412264434,0.275971457591503,
0.277527655559406,0.280058748146808,0.290002469312615,0.308293612311992,
0.31803591741021,0.321673273167989,0.324297130762851,0.327062674753666,
0.331451761887082,0.354460658499812,0.363540349683242,0.368942050663461,
0.37100398708861,0.372474576449311,0.374186823311687,0.377347332450581,
0.391965672135443,0.406001920509121,0.414545700221812,0.41805035590891,
0.420672662087154,0.423526323958717,0.42827248989015,0.448032783400729,
0.462974579000867,0.465956762587759,0.467617303251053,0.469100891045124,
0.471297103908426,0.477206238672996,0.499268651330173,0.509763136066544,
0.513498286254066,0.516152580317041,0.518916554069543,0.523233147159251,
0.546707891920172,0.5555022822345,0.560801060174836,0.562857398999995,0.564332349502359,
0.566055861942539,0.569275343848298,0.582354352730892,0.594203837528408,
0.605560438582849,0.609378420130365),.UNSPECIFIED.);
#1653=B_SPLINE_CURVE_WITH_KNOTS('',3,(#127370,#127371,#127372,#127373,#127374,
#127375,#127376,#127377,#127378,#127379,#127380,#127381,#127382,#127383,
#127384,#127385,#127386,#127387,#127388,#127389,#127390,#127391,#127392,
#127393,#127394,#127395,#127396,#127397,#127398,#127399,#127400,#127401,
#127402,#127403,#127404,#127405,#127406,#127407,#127408,#127409,#127410,
#127411,#127412,#127413,#127414,#127415,#127416,#127417,#127418,#127419,
#127420,#127421,#127422,#127423,#127424,#127425,#127426,#127427,#127428,
#127429,#127430,#127431,#127432,#127433,#127434,#127435,#127436,#127437,
#127438,#127439,#127440,#127441,#127442,#127443,#127444,#127445,#127446,
#127447,#127448,#127449,#127450,#127451,#127452,#127453,#127454,#127455,
#127456,#127457,#127458,#127459,#127460,#127461,#127462,#127463,#127464,
#127465,#127466,#127467,#127468,#127469,#127470,#127471,#127472,#127473,
#127474,#127475,#127476,#127477,#127478,#127479,#127480,#127481,#127482,
#127483,#127484,#127485,#127486,#127487,#127488,#127489,#127490,#127491,
#127492,#127493,#127494,#127495,#127496,#127497,#127498,#127499,#127500,
#127501,#127502,#127503,#127504,#127505,#127506,#127507,#127508,#127509,
#127510,#127511,#127512,#127513,#127514,#127515,#127516,#127517,#127518,
#127519,#127520,#127521,#127522,#127523,#127524,#127525,#127526,#127527,
#127528,#127529,#127530,#127531,#127532,#127533,#127534,#127535,#127536,
#127537,#127538,#127539,#127540,#127541,#127542,#127543,#127544,#127545,
#127546,#127547,#127548,#127549,#127550,#127551),.UNSPECIFIED.,.F.,.F.,
(4,2,2,2,2,2,2,2,2,2,2,2,2,2,2,2,2,2,2,2,2,2,2,2,2,2,2,2,2,2,2,2,2,2,2,
2,2,2,2,2,2,2,2,2,2,2,2,2,2,2,2,2,2,2,2,2,2,2,2,2,2,2,2,2,2,2,2,2,2,2,2,
2,2,2,2,2,2,2,2,2,2,2,2,2,2,2,2,2,2,2,4),(0.609195619805639,0.625836591744223,
0.630724530933535,0.633663812077152,0.636369805467325,0.640000451724975,
0.649019629401262,0.664447742241405,0.676787354309999,0.680005585928994,
0.681762653288162,0.683296445509315,0.685489354608689,0.691518502334891,
0.702306140883459,0.721763852827824,0.726595122380225,0.729523082525254,
0.732232962020334,0.735890994775529,0.745123409561988,0.761279856723455,
0.773672716489257,0.77633483124701,0.777957126369306,0.779564627000971,
0.782156874269418,0.793050204386433,0.818300652538408,0.822773432172227,
0.825629936986889,0.828373004224322,0.832241027854228,0.843353789820006,
0.855520513510064,0.868397105928568,0.871641143390267,0.873403587583718,
0.874935820666734,0.877117908059764,0.883061100411173,0.893587699113478,
0.913469840618771,0.918270373770518,0.921192159859008,0.923904250351927,
0.927577684486519,0.936933185417741,0.950676183130047,0.965226615234117,
0.967935362305547,0.969567488647443,0.971165872655077,0.973715185559099,
0.983803321260223,0.998853179383179,1.01078026119092,1.01484334543049,1.01734359536002,
1.02010113950087,1.02405357629441,1.03609574529333,1.05440800406234,1.06167553801317,
1.06406534882108,1.06561660540468,1.06728797508272,1.07018324501945,1.0738730609813,
1.08266770840829,1.10591969986608,1.11030869246259,1.11314860394664,1.11590197609641,
1.11983028820028,1.13159375606052,1.14334493874623,1.15587132646578,1.15909683180329,
1.16085540183652,1.16238927915248,1.16458041464355,1.17059173982159,1.18132582692828,
1.18815902010274,1.20225533145114,1.20637803713945,1.20888907459917,1.21142899558228,
1.21454154335485,1.21829292486733),.UNSPECIFIED.);
#1654=B_SPLINE_CURVE_WITH_KNOTS('',3,(#127552,#127553,#127554,#127555,#127556,
#127557,#127558,#127559,#127560,#127561,#127562,#127563,#127564,#127565,
#127566,#127567,#127568,#127569,#127570,#127571,#127572,#127573,#127574,
#127575,#127576,#127577,#127578,#127579,#127580,#127581,#127582,#127583,
#127584,#127585,#127586,#127587,#127588,#127589,#127590,#127591,#127592,
#127593,#127594,#127595,#127596,#127597,#127598,#127599,#127600,#127601,
#127602,#127603,#127604,#127605,#127606,#127607,#127608,#127609,#127610,
#127611,#127612,#127613,#127614,#127615,#127616,#127617,#127618,#127619,
#127620,#127621,#127622,#127623,#127624,#127625,#127626,#127627,#127628,
#127629,#127630,#127631,#127632,#127633,#127634,#127635,#127636,#127637,
#127638,#127639,#127640,#127641,#127642,#127643,#127644,#127645,#127646,
#127647,#127648,#127649,#127650,#127651,#127652,#127653,#127654,#127655,
#127656,#127657,#127658,#127659,#127660,#127661,#127662,#127663,#127664,
#127665,#127666,#127667,#127668,#127669,#127670,#127671,#127672,#127673,
#127674,#127675,#127676,#127677,#127678,#127679,#127680,#127681,#127682,
#127683,#127684,#127685,#127686,#127687,#127688,#127689,#127690,#127691,
#127692,#127693,#127694,#127695,#127696,#127697,#127698,#127699,#127700,
#127701,#127702,#127703,#127704,#127705,#127706,#127707,#127708,#127709,
#127710,#127711,#127712,#127713,#127714,#127715,#127716,#127717,#127718,
#127719,#127720,#127721,#127722,#127723,#127724,#127725,#127726,#127727),
 .UNSPECIFIED.,.F.,.F.,(4,2,2,2,2,2,2,2,2,2,2,2,2,2,2,2,2,2,2,2,2,2,2,2,
2,2,2,2,2,2,2,2,2,2,2,2,2,2,2,2,2,2,2,2,2,2,2,2,2,2,2,2,2,2,2,2,2,2,2,2,
2,2,2,2,2,2,2,2,2,2,2,2,2,2,2,2,2,2,2,2,2,2,2,2,2,2,2,4),(0.609378420130365,
0.612018261019042,0.614749532539526,0.618912068663256,0.636505046351328,
0.65494406438821,0.657910724626156,0.659563280054749,0.661060644757464,
0.663265236923216,0.669740261678691,0.682089605334379,0.699480950387193,
0.704309301736647,0.707176017406193,0.709787490275448,0.713242974764558,
0.72146460941387,0.734601179923452,0.750546235794313,0.753668305013858,
0.755372632290222,0.756853898894493,0.758951506429721,0.764551085502066,
0.774164185389945,0.795931707416114,0.800483792711178,0.803294285009617,
0.80592385165699,0.80951130973408,0.818725931862822,0.833852378769016,0.846389382724306,
0.849576729273647,0.851294237547501,0.852771318082724,0.854841262120309,
0.860237659074661,0.86929352202869,0.892195415241358,0.896592589213518,
0.899371750568979,0.902015529817111,0.905693754047723,0.915674529561137,
0.934989613237843,0.943714825136999,0.946183102048811,0.94757844128154,
0.949109895292506,0.951495967565137,0.959876597557263,0.981786870823796,
0.990051400722908,0.993239578710188,0.99587603083011,0.9986181447563,1.00282732834149,
1.02167459701192,1.03853736295692,1.04158991940377,1.04327888819084,1.04476389158991,
1.04688982785566,1.05270942557411,1.06295651185913,1.08354366128914,1.08823160115648,
1.09106936404024,1.09368842933782,1.09720558872425,1.1058787280598,1.12032334244059,
1.13427287713437,1.13744942777678,1.1391647027966,1.14064244752089,1.14271684560393,
1.14814511063743,1.1572866691416,1.18000809371754,1.18443110260207,1.18721558580083,
1.18985695499119,1.19351949368841,1.19766710350325,1.21853221181177),
 .UNSPECIFIED.);
#1655=B_SPLINE_CURVE_WITH_KNOTS('',3,(#127732,#127733,#127734,#127735,#127736,
#127737,#127738,#127739,#127740,#127741,#127742,#127743,#127744,#127745,
#127746,#127747,#127748,#127749,#127750,#127751,#127752,#127753,#127754,
#127755,#127756,#127757,#127758,#127759,#127760,#127761,#127762,#127763,
#127764,#127765,#127766,#127767,#127768,#127769,#127770,#127771,#127772,
#127773,#127774,#127775,#127776,#127777,#127778,#127779,#127780,#127781,
#127782,#127783,#127784,#127785,#127786,#127787,#127788,#127789,#127790,
#127791,#127792,#127793,#127794,#127795,#127796,#127797,#127798,#127799,
#127800,#127801,#127802,#127803,#127804,#127805,#127806,#127807,#127808,
#127809,#127810,#127811,#127812,#127813,#127814,#127815,#127816,#127817,
#127818,#127819,#127820,#127821,#127822,#127823,#127824,#127825,#127826,
#127827,#127828,#127829,#127830,#127831,#127832,#127833,#127834,#127835,
#127836,#127837,#127838,#127839,#127840,#127841,#127842,#127843,#127844,
#127845,#127846,#127847,#127848,#127849,#127850,#127851,#127852,#127853,
#127854,#127855,#127856,#127857,#127858,#127859,#127860,#127861,#127862,
#127863,#127864,#127865,#127866,#127867,#127868,#127869,#127870,#127871,
#127872,#127873,#127874,#127875,#127876,#127877,#127878,#127879,#127880,
#127881,#127882,#127883,#127884,#127885,#127886,#127887,#127888,#127889,
#127890,#127891,#127892,#127893,#127894,#127895,#127896,#127897,#127898,
#127899,#127900,#127901,#127902,#127903,#127904,#127905,#127906,#127907,
#127908,#127909,#127910,#127911),.UNSPECIFIED.,.F.,.F.,(4,2,2,2,2,2,2,2,
2,2,2,2,2,2,2,2,2,2,2,2,2,2,2,2,2,2,2,2,2,2,2,2,2,2,2,2,2,2,2,2,2,2,2,2,
2,2,2,2,2,2,2,2,2,2,2,2,2,2,2,2,2,2,2,2,2,2,2,2,2,2,2,2,2,2,2,2,2,2,2,2,
2,2,2,2,2,2,2,2,2,4),(0.000273487393315781,0.00668233346743799,0.00878609781692979,
0.0103134599133232,0.0117975148680287,0.0135777641845307,0.0169067857893203,
0.0328729072272741,0.0429255957088579,0.053160566460337,0.0569373680766626,
0.0596652430555349,0.0625495357509145,0.0671628630974127,0.0887819817328903,
0.101670084334189,0.104999883847082,0.106760479612903,0.108293146614009,
0.110478679342832,0.116039509789547,0.134351598502859,0.143681644379522,
0.150343388885038,0.153616877504323,0.15602876636482,0.159081955031285,
0.16439949414022,0.186476116936597,0.197789695721472,0.200945388483554,
0.202670896217642,0.204215149808471,0.206113165149188,0.21099136274985,
0.23403270957221,0.244710670866626,0.248535132571594,0.251270903461355,
0.254140288972433,0.258678092552839,0.280869681227153,0.29340072818385,
0.296692921680029,0.298446052454859,0.299980974008835,0.30218176067146,
0.307838946549081,0.324246377305529,0.334620885239953,0.341766160368095,
0.345121457282295,0.34777266769147,0.350854357541875,0.356310502244138,
0.381933264092872,0.390755454099656,0.393221589200865,0.394803403819953,
0.396250867000954,0.39883513326232,0.408673790254529,0.426868100434012,
0.436631947879639,0.440355252498272,0.443074997540403,0.44597830587298,
0.450685673024221,0.471527379754759,0.481503349307649,0.485473236366192,
0.488532010842608,0.490237701450933,0.491772503840068,0.494067898864919,
0.500448675418648,0.517953107030139,0.531646616867548,0.535722368892298,
0.538502798460077,0.541309275474993,0.545523490887629,0.561305512379495,
0.575700119524876,0.582747278133253,0.585056256017955,0.586608656824652,
0.588314878278613,0.591376326626021,0.609195619805639),.UNSPECIFIED.);
#1656=B_SPLINE_CURVE_WITH_KNOTS('',3,(#127912,#127913,#127914,#127915,#127916,
#127917,#127918,#127919,#127920,#127921,#127922,#127923,#127924,#127925,
#127926,#127927,#127928,#127929,#127930,#127931,#127932,#127933,#127934,
#127935,#127936,#127937,#127938,#127939,#127940,#127941,#127942,#127943,
#127944,#127945,#127946,#127947,#127948,#127949,#127950,#127951,#127952,
#127953,#127954,#127955,#127956,#127957,#127958,#127959,#127960,#127961,
#127962,#127963,#127964,#127965,#127966,#127967,#127968,#127969,#127970,
#127971,#127972,#127973,#127974,#127975,#127976,#127977,#127978,#127979,
#127980,#127981,#127982,#127983,#127984,#127985,#127986,#127987,#127988,
#127989,#127990,#127991,#127992,#127993,#127994,#127995,#127996,#127997,
#127998,#127999,#128000,#128001,#128002,#128003,#128004,#128005,#128006,
#128007,#128008,#128009,#128010,#128011,#128012,#128013,#128014,#128015,
#128016,#128017,#128018,#128019,#128020,#128021,#128022,#128023,#128024,
#128025,#128026,#128027,#128028,#128029,#128030,#128031,#128032,#128033,
#128034,#128035,#128036,#128037,#128038,#128039,#128040,#128041,#128042,
#128043,#128044,#128045,#128046,#128047,#128048,#128049,#128050,#128051,
#128052,#128053,#128054,#128055,#128056,#128057,#128058,#128059,#128060,
#128061,#128062,#128063,#128064,#128065,#128066,#128067,#128068,#128069,
#128070,#128071,#128072,#128073,#128074,#128075,#128076,#128077,#128078,
#128079,#128080,#128081,#128082,#128083,#128084,#128085,#128086,#128087,
#128088,#128089,#128090,#128091,#128092,#128093,#128094,#128095,#128096,
#128097,#128098,#128099),.UNSPECIFIED.,.F.,.F.,(4,2,2,2,2,2,2,2,2,2,2,2,
2,2,2,2,2,2,2,2,2,2,2,2,2,2,2,2,2,2,2,2,2,2,2,2,2,2,2,2,2,2,2,2,2,2,2,2,
2,2,2,2,2,2,2,2,2,2,2,2,2,2,2,2,2,2,2,2,2,2,2,2,2,2,2,2,2,2,2,2,2,2,2,2,
2,2,2,2,2,2,2,2,2,4),(5.28102015283622E-5,0.00943930468759837,0.0136584492307033,
0.015350078067837,0.016722480911901,0.0182094940979389,0.0200110829088309,
0.024481371733638,0.0415374280043719,0.0566370430245147,0.0573842064374152,
0.0588664171978575,0.0590581142496318,0.0627484768252054,0.0653944205673456,
0.0681701130928783,0.0725493070509845,0.0955555996973102,0.104549675921614,
0.109923152915613,0.111989992268153,0.113466774101365,0.115186208271291,
0.118382598729794,0.131101908410891,0.142486572219041,0.154560154990933,
0.158443034388585,0.161122777535872,0.163847727456843,0.16796965475202,
0.18356756801777,0.195266214822312,0.204966827504056,0.207445173091656,
0.208995498356967,0.210565679766474,0.213137768772695,0.22391462815933,
0.241502950806235,0.248020485280757,0.253162610366718,0.256091017966324,
0.258687209439581,0.26202081568506,0.269433422636807,0.29255360431755,0.301080861792751,
0.303478172252538,0.305011843272254,0.306602299809132,0.30926959749595,
0.323933588846315,0.33772529688717,0.347094881854784,0.350701445715302,
0.353333829207641,0.356137147819951,0.360654259109438,0.382671153379249,
0.392146790415539,0.39769701183653,0.399787776390432,0.401267701438489,
0.402974118293782,0.406108992539898,0.421411792528695,0.434990439825889,
0.443370045702156,0.446847013982485,0.449460369231819,0.452315181419452,
0.457088513067437,0.484034309722774,0.49293939660373,0.495364979368958,
0.496904460196579,0.498292439523088,0.500720829281657,0.508895055080013,
0.528724418268833,0.538814464662127,0.542505308417374,0.545151401306737,
0.547594734661768,0.551661442879315,0.565353561274739,0.579655298254744,
0.588843029197885,0.591288270136979,0.592831733882104,0.594409860179039,
0.597019166477871,0.608918989341705),.UNSPECIFIED.);
#1657=B_SPLINE_CURVE_WITH_KNOTS('',3,(#128104,#128105,#128106,#128107,#128108,
#128109,#128110,#128111,#128112,#128113,#128114,#128115,#128116,#128117,
#128118,#128119,#128120,#128121,#128122,#128123,#128124,#128125,#128126,
#128127,#128128,#128129,#128130,#128131,#128132,#128133,#128134,#128135,
#128136,#128137,#128138,#128139,#128140,#128141,#128142,#128143,#128144,
#128145,#128146,#128147,#128148,#128149,#128150,#128151,#128152,#128153,
#128154,#128155,#128156,#128157,#128158,#128159,#128160,#128161,#128162,
#128163,#128164,#128165,#128166,#128167,#128168,#128169,#128170,#128171,
#128172,#128173,#128174,#128175,#128176,#128177,#128178,#128179,#128180,
#128181,#128182,#128183,#128184,#128185,#128186,#128187,#128188,#128189,
#128190,#128191,#128192,#128193,#128194,#128195,#128196,#128197,#128198,
#128199,#128200,#128201,#128202,#128203,#128204,#128205,#128206,#128207,
#128208,#128209,#128210,#128211,#128212,#128213,#128214,#128215,#128216,
#128217,#128218,#128219,#128220,#128221,#128222,#128223,#128224,#128225,
#128226,#128227,#128228,#128229,#128230,#128231,#128232,#128233,#128234,
#128235,#128236,#128237,#128238,#128239,#128240,#128241,#128242,#128243,
#128244,#128245,#128246,#128247,#128248,#128249,#128250,#128251,#128252,
#128253,#128254,#128255,#128256,#128257),.UNSPECIFIED.,.F.,.F.,(4,3,3,3,
3,3,3,3,3,3,3,3,3,3,3,3,3,3,3,3,3,3,3,3,3,3,3,3,3,3,3,3,3,3,3,3,3,3,3,3,
3,3,3,3,3,3,3,3,3,3,3,4),(-29.2243093234641,-29.0911455076753,-28.9577015471726,
-28.823781010616,-28.7578067271164,-28.6319159028052,-28.5062137687136,
-28.3806391369115,-28.2551310424176,-28.129531928478,-28.0038936673963,
-27.8780008716122,-27.7692014418906,-27.6433106177164,-27.5176084837613,
-27.3920338520949,-27.2665257577356,-27.1409266439278,-27.0152883829764,
-26.8893955873186,-26.7805961566649,-26.6547053325348,-26.5290031986255,
-26.4034285670066,-26.2779204726964,-26.1523213589396,-26.0266830980403,
-25.9007903024356,-25.7919908714392,-25.6661000466945,-25.5403979121686,
-25.4148232799325,-25.2893151850059,-25.1637160706394,-25.0380778091335,
-24.9121850129357,-24.8033855862134,-24.6774947626185,-24.5517926292399,
-24.4262179981462,-24.3007099043544,-24.1751107911009,-24.0494725306974,
-23.9235797355689,-23.8147803009877,-23.6905595755302,-23.566526324309,
-23.4426162002402,-23.3172456242379,-23.1933193126604,-23.0672266044457,
-22.941133896231),.UNSPECIFIED.);
#1658=B_SPLINE_CURVE_WITH_KNOTS('',3,(#128258,#128259,#128260,#128261,#128262,
#128263,#128264,#128265,#128266,#128267,#128268,#128269,#128270,#128271,
#128272,#128273,#128274,#128275,#128276,#128277,#128278,#128279,#128280,
#128281,#128282,#128283,#128284,#128285,#128286,#128287,#128288,#128289,
#128290,#128291,#128292,#128293,#128294,#128295,#128296,#128297,#128298,
#128299,#128300,#128301,#128302,#128303,#128304,#128305,#128306,#128307,
#128308,#128309,#128310,#128311,#128312,#128313,#128314,#128315,#128316,
#128317,#128318,#128319,#128320,#128321,#128322,#128323,#128324,#128325,
#128326,#128327,#128328,#128329,#128330,#128331,#128332,#128333,#128334,
#128335,#128336,#128337,#128338,#128339,#128340,#128341,#128342,#128343,
#128344,#128345,#128346,#128347,#128348,#128349,#128350,#128351,#128352,
#128353,#128354,#128355,#128356,#128357,#128358,#128359,#128360,#128361,
#128362,#128363,#128364,#128365,#128366,#128367,#128368,#128369,#128370,
#128371,#128372,#128373,#128374,#128375,#128376,#128377,#128378,#128379,
#128380,#128381,#128382,#128383,#128384,#128385,#128386,#128387,#128388,
#128389,#128390,#128391,#128392,#128393,#128394,#128395,#128396,#128397,
#128398,#128399,#128400,#128401,#128402,#128403,#128404,#128405,#128406,
#128407,#128408,#128409,#128410,#128411,#128412,#128413,#128414,#128415,
#128416,#128417,#128418,#128419,#128420,#128421,#128422,#128423,#128424,
#128425,#128426,#128427,#128428,#128429,#128430,#128431,#128432,#128433,
#128434,#128435),.UNSPECIFIED.,.F.,.F.,(4,2,2,2,2,2,2,2,2,2,2,2,2,2,2,2,
2,2,2,2,2,2,2,2,2,2,2,2,2,2,2,2,2,2,2,2,2,2,2,2,2,2,2,2,2,2,2,2,2,2,2,2,
2,2,2,2,2,2,2,2,2,2,2,2,2,2,2,2,2,2,2,2,2,2,2,2,2,2,2,2,2,2,2,2,2,2,2,2,
4),(0.608918989341705,0.632484436711806,0.637273809156127,0.640131774699361,
0.642744032348447,0.646213563623638,0.654541386609907,0.667973786822127,
0.683457893919245,0.686599175903856,0.688306897401734,0.689786345308303,
0.691874324148808,0.697404001959282,0.706823346973857,0.728972833995634,
0.733474289118519,0.736274343968621,0.738907918764235,0.742522989269425,
0.751964794522928,0.765674055561374,0.780303875070739,0.782969515737605,
0.784559545195217,0.786093298710694,0.788491532060691,0.797030781120296,
0.820237459707686,0.827591627808917,0.830915854723068,0.833510868366637,
0.836444335081826,0.841613195675993,0.848176484966463,0.866064239814026,
0.876456469708276,0.879010354951903,0.880576553732779,0.882130191610296,
0.884624970483063,0.894601588162329,0.910884464927515,0.922141959064336,
0.926017983330025,0.928428747876728,0.931103967257791,0.934963560827957,
0.946770646479986,0.958401217906793,0.971160568215792,0.974358619255303,
0.97607824984295,0.977554668640882,0.979620354387249,0.984986735521101,
0.99396307148355,1.01702366990304,1.02139639696923,1.02417049213732,1.02681661387665,
1.03051008576096,1.04062992210639,1.0606214488029,1.06860239311554,1.07101249078323,
1.07239689032026,1.07393981267283,1.07638331109697,1.08554723066564,1.10040223557177,
1.11362534522306,1.11767233363091,1.12011197650495,1.12276016036437,1.12646557909108,
1.13669345648822,1.1572378961673,1.16464061788624,1.16699804118402,1.16837290655736,
1.16992817595086,1.17243062336994,1.18254094045894,1.19737834953709,1.20973700949331,
1.2136250316396,1.2159190614085,1.21794213992136),.UNSPECIFIED.);
#1659=B_SPLINE_CURVE_WITH_KNOTS('',3,(#128440,#128441,#128442,#128443,#128444,
#128445,#128446,#128447,#128448,#128449,#128450,#128451,#128452,#128453,
#128454,#128455,#128456,#128457,#128458,#128459,#128460,#128461,#128462,
#128463,#128464,#128465,#128466,#128467,#128468,#128469,#128470,#128471,
#128472,#128473,#128474,#128475,#128476,#128477,#128478,#128479,#128480,
#128481,#128482,#128483,#128484,#128485,#128486,#128487,#128488,#128489,
#128490,#128491,#128492,#128493,#128494,#128495,#128496,#128497,#128498,
#128499,#128500,#128501,#128502,#128503,#128504,#128505,#128506,#128507,
#128508,#128509,#128510,#128511,#128512,#128513,#128514,#128515,#128516,
#128517,#128518,#128519,#128520,#128521,#128522,#128523,#128524,#128525,
#128526,#128527,#128528,#128529,#128530,#128531,#128532,#128533,#128534,
#128535,#128536,#128537,#128538,#128539,#128540,#128541,#128542,#128543,
#128544,#128545,#128546,#128547,#128548,#128549,#128550,#128551,#128552,
#128553,#128554,#128555,#128556,#128557,#128558,#128559,#128560,#128561,
#128562,#128563,#128564,#128565,#128566,#128567,#128568,#128569,#128570,
#128571,#128572,#128573,#128574,#128575,#128576,#128577,#128578,#128579,
#128580,#128581,#128582,#128583,#128584,#128585,#128586,#128587,#128588,
#128589,#128590,#128591,#128592,#128593,#128594,#128595,#128596,#128597,
#128598,#128599,#128600,#128601,#128602,#128603,#128604,#128605,#128606,
#128607,#128608,#128609,#128610,#128611,#128612,#128613),.UNSPECIFIED.,
 .F.,.F.,(4,2,2,2,2,2,2,2,2,2,2,2,2,2,2,2,2,2,2,2,2,2,2,2,2,2,2,2,2,2,2,
2,2,2,2,2,2,2,2,2,2,2,2,2,2,2,2,2,2,2,2,2,2,2,2,2,2,2,2,2,2,2,2,2,2,2,2,
2,2,2,2,2,2,2,2,2,2,2,2,2,2,2,2,2,2,2,4),(0.60887951146085,0.63078846196145,
0.636246071514392,0.639327828687595,0.641978652326842,0.645332871968072,
0.652473656908019,0.662838048063838,0.679225586919404,0.684888859343448,
0.687090294742984,0.688625163796033,0.690377561068731,0.693666908008892,
0.706172946614204,0.728420820783908,0.732952316780898,0.735820161194292,
0.73855611564422,0.742383636555123,0.7530970173112,0.776415355770046,0.781045890247718,
0.782906669269154,0.784442815939323,0.786190758553567,0.789458148429817,
0.801761723123946,0.824340727456653,0.828825622237181,0.831684162025967,
0.834425220388517,0.838283641176352,0.849303731922222,0.869851599669049,
0.876304128448469,0.878607601932729,0.88014339990219,0.881845072863965,
0.884886194535029,0.900814123069112,0.919405902405354,0.924273431886802,
0.927208019920632,0.929914422328036,0.933552900126604,0.942638452712715,
0.958293277779198,0.970324330388045,0.973530591100979,0.975284783676508,
0.976818788544093,0.979015726960102,0.98508074568147,0.995981619500491,
1.01524747154595,1.0200880836682,1.02301732688048,1.02572563834081,1.02937727686331,
1.03856518792535,1.05457076711339,1.06715902030929,1.06982112990831,1.07144311326391,
1.07304999990307,1.07564079581327,1.08651692922536,1.11178506740517,1.11625085324721,
1.11910537720804,1.1218482805648,1.12571905643322,1.13686879287472,1.1488418285501,
1.16184046939339,1.16509218560743,1.16685590326623,1.16838706086445,1.17056466767868,
1.17647680310206,1.18691247212009,1.20692216688272,1.21162581167888,1.21450938681323,
1.21633432088655,1.21787769075378),.UNSPECIFIED.);
#1660=B_SPLINE_CURVE_WITH_KNOTS('',3,(#128614,#128615,#128616,#128617,#128618,
#128619,#128620,#128621,#128622,#128623,#128624,#128625,#128626,#128627,
#128628,#128629,#128630,#128631,#128632,#128633,#128634,#128635,#128636,
#128637,#128638,#128639,#128640,#128641,#128642,#128643,#128644,#128645,
#128646,#128647,#128648,#128649,#128650,#128651,#128652,#128653,#128654,
#128655,#128656,#128657,#128658,#128659,#128660,#128661,#128662,#128663,
#128664,#128665,#128666,#128667,#128668,#128669,#128670,#128671,#128672,
#128673,#128674,#128675,#128676,#128677,#128678,#128679,#128680,#128681,
#128682,#128683,#128684,#128685,#128686,#128687,#128688,#128689,#128690,
#128691,#128692,#128693,#128694,#128695,#128696,#128697,#128698,#128699,
#128700,#128701,#128702,#128703,#128704,#128705,#128706,#128707,#128708,
#128709,#128710,#128711,#128712,#128713,#128714,#128715,#128716,#128717,
#128718,#128719,#128720,#128721,#128722,#128723,#128724,#128725,#128726,
#128727,#128728,#128729,#128730,#128731,#128732,#128733,#128734,#128735,
#128736,#128737,#128738,#128739,#128740,#128741,#128742,#128743,#128744,
#128745,#128746,#128747,#128748,#128749,#128750,#128751,#128752,#128753,
#128754,#128755,#128756,#128757,#128758,#128759,#128760,#128761,#128762,
#128763,#128764,#128765,#128766,#128767,#128768,#128769,#128770,#128771,
#128772,#128773,#128774,#128775,#128776,#128777,#128778,#128779,#128780,
#128781,#128782,#128783,#128784,#128785,#128786,#128787,#128788,#128789,
#128790,#128791),.UNSPECIFIED.,.F.,.F.,(4,2,2,2,2,2,2,2,2,2,2,2,2,2,2,2,
2,2,2,2,2,2,2,2,2,2,2,2,2,2,2,2,2,2,2,2,2,2,2,2,2,2,2,2,2,2,2,2,2,2,2,2,
2,2,2,2,2,2,2,2,2,2,2,2,2,2,2,2,2,2,2,2,2,2,2,2,2,2,2,2,2,2,2,2,2,2,2,2,
4),(8.19526309981665E-5,0.00244591647159546,0.00565097144129316,0.0199149569692758,
0.0346688995672485,0.0401375564983184,0.0439812982325549,0.0458055837598293,
0.0472688651094312,0.0491522821191064,0.0534505013740185,0.0774954801291768,
0.0882801505299676,0.0920443731556304,0.0947027717025768,0.0971306863623881,
0.101108584909388,0.113304743877449,0.128199856417806,0.138358251533931,
0.140863250575921,0.142419113123174,0.143983132271331,0.146526606389028,
0.156612415718612,0.174766481132769,0.181372385347927,0.186565427051088,
0.189503749625414,0.192098088266055,0.195414590006257,0.202437264464677,
0.224067039983559,0.231008360773772,0.235545672652667,0.237488118646269,
0.238813405926997,0.24054720908878,0.243812627023049,0.264827399178171,
0.274644925797415,0.281500937427829,0.284743957184957,0.287332042226077,
0.290318764903073,0.295607812312921,0.321605051886933,0.330427486138935,
0.332846830259632,0.334384888614309,0.33577375103773,0.338207607091329,
0.346450387533153,0.366212155480024,0.37628750741496,0.379976352313982,
0.382621825170941,0.385397563055197,0.389778004250474,0.412770634735769,
0.421769357309952,0.427144369638574,0.429211275916643,0.43068793648639,
0.432407029232186,0.435602298287446,0.448305247961947,0.459984858139832,
0.467953544759689,0.473896732047786,0.476978724664271,0.47956182752582,
0.482689285081147,0.488682379930929,0.511611371954516,0.522106312313085,
0.524629487098124,0.526189242649236,0.527561164028974,0.529901660446056,
0.53711005792618,0.55785815136795,0.568126553747768,0.571836688000997,0.574485777607362,
0.576924569385596,0.580966197696916,0.594087692635498,0.609138008733486),
 .UNSPECIFIED.);
#1661=B_SPLINE_CURVE_WITH_KNOTS('',3,(#128796,#128797,#128798,#128799,#128800,
#128801,#128802,#128803,#128804,#128805,#128806,#128807,#128808,#128809,
#128810,#128811,#128812,#128813,#128814,#128815,#128816,#128817,#128818,
#128819,#128820,#128821,#128822,#128823,#128824,#128825,#128826,#128827,
#128828,#128829,#128830,#128831,#128832,#128833,#128834,#128835,#128836,
#128837,#128838,#128839,#128840,#128841,#128842,#128843,#128844,#128845,
#128846,#128847,#128848,#128849,#128850,#128851,#128852,#128853,#128854,
#128855,#128856,#128857,#128858,#128859,#128860,#128861,#128862,#128863,
#128864,#128865,#128866,#128867,#128868,#128869,#128870,#128871,#128872,
#128873,#128874,#128875,#128876,#128877,#128878,#128879,#128880,#128881,
#128882,#128883,#128884,#128885,#128886,#128887,#128888,#128889,#128890,
#128891,#128892,#128893,#128894,#128895,#128896,#128897,#128898,#128899,
#128900,#128901,#128902,#128903,#128904,#128905,#128906,#128907,#128908,
#128909,#128910,#128911,#128912,#128913,#128914,#128915,#128916,#128917,
#128918,#128919,#128920,#128921,#128922,#128923,#128924,#128925,#128926,
#128927,#128928,#128929,#128930,#128931,#128932,#128933,#128934,#128935,
#128936,#128937,#128938,#128939,#128940,#128941,#128942,#128943,#128944,
#128945,#128946,#128947,#128948,#128949,#128950,#128951,#128952,#128953,
#128954,#128955,#128956,#128957,#128958,#128959,#128960,#128961,#128962,
#128963,#128964,#128965,#128966,#128967,#128968,#128969,#128970,#128971,
#128972,#128973,#128974,#128975),.UNSPECIFIED.,.F.,.F.,(4,2,2,2,2,2,2,2,
2,2,2,2,2,2,2,2,2,2,2,2,2,2,2,2,2,2,2,2,2,2,2,2,2,2,2,2,2,2,2,2,2,2,2,2,
2,2,2,2,2,2,2,2,2,2,2,2,2,2,2,2,2,2,2,2,2,2,2,2,2,2,2,2,2,2,2,2,2,2,2,2,
2,2,2,2,2,2,2,2,2,4),(5.12893345518819E-5,0.00961602028826353,0.0138783864723404,
0.0156577421109236,0.0170829123827336,0.0186135194993552,0.0207841578286592,
0.0262525119274115,0.0479517746797167,0.058911971909783,0.0628681794158502,
0.0656265742126552,0.0681264307526814,0.072186322735615,0.0840825386761356,
0.0991420979771004,0.10923377375189,0.111783160187943,0.113381645735688,
0.115013709611778,0.117722508140764,0.132281156871619,0.146032956853938,
0.155390619215895,0.159064220483621,0.161776114995443,0.164697371586683,
0.169496306846321,0.189372877381887,0.199890315284252,0.205830294353542,
0.208011752229538,0.209543788477623,0.211306257456261,0.21455078464435,
0.227436396483612,0.239609130322308,0.250725515970482,0.254593950766497,
0.257336970593552,0.260193122774559,0.264664753603286,0.289900385296866,
0.300787723467629,0.303379280451442,0.30498658958962,0.306608894513891,
0.309271446940452,0.321678209138169,0.33783682768254,0.347070195129053,
0.350728277760952,0.353437994709968,0.356365584223798,0.361195850267435,
0.380634609718299,0.39141847616228,0.397446093878205,0.399638629425916,
0.401172283903535,0.402929258052662,0.40614760768069,0.418485323473566,
0.433927164536807,0.442950562303215,0.446581596511575,0.4492873896495,0.452225977633481,
0.457111666114936,0.473971883262096,0.486538924812271,0.491039882527733,
0.494396709786513,0.496162646300481,0.497693793009992,0.499868740166097,
0.505364259950254,0.52720459259777,0.538212727787643,0.542070519412112,
0.54481173291316,0.547670938937443,0.552158024087738,0.577320729651941,
0.588246094979848,0.590839482092983,0.592447175756965,0.594069070452291,
0.596729685440606,0.60887951146085),.UNSPECIFIED.);
#1662=B_SPLINE_CURVE_WITH_KNOTS('',3,(#128976,#128977,#128978,#128979,#128980,
#128981,#128982,#128983,#128984,#128985,#128986,#128987,#128988,#128989,
#128990,#128991,#128992,#128993,#128994,#128995,#128996,#128997,#128998,
#128999,#129000,#129001,#129002,#129003,#129004,#129005,#129006,#129007,
#129008,#129009,#129010,#129011,#129012,#129013,#129014,#129015,#129016,
#129017,#129018,#129019,#129020,#129021,#129022,#129023,#129024,#129025,
#129026,#129027,#129028,#129029,#129030,#129031,#129032,#129033,#129034,
#129035,#129036,#129037,#129038,#129039,#129040,#129041,#129042,#129043,
#129044,#129045,#129046,#129047,#129048,#129049,#129050,#129051,#129052,
#129053,#129054,#129055,#129056,#129057,#129058,#129059,#129060,#129061,
#129062,#129063,#129064,#129065,#129066,#129067,#129068,#129069,#129070,
#129071,#129072,#129073,#129074,#129075,#129076,#129077,#129078,#129079,
#129080,#129081,#129082,#129083,#129084,#129085,#129086,#129087,#129088,
#129089,#129090,#129091,#129092,#129093,#129094,#129095,#129096,#129097,
#129098,#129099,#129100,#129101,#129102,#129103,#129104,#129105,#129106,
#129107,#129108,#129109,#129110,#129111,#129112,#129113,#129114,#129115,
#129116,#129117,#129118,#129119,#129120,#129121,#129122,#129123,#129124,
#129125,#129126,#129127,#129128,#129129,#129130,#129131,#129132,#129133,
#129134,#129135,#129136,#129137,#129138,#129139,#129140,#129141,#129142,
#129143,#129144,#129145,#129146,#129147,#129148,#129149,#129150,#129151,
#129152,#129153,#129154,#129155,#129156,#129157,#129158,#129159),
 .UNSPECIFIED.,.F.,.F.,(4,2,2,2,2,2,2,2,2,2,2,2,2,2,2,2,2,2,2,2,2,2,2,2,
2,2,2,2,2,2,2,2,2,2,2,2,2,2,2,2,2,2,2,2,2,2,2,2,2,2,2,2,2,2,2,2,2,2,2,2,
2,2,2,2,2,2,2,2,2,2,2,2,2,2,2,2,2,2,2,2,2,2,2,2,2,2,2,2,2,2,2,4),(0.609138008733486,
0.618121686590817,0.620604124036998,0.622002105544986,0.623530686121969,
0.625903148796938,0.63411857238587,0.654830264979436,0.664113515625273,
0.667800981357054,0.670420033508957,0.673189666814462,0.677539534727236,
0.682745306721759,0.69406344669956,0.712962843599388,0.716008422889573,
0.717695663655213,0.719180811500166,0.721309152445293,0.727149459063446,
0.737458921942084,0.757930808098366,0.762629080484255,0.765468653405884,
0.768086592985896,0.771597950377354,0.78023050055152,0.794553633104294,
0.808650559203278,0.81183956428775,0.813557331675355,0.815034252303567,
0.81710348489575,0.82249526626144,0.831539337123217,0.854458488696198,0.858852055941957,
0.861630393630956,0.8642744036964,0.867954663137728,0.877955158175062,0.897367019277808,
0.90597650074626,0.90843761403847,0.909831549257518,0.911364091088334,0.913756465787837,
0.922220946046426,0.944802275419074,0.95250189492096,0.955923107500246,
0.958536786579955,0.961388948826537,0.966150409850912,0.981025765637848,
0.998392295653103,1.0029525356252,1.00474845045902,1.00623414369772,1.00791926860864,
1.01104118184762,1.02241662056397,1.04442112541473,1.04979707790695,1.05280145201634,
1.05538771208352,1.05860610285131,1.06531789688386,1.07482667917306,1.09400778017891,
1.09875486238431,1.10059770369467,1.10207878647515,1.10372980381599,1.10668617869406,
1.1212735270503,1.14167830590248,1.14637186445387,1.14921010743941,1.15182777682574,
1.15534023905504,1.16394194266049,1.17820731836293,1.19226971700874,1.19552429316274,
1.19725560607294,1.19858093669015,1.20002590475801,1.2019659721872,1.20634034158939,
1.21790188230871),.UNSPECIFIED.);
#1663=B_SPLINE_CURVE_WITH_KNOTS('',3,(#129164,#129165,#129166,#129167,#129168,
#129169,#129170,#129171,#129172,#129173,#129174,#129175,#129176,#129177,
#129178,#129179,#129180,#129181,#129182,#129183,#129184,#129185,#129186,
#129187,#129188,#129189,#129190,#129191,#129192,#129193,#129194,#129195,
#129196,#129197,#129198,#129199,#129200,#129201,#129202,#129203,#129204,
#129205,#129206,#129207,#129208,#129209,#129210,#129211,#129212,#129213,
#129214,#129215,#129216,#129217,#129218,#129219,#129220,#129221,#129222,
#129223,#129224,#129225,#129226,#129227,#129228,#129229,#129230,#129231,
#129232,#129233,#129234,#129235,#129236,#129237,#129238,#129239,#129240,
#129241,#129242,#129243,#129244,#129245,#129246,#129247,#129248,#129249,
#129250,#129251,#129252,#129253,#129254,#129255,#129256,#129257,#129258,
#129259,#129260,#129261,#129262,#129263,#129264,#129265,#129266,#129267,
#129268,#129269,#129270,#129271,#129272,#129273,#129274,#129275,#129276,
#129277,#129278,#129279,#129280,#129281,#129282,#129283,#129284,#129285,
#129286,#129287,#129288,#129289,#129290,#129291,#129292,#129293,#129294,
#129295,#129296,#129297,#129298,#129299,#129300,#129301,#129302,#129303,
#129304,#129305,#129306,#129307,#129308,#129309,#129310,#129311,#129312,
#129313,#129314,#129315,#129316,#129317,#129318,#129319,#129320,#129321,
#129322,#129323,#129324,#129325,#129326,#129327,#129328,#129329,#129330,
#129331,#129332,#129333,#129334,#129335,#129336,#129337),.UNSPECIFIED.,
 .F.,.F.,(4,2,2,2,2,2,2,2,2,2,2,2,2,2,2,2,2,2,2,2,2,2,2,2,2,2,2,2,2,2,2,
2,2,2,2,2,2,2,2,2,2,2,2,2,2,2,2,2,2,2,2,2,2,2,2,2,2,2,2,2,2,2,2,2,2,2,2,
2,2,2,2,2,2,2,2,2,2,2,2,2,2,2,2,2,2,2,4),(0.609294493087457,0.612279274065476,
0.61497192061227,0.618502815827184,0.626793786753854,0.640018988953453,
0.655625305147717,0.658796725165967,0.660543726057257,0.662080335124041,
0.664293274988974,0.670486473944873,0.68179004732075,0.700448315669616,
0.705315168785881,0.708250050099495,0.710957161248477,0.714597268008012,
0.723691275086161,0.739371403554182,0.751376313844737,0.754582274304652,
0.756336637342183,0.757871039088155,0.760068886138465,0.76613869369244,
0.777052709909105,0.796305799994951,0.801148381623591,0.804078446237653,
0.806787284056524,0.810439270506911,0.819625663961472,0.835622484328683,
0.848230270695418,0.850893023069629,0.852515373479983,0.854122598581708,
0.856713901661463,0.867591207402952,0.892867173331642,0.89733344193225,
0.900188491779084,0.902932052294452,0.906804016152967,0.917959726214802,
0.929939874734508,0.942933487951805,0.94618533305264,0.947949313116664,
0.949480837750616,0.951659156849383,0.957574444124615,0.968017960039134,
0.988040341506333,0.992828943200652,0.995748063367594,0.99846059597962,
1.00213919537037,1.01153908642404,1.02830423792746,1.0398852037876,1.04253440435527,
1.04415378920164,1.04576353760859,1.0483672901349,1.05951348088051,1.08427736603894,
1.08885034179558,1.09172635390582,1.09445781871163,1.09825854854641,1.10871823539971,
1.13038334860397,1.13650879204335,1.13877187099174,1.14030100385222,1.14201899391671,
1.14513920447827,1.15615698640013,1.1801774311948,1.18471024799207,1.18757814899122,
1.19031362350176,1.1941395743653,1.19983412647968,1.2183544972758),
 .UNSPECIFIED.);
#1664=B_SPLINE_CURVE_WITH_KNOTS('',3,(#129338,#129339,#129340,#129341,#129342,
#129343,#129344,#129345,#129346,#129347,#129348,#129349,#129350,#129351,
#129352,#129353,#129354,#129355,#129356,#129357,#129358,#129359,#129360,
#129361,#129362,#129363,#129364,#129365,#129366,#129367,#129368,#129369,
#129370,#129371,#129372,#129373,#129374,#129375,#129376,#129377,#129378,
#129379,#129380,#129381,#129382,#129383,#129384,#129385,#129386,#129387,
#129388,#129389,#129390,#129391,#129392,#129393,#129394,#129395,#129396,
#129397,#129398,#129399,#129400,#129401,#129402,#129403,#129404,#129405,
#129406,#129407,#129408,#129409,#129410,#129411,#129412,#129413,#129414,
#129415,#129416,#129417,#129418,#129419,#129420,#129421,#129422,#129423,
#129424,#129425,#129426,#129427,#129428,#129429,#129430,#129431,#129432,
#129433,#129434,#129435,#129436,#129437,#129438,#129439,#129440,#129441,
#129442,#129443,#129444,#129445,#129446,#129447,#129448,#129449,#129450,
#129451,#129452,#129453,#129454,#129455,#129456,#129457,#129458,#129459,
#129460,#129461,#129462,#129463,#129464,#129465,#129466,#129467,#129468,
#129469,#129470,#129471,#129472,#129473,#129474,#129475,#129476,#129477,
#129478,#129479,#129480,#129481,#129482,#129483,#129484,#129485,#129486,
#129487,#129488,#129489,#129490,#129491,#129492,#129493,#129494,#129495,
#129496,#129497,#129498,#129499,#129500,#129501,#129502,#129503,#129504,
#129505,#129506,#129507,#129508,#129509,#129510,#129511,#129512,#129513,
#129514,#129515),.UNSPECIFIED.,.F.,.F.,(4,2,2,2,2,2,2,2,2,2,2,2,2,2,2,2,
2,2,2,2,2,2,2,2,2,2,2,2,2,2,2,2,2,2,2,2,2,2,2,2,2,2,2,2,2,2,2,2,2,2,2,2,
2,2,2,2,2,2,2,2,2,2,2,2,2,2,2,2,2,2,2,2,2,2,2,2,2,2,2,2,2,2,2,2,2,2,2,2,
4),(4.48084807998542E-5,0.0151895777249643,0.0211597089994056,0.0241810351308087,
0.0270781628467691,0.0296805266355577,0.0330134375814879,0.0403420703475364,
0.0634508972498917,0.0719769345664564,0.0743741833310849,0.0759078615777264,
0.0774983741590798,0.0801658532645623,0.0948327763534422,0.108628642746622,
0.117993146897431,0.121599128960157,0.124231455826626,0.127035048151024,
0.131553364787702,0.153562173692234,0.163042257784255,0.168594117172197,
0.170685122280674,0.172165100115765,0.173871437850454,0.177005853269734,
0.192680303941157,0.206009550050221,0.214300926818803,0.217765564950306,
0.220377299650659,0.223237750965991,0.228039007803243,0.24694125143082,
0.258209233169335,0.264360434034748,0.266527086387937,0.26801828057052,
0.269688169226704,0.272734729901128,0.293979348286441,0.303918578330245,
0.310830813132952,0.314083363529147,0.316672281479533,0.319652574267506,
0.32490979924372,0.350959712738519,0.359787274778588,0.362207103561469,
0.363745325806985,0.365134213070399,0.367567889566214,0.375807187632045,
0.395573891358208,0.405650631215977,0.40933979037851,0.411985441904402,
0.414761326339755,0.419141909308159,0.4421368705191,0.451135727455969,0.456510915015384,
0.458577927971528,0.460054677603236,0.461773889507287,0.464969415388399,
0.478839018033031,0.493329402537119,0.502017403090592,0.505536464241162,
0.50815563162367,0.510992255872711,0.515675363887792,0.536284222426344,
0.546504997765943,0.552315476919564,0.554440061815629,0.555924742939173,
0.557613938883323,0.560668397200182,0.577529839932072,0.596420446495926,
0.600616890931166,0.603356196005889,0.605993806741988,0.609188119348819),
 .UNSPECIFIED.);
#1665=B_SPLINE_CURVE_WITH_KNOTS('',3,(#129520,#129521,#129522,#129523,#129524,
#129525,#129526,#129527,#129528,#129529,#129530,#129531,#129532,#129533,
#129534,#129535,#129536,#129537,#129538,#129539,#129540,#129541,#129542,
#129543,#129544,#129545,#129546,#129547,#129548,#129549,#129550,#129551,
#129552,#129553,#129554,#129555,#129556,#129557,#129558,#129559,#129560,
#129561,#129562,#129563,#129564,#129565,#129566,#129567,#129568,#129569,
#129570,#129571,#129572,#129573,#129574,#129575,#129576,#129577,#129578,
#129579,#129580,#129581,#129582,#129583,#129584,#129585,#129586,#129587,
#129588,#129589,#129590,#129591,#129592,#129593,#129594,#129595,#129596,
#129597,#129598,#129599,#129600,#129601,#129602,#129603,#129604,#129605,
#129606,#129607,#129608,#129609,#129610,#129611,#129612,#129613,#129614,
#129615,#129616,#129617,#129618,#129619,#129620,#129621,#129622,#129623,
#129624,#129625,#129626,#129627,#129628,#129629,#129630,#129631,#129632,
#129633,#129634,#129635,#129636,#129637,#129638,#129639,#129640,#129641,
#129642,#129643,#129644,#129645,#129646,#129647,#129648,#129649,#129650,
#129651,#129652,#129653,#129654,#129655,#129656,#129657,#129658,#129659,
#129660,#129661,#129662,#129663,#129664,#129665,#129666,#129667,#129668,
#129669,#129670,#129671,#129672,#129673,#129674,#129675,#129676,#129677,
#129678,#129679,#129680,#129681,#129682,#129683,#129684,#129685,#129686,
#129687,#129688,#129689,#129690,#129691),.UNSPECIFIED.,.F.,.F.,(4,2,2,2,
2,2,2,2,2,2,2,2,2,2,2,2,2,2,2,2,2,2,2,2,2,2,2,2,2,2,2,2,2,2,2,2,2,2,2,2,
2,2,2,2,2,2,2,2,2,2,2,2,2,2,2,2,2,2,2,2,2,2,2,2,2,2,2,2,2,2,2,2,2,2,2,2,
2,2,2,2,2,2,2,2,2,4),(0.00027441463337703,0.0227636344260558,0.0322427410889548,
0.0359313348477803,0.0386454365053149,0.0415608691984186,0.0463307052750516,
0.0665447975002483,0.0768652460854365,0.0827392509239614,0.0849122885035225,
0.086443149400746,0.0882099542434203,0.0914751140924374,0.104518576206399,
0.116544106461167,0.127622856500184,0.131487565135147,0.134229917503476,
0.137087068379059,0.141563916580247,0.166774405195101,0.177674564619549,
0.180266706225982,0.181874119018986,0.183496253788006,0.186158086626929,
0.198445734692305,0.214691712589056,0.223949729926721,0.227610891672681,
0.230321020449478,0.233247305120228,0.238071189693857,0.257608118769696,
0.268331010584425,0.274338721466226,0.276528746899259,0.278062024199386,
0.27982021575149,0.283044381765916,0.295530276535114,0.307737121188378,
0.319181811325464,0.323081586699972,0.325830046824822,0.328340183557665,
0.332461613406117,0.345746920269917,0.36046451453457,0.369508991325578,
0.371990971145363,0.373575722034662,0.375019587866653,0.377585796594849,
0.387019427809224,0.405546790550378,0.415387362640507,0.419119158255573,
0.421839786027067,0.424739208246939,0.429429073363312,0.450413828377309,
0.460308783189393,0.464259933572517,0.467307768497564,0.469010982618376,
0.470546401756773,0.472846809297149,0.479271700426983,0.500640134566339,
0.511052030554104,0.514848043354771,0.517578929586235,0.520456799323398,
0.525038297061851,0.549748520976427,0.560913927729103,0.563518437595197,
0.565128442483085,0.566747808622801,0.569396625300546,0.58094472891131,
0.597752195824288,0.604176596763572,0.609294493087457),.UNSPECIFIED.);
#1666=B_SPLINE_CURVE_WITH_KNOTS('',3,(#129692,#129693,#129694,#129695,#129696,
#129697,#129698,#129699,#129700,#129701,#129702,#129703,#129704,#129705,
#129706,#129707,#129708,#129709,#129710,#129711,#129712,#129713,#129714,
#129715,#129716,#129717,#129718,#129719,#129720,#129721,#129722,#129723,
#129724,#129725,#129726,#129727,#129728,#129729,#129730,#129731,#129732,
#129733,#129734,#129735,#129736,#129737,#129738,#129739,#129740,#129741,
#129742,#129743,#129744,#129745,#129746,#129747,#129748,#129749,#129750,
#129751,#129752,#129753,#129754,#129755,#129756,#129757,#129758,#129759,
#129760,#129761,#129762,#129763,#129764,#129765,#129766,#129767,#129768,
#129769,#129770,#129771,#129772,#129773,#129774,#129775,#129776,#129777,
#129778,#129779,#129780,#129781,#129782,#129783,#129784,#129785,#129786,
#129787,#129788,#129789,#129790,#129791,#129792,#129793,#129794,#129795,
#129796,#129797,#129798,#129799,#129800,#129801,#129802,#129803,#129804,
#129805,#129806,#129807,#129808,#129809,#129810,#129811,#129812,#129813,
#129814,#129815,#129816,#129817,#129818,#129819,#129820,#129821,#129822,
#129823,#129824,#129825,#129826,#129827,#129828,#129829,#129830,#129831,
#129832,#129833,#129834,#129835,#129836,#129837,#129838,#129839,#129840,
#129841,#129842,#129843,#129844,#129845,#129846,#129847,#129848,#129849,
#129850,#129851,#129852,#129853,#129854,#129855,#129856,#129857,#129858,
#129859,#129860,#129861,#129862,#129863,#129864,#129865,#129866,#129867),
 .UNSPECIFIED.,.F.,.F.,(4,2,2,2,2,2,2,2,2,2,2,2,2,2,2,2,2,2,2,2,2,2,2,2,
2,2,2,2,2,2,2,2,2,2,2,2,2,2,2,2,2,2,2,2,2,2,2,2,2,2,2,2,2,2,2,2,2,2,2,2,
2,2,2,2,2,2,2,2,2,2,2,2,2,2,2,2,2,2,2,2,2,2,2,2,2,2,2,4),(0.609188119348819,
0.618088851492723,0.633251114555404,0.646123396145481,0.649328424879929,
0.651049569329106,0.652525729076646,0.654588946612196,0.659937032324217,
0.668864420913284,0.692031038401225,0.696388585364891,0.699159732645307,
0.701807663723004,0.705511420767342,0.715723765954798,0.73618623161773,
0.743675524160358,0.746040354126816,0.747416559450016,0.748970029804227,
0.75146388487105,0.761423724940592,0.777623940814963,0.788967600956461,
0.79285090894607,0.795262921885291,0.797936912129993,0.801789426093628,
0.813514444614515,0.825109158173883,0.837991138658734,0.841196760179125,
0.842918011848968,0.844394116928159,0.846457059844592,0.851803317821929,
0.860725937879379,0.883902030814145,0.888258056202085,0.891028868527889,
0.893676917724308,0.897381577058123,0.907602576370799,0.928110941942554,
0.935551435755209,0.937912091513974,0.939287532172419,0.940841992354981,
0.94334062461135,0.953383857780236,0.96999816569416,0.972396809936449,0.981382967455826,
0.985030666058229,0.987669352280554,0.990458136533524,0.9949039347227,1.00026281686337,
1.01217754719982,1.03026941080494,1.03327206851665,1.03493281777466,1.03642727176729,
1.0386146786155,1.04494293428585,1.05679214336884,1.07487141672425,1.0796911322994,
1.08255510669432,1.08516547322749,1.08862146343895,1.09685403931589,1.11002083763632,
1.12593023907983,1.1290533738711,1.13075719629866,1.13223758013055,1.13433276094272,
1.13991693633654,1.1494881249364,1.17133428962439,1.17587548115476,1.17868344602129,
1.18131339927006,1.18490578156157,1.19416368997785,1.21816034869378),
 .UNSPECIFIED.);
#1667=B_SPLINE_CURVE_WITH_KNOTS('',3,(#129872,#129873,#129874,#129875,#129876,
#129877,#129878,#129879,#129880,#129881,#129882,#129883,#129884,#129885,
#129886,#129887,#129888,#129889,#129890,#129891,#129892,#129893,#129894,
#129895,#129896,#129897,#129898,#129899,#129900,#129901,#129902,#129903,
#129904,#129905,#129906,#129907,#129908,#129909,#129910,#129911,#129912,
#129913,#129914,#129915,#129916,#129917,#129918,#129919,#129920,#129921,
#129922,#129923,#129924,#129925,#129926,#129927,#129928,#129929,#129930,
#129931,#129932,#129933,#129934,#129935,#129936,#129937,#129938,#129939,
#129940,#129941,#129942,#129943,#129944,#129945,#129946,#129947,#129948,
#129949,#129950,#129951,#129952,#129953,#129954,#129955,#129956,#129957,
#129958,#129959,#129960,#129961,#129962,#129963,#129964,#129965,#129966,
#129967,#129968,#129969,#129970,#129971,#129972,#129973,#129974,#129975,
#129976,#129977,#129978,#129979,#129980,#129981,#129982,#129983,#129984,
#129985,#129986,#129987,#129988,#129989,#129990,#129991,#129992,#129993,
#129994,#129995,#129996,#129997,#129998,#129999,#130000,#130001,#130002,
#130003,#130004,#130005,#130006,#130007,#130008,#130009,#130010,#130011,
#130012,#130013,#130014,#130015,#130016,#130017,#130018,#130019,#130020,
#130021,#130022,#130023,#130024,#130025),.UNSPECIFIED.,.F.,.F.,(4,3,3,3,
3,3,3,3,3,3,3,3,3,3,3,3,3,3,3,3,3,3,3,3,3,3,3,3,3,3,3,3,3,3,3,3,3,3,3,3,
3,3,3,3,3,3,3,3,3,3,3,4),(-60.6402364208082,-60.4782147259492,-60.3931758543397,
-60.2672790840686,-60.1415709515627,-60.0159902828507,-59.8904761268088,
-59.7648709710315,-59.6392266695458,-59.5133279238666,-59.404570569114,
-59.2786776312088,-59.1529733209067,-59.0273964554494,-58.9018860749222,
-58.7762846146787,-58.6506439704419,-58.5247487641054,-58.4159652838882,
-58.2900772181433,-58.1643778917407,-58.0388061101619,-57.9133009019233,
-57.7877047030512,-57.6620693774554,-57.5361795087896,-57.4273599986625,
-57.3014681741924,-57.1757650286975,-57.0501893766061,-56.9246802552742,
-56.799080114101,-56.6734408239648,-56.5475470110616,-56.4387547134368,
-56.3128637271534,-56.1871614244939,-56.0615866179333,-55.9360783428843,
-55.8104790410212,-55.6848405876649,-55.558947595072,-55.450149428211,-55.3242589588329,
-55.1985571863574,-55.0729829220047,-54.9474751999556,-54.8218764627213,
-54.6962385812792,-54.5703461645474,-54.4615441429853,-54.3570525280441),
 .UNSPECIFIED.);
#1668=B_SPLINE_CURVE_WITH_KNOTS('',3,(#130026,#130027,#130028,#130029,#130030,
#130031,#130032,#130033,#130034,#130035,#130036,#130037,#130038,#130039,
#130040,#130041,#130042,#130043,#130044,#130045,#130046,#130047,#130048,
#130049,#130050,#130051,#130052,#130053,#130054,#130055,#130056,#130057,
#130058,#130059,#130060,#130061,#130062,#130063,#130064,#130065,#130066,
#130067,#130068,#130069,#130070,#130071,#130072,#130073,#130074,#130075,
#130076,#130077,#130078,#130079,#130080,#130081,#130082,#130083,#130084,
#130085,#130086,#130087,#130088,#130089,#130090,#130091,#130092,#130093,
#130094,#130095,#130096,#130097,#130098,#130099,#130100,#130101,#130102,
#130103,#130104,#130105,#130106,#130107,#130108,#130109,#130110,#130111,
#130112,#130113,#130114,#130115,#130116,#130117,#130118,#130119,#130120,
#130121,#130122,#130123,#130124,#130125,#130126,#130127,#130128,#130129,
#130130,#130131,#130132,#130133,#130134,#130135,#130136,#130137,#130138,
#130139,#130140,#130141,#130142,#130143,#130144,#130145,#130146,#130147,
#130148,#130149,#130150,#130151,#130152,#130153,#130154,#130155,#130156,
#130157,#130158,#130159,#130160,#130161,#130162,#130163,#130164,#130165,
#130166,#130167,#130168,#130169,#130170,#130171,#130172,#130173,#130174,
#130175,#130176,#130177,#130178,#130179,#130180,#130181,#130182,#130183,
#130184,#130185,#130186,#130187,#130188,#130189,#130190,#130191,#130192,
#130193,#130194,#130195,#130196,#130197,#130198,#130199,#130200,#130201,
#130202,#130203,#130204,#130205,#130206,#130207),.UNSPECIFIED.,.F.,.F.,
(4,2,2,2,2,2,2,2,2,2,2,2,2,2,2,2,2,2,2,2,2,2,2,2,2,2,2,2,2,2,2,2,2,2,2,
2,2,2,2,2,2,2,2,2,2,2,2,2,2,2,2,2,2,2,2,2,2,2,2,2,2,2,2,2,2,2,2,2,2,2,2,
2,2,2,2,2,2,2,2,2,2,2,2,2,2,2,2,2,2,2,4),(7.25993422053199E-5,0.00369566804877558,
0.00618834178124166,0.00773784430141063,0.00910319675066312,0.0106852833649096,
0.0133134497730082,0.0261054828078791,0.0331610911352754,0.0499936763290807,
0.0541386006359566,0.0568679278235674,0.0595129230942833,0.0627374444668784,
0.0713106167633259,0.0928459506236268,0.101174364557697,0.103555949911492,
0.105086420675871,0.106482637911173,0.108955522422688,0.11775688050675,
0.13701672551699,0.146986699811162,0.150663828661202,0.153307445971623,
0.156086993241243,0.160486090426006,0.183351853125453,0.192411579863944,
0.197809442806072,0.199879545556519,0.201356673666114,0.203074133590082,
0.206261389796618,0.218796887175313,0.233932428478149,0.243149431099175,
0.24673698031787,0.249366315129622,0.252176283103351,0.25672693241933,0.278483460683517,
0.288089925929344,0.293686878783432,0.295783774293984,0.297264473522018,
0.298967511369874,0.302086821858706,0.318146208316721,0.331233332100341,
0.339437081919361,0.342889099991582,0.345498979467513,0.34836486259968,
0.353194021885801,0.368906863329096,0.382483351759184,0.38929185470536,
0.391532460673219,0.393036074454538,0.394675843175733,0.39757754460442,
0.416584588979802,0.431515519003177,0.436852156073985,0.439818538441746,
0.442408801017214,0.445681024475371,0.452713461719678,0.476319414830594,
0.484901400945815,0.487302719149374,0.488837089916244,0.490426343316705,
0.493088216099066,0.507657015514054,0.522357079148755,0.531112464042791,
0.534640400318591,0.537260769989273,0.54009361677814,0.544758294763645,
0.568935359620865,0.576800092172742,0.581730853438571,0.583734128484157,
0.585203525830628,0.586961159003475,0.5904493867492,0.608920537561877),
 .UNSPECIFIED.);
#1669=B_SPLINE_CURVE_WITH_KNOTS('',3,(#130212,#130213,#130214,#130215,#130216,
#130217,#130218,#130219,#130220,#130221,#130222,#130223,#130224,#130225,
#130226,#130227,#130228,#130229,#130230,#130231,#130232,#130233,#130234,
#130235,#130236,#130237,#130238,#130239,#130240,#130241,#130242,#130243,
#130244,#130245,#130246,#130247,#130248,#130249,#130250,#130251,#130252,
#130253,#130254,#130255,#130256,#130257,#130258,#130259,#130260,#130261,
#130262,#130263,#130264,#130265,#130266,#130267,#130268,#130269,#130270,
#130271,#130272,#130273,#130274,#130275,#130276,#130277,#130278,#130279,
#130280,#130281,#130282,#130283,#130284,#130285,#130286,#130287,#130288,
#130289,#130290,#130291,#130292,#130293,#130294,#130295,#130296,#130297,
#130298,#130299,#130300,#130301,#130302,#130303,#130304,#130305,#130306,
#130307,#130308,#130309,#130310,#130311,#130312,#130313,#130314,#130315,
#130316,#130317,#130318,#130319,#130320,#130321,#130322,#130323,#130324,
#130325,#130326,#130327,#130328,#130329,#130330,#130331,#130332,#130333,
#130334,#130335,#130336,#130337,#130338,#130339,#130340,#130341,#130342,
#130343,#130344,#130345,#130346,#130347,#130348,#130349,#130350,#130351,
#130352,#130353,#130354,#130355,#130356,#130357,#130358,#130359,#130360,
#130361,#130362,#130363,#130364,#130365,#130366,#130367,#130368,#130369,
#130370,#130371,#130372,#130373,#130374,#130375,#130376,#130377,#130378,
#130379,#130380,#130381,#130382,#130383,#130384,#130385,#130386,#130387,
#130388,#130389,#130390,#130391,#130392,#130393,#130394,#130395,#130396,
#130397,#130398,#130399,#130400,#130401),.UNSPECIFIED.,.F.,.F.,(4,3,3,3,
3,3,3,3,3,3,3,3,3,3,3,3,3,3,3,3,3,3,3,3,3,3,3,3,3,3,3,3,3,3,3,3,3,3,3,3,
3,3,3,3,3,3,3,3,3,3,3,3,3,3,3,3,3,3,3,3,3,3,3,4),(-66.9234231424034,-66.7973292349505,
-66.6710781156156,-66.5447477367036,-66.4181217720289,-66.3248576010649,
-66.324807565694,-66.2088850243393,-66.1987599683357,-66.0729012718308,
-65.9471706622924,-65.8215075487528,-65.6957564473878,-65.5699676397352,
-65.4439289408944,-65.3362456643337,-65.3362022804683,-65.2195847317972,
-65.2101075849637,-65.0841968766125,-64.9584094730824,-64.8326849073244,
-64.706865627026,-64.5810048306654,-64.4548887683224,-64.3476423483233,
-64.3475969952426,-64.2314304079549,-64.2218574338031,-64.0963089413872,
-63.9708899769272,-63.8455392267311,-63.720098590772,-63.5946196851449,
-63.4688854072963,-63.3590377815925,-63.3589917100169,-63.2427560995522,
-63.2330689835492,-63.1073347979478,-62.9817280397894,-62.8561878182684,
-62.7305568863553,-62.6048869281379,-62.4789631013509,-62.3704315643027,
-62.3703864247911,-62.2540719067799,-62.2444736699696,-62.1187490531194,
-61.9931514396376,-61.8676199169368,-61.7419968992799,-61.6163344354188,
-61.4904172856392,-61.3818266163067,-61.3817811395654,-61.2665055674753,
-61.257325972207,-61.1330666724535,-61.0089048450847,-60.8848099234832,
-60.7606137535066,-60.6402378352237),.UNSPECIFIED.);
#1670=B_SPLINE_CURVE_WITH_KNOTS('',3,(#130402,#130403,#130404,#130405,#130406,
#130407,#130408,#130409,#130410,#130411,#130412,#130413,#130414,#130415,
#130416,#130417,#130418,#130419,#130420,#130421,#130422,#130423,#130424,
#130425,#130426,#130427,#130428,#130429,#130430,#130431,#130432,#130433,
#130434,#130435,#130436,#130437,#130438,#130439,#130440,#130441,#130442,
#130443,#130444,#130445,#130446,#130447,#130448,#130449,#130450,#130451,
#130452,#130453,#130454,#130455,#130456,#130457,#130458,#130459,#130460,
#130461,#130462,#130463,#130464,#130465,#130466,#130467,#130468,#130469,
#130470,#130471,#130472,#130473,#130474,#130475,#130476,#130477,#130478,
#130479,#130480,#130481,#130482,#130483,#130484,#130485,#130486,#130487,
#130488,#130489,#130490,#130491,#130492,#130493,#130494,#130495,#130496,
#130497,#130498,#130499,#130500,#130501,#130502,#130503,#130504,#130505,
#130506,#130507,#130508,#130509,#130510,#130511,#130512,#130513,#130514,
#130515,#130516,#130517,#130518,#130519,#130520,#130521,#130522,#130523,
#130524,#130525,#130526,#130527,#130528,#130529,#130530,#130531,#130532,
#130533,#130534,#130535,#130536,#130537,#130538,#130539,#130540,#130541,
#130542,#130543,#130544,#130545,#130546,#130547,#130548,#130549,#130550,
#130551,#130552,#130553,#130554,#130555,#130556,#130557,#130558,#130559,
#130560,#130561,#130562,#130563,#130564,#130565,#130566,#130567,#130568,
#130569,#130570,#130571,#130572,#130573,#130574,#130575,#130576,#130577,
#130578,#130579,#130580,#130581,#130582,#130583),.UNSPECIFIED.,.F.,.F.,
(4,2,2,2,2,2,2,2,2,2,2,2,2,2,2,2,2,2,2,2,2,2,2,2,2,2,2,2,2,2,2,2,2,2,2,
2,2,2,2,2,2,2,2,2,2,2,2,2,2,2,2,2,2,2,2,2,2,2,2,2,2,2,2,2,2,2,2,2,2,2,2,
2,2,2,2,2,2,2,2,2,2,2,2,2,2,2,2,2,2,2,4),(0.608920537561877,0.624256168821786,
0.629113545833075,0.631984807747575,0.634592672523624,0.638031779520276,
0.646148364536954,0.658998977436563,0.675381501983869,0.678505790283175,
0.680209709878118,0.681689799426814,0.683783962833883,0.689361458107024,
0.698913960843616,0.720802163427926,0.725338537781256,0.728145489516899,
0.730775776501109,0.734370663585568,0.74364943537995,0.758989794829869,
0.771231344264241,0.774406042415989,0.776120879293817,0.77759916748082,
0.779675436334702,0.785114454594341,0.794285845542122,0.816916219815622,
0.821348668097504,0.824135389091964,0.826776458273983,0.830434692948252,
0.840235884974788,0.858744218665279,0.868381253314547,0.870908487310343,
0.872469105255741,0.87402668594989,0.876544555470676,0.886961905685532,
0.909482481109093,0.915882818588326,0.919045664496742,0.921627181159771,
0.924671388852573,0.930422299408979,0.94305445112279,0.959548356727087,
0.965120913715681,0.967268595971487,0.968755837047758,0.970432241905588,
0.973512635765905,0.984535804865729,1.00817377297338,1.01295478777827,1.01581133191923,
1.01842447860032,1.02189854342733,1.03025811199955,1.04378644621304,1.05910718918934,
1.06224292418989,1.06395039714074,1.06543508638462,1.0675369240636,1.07314016936173,
1.08276533216519,1.10434385098459,1.10890314240192,1.11171865226943,1.1143538825839,
1.11795124642645,1.12721193308001,1.14247082217507,1.15484174720004,1.15802184143598,
1.15973787719428,1.16120698748422,1.1632603011753,1.16860217125017,1.17752424378311,
1.18797933217666,1.20152973972704,1.20554483227242,1.20796744875538,1.21041405025214,
1.21298593217112,1.21791947617356),.UNSPECIFIED.);
#1671=B_SPLINE_CURVE_WITH_KNOTS('',3,(#130589,#130590,#130591,#130592,#130593,
#130594,#130595,#130596,#130597,#130598,#130599,#130600,#130601,#130602,
#130603,#130604,#130605,#130606,#130607,#130608,#130609,#130610,#130611,
#130612,#130613,#130614,#130615,#130616,#130617,#130618,#130619,#130620,
#130621,#130622,#130623,#130624,#130625,#130626,#130627,#130628),
 .UNSPECIFIED.,.F.,.F.,(4,2,2,2,2,2,2,2,2,2,2,2,2,2,2,2,2,2,2,4),(-0.104760453105363,
-0.0994634724235555,-0.0968929368591775,-0.0954871930896152,-0.0939247039312219,
-0.0913394407810213,-0.0808838676492878,-0.0652008291509204,-0.0612243537920569,
-0.0588035558409778,-0.0561167224443349,-0.0521532597402351,-0.03944228777409,
-0.0260061456948558,-0.0234232455547038,-0.0218595630230891,-0.0202410662692351,
-0.0185042201956334,-0.0157590766080668,-1.33456115395515E-5),
 .UNSPECIFIED.);
#1672=B_SPLINE_CURVE_WITH_KNOTS('',3,(#130631,#130632,#130633,#130634,#130635,
#130636,#130637,#130638),.UNSPECIFIED.,.F.,.F.,(4,2,2,4),(-0.0123240142976081,
-0.00994052883850335,-0.00623763007844346,-1.5266722490738E-5),
 .UNSPECIFIED.);
#1673=B_SPLINE_CURVE_WITH_KNOTS('',3,(#130643,#130644,#130645,#130646,#130647,
#130648,#130649,#130650,#130651,#130652,#130653,#130654,#130655,#130656,
#130657,#130658,#130659,#130660,#130661,#130662,#130663,#130664,#130665,
#130666,#130667,#130668,#130669,#130670,#130671,#130672,#130673,#130674,
#130675,#130676,#130677,#130678,#130679,#130680,#130681,#130682,#130683,
#130684,#130685,#130686,#130687,#130688,#130689,#130690,#130691,#130692,
#130693,#130694,#130695,#130696,#130697,#130698,#130699,#130700,#130701,
#130702,#130703,#130704,#130705,#130706,#130707,#130708,#130709,#130710,
#130711,#130712,#130713,#130714,#130715,#130716,#130717,#130718,#130719,
#130720,#130721,#130722,#130723,#130724,#130725,#130726,#130727,#130728,
#130729,#130730,#130731,#130732,#130733,#130734,#130735,#130736,#130737,
#130738,#130739,#130740,#130741,#130742,#130743,#130744,#130745,#130746,
#130747,#130748,#130749,#130750,#130751,#130752,#130753,#130754,#130755,
#130756,#130757,#130758,#130759,#130760,#130761,#130762,#130763,#130764,
#130765,#130766,#130767,#130768,#130769,#130770,#130771,#130772,#130773,
#130774,#130775,#130776,#130777,#130778,#130779,#130780,#130781,#130782,
#130783,#130784,#130785,#130786,#130787,#130788,#130789,#130790,#130791,
#130792,#130793,#130794,#130795,#130796,#130797,#130798,#130799,#130800,
#130801,#130802,#130803,#130804,#130805,#130806,#130807,#130808),
 .UNSPECIFIED.,.F.,.F.,(4,2,2,2,2,2,2,2,2,2,2,2,2,2,2,2,2,2,2,2,2,2,2,2,
2,2,2,2,2,2,2,2,2,2,2,2,2,2,2,2,2,2,2,2,2,2,2,2,2,2,2,2,2,2,2,2,2,2,2,2,
2,2,2,2,2,2,2,2,2,2,2,2,2,2,2,2,2,2,2,2,2,2,4),(-0.571051559787927,-0.569996074513531,
-0.565671843249809,-0.560366882428473,-0.546557663273505,-0.539600185118641,
-0.537343957564249,-0.535840305815804,-0.534121793565648,-0.530741555086234,
-0.52597114521168,-0.516700251387653,-0.506185232178122,-0.502125052067211,
-0.499691568810702,-0.497019310272292,-0.493138314866569,-0.479934522013935,
-0.466858149278131,-0.464241332196048,-0.46267224585702,-0.461069704528704,
-0.458287920534849,-0.448560877492757,-0.432407578658465,-0.428491638974536,
-0.425840043368729,-0.423093042035003,-0.418789852070253,-0.413521171611082,
-0.399948314192901,-0.392630366694188,-0.390395974064222,-0.388895616885867,
-0.387167291862575,-0.383733032148312,-0.378851404193333,-0.36974050271539,
-0.359259111648477,-0.355200859325038,-0.352767892745599,-0.350095750197438,
-0.346214024981766,-0.332971962391731,-0.319942484826,-0.317322171459366,
-0.315752530832435,-0.314151231754787,-0.311374776483078,-0.301695541193718,
-0.285456510792349,-0.281550740964732,-0.278900956782245,-0.276151817980632,
-0.271836284421581,-0.266546170902295,-0.252832762870907,-0.245771822322346,
-0.243505809537544,-0.24201514600845,-0.240306329955738,-0.236981179840528,
-0.232322911665265,-0.214495799010595,-0.209340260128373,-0.206410138371564,
-0.203802567318848,-0.200375304828084,-0.191486995531469,-0.181599018465889,
-0.172438193643578,-0.170117338375145,-0.168618564225245,-0.16693542441401,
-0.163738236452623,-0.149178611996683,-0.137871258862018,-0.13425969181125,
-0.131631584954883,-0.128790949103628,-0.123968675471476,-0.11535376263171,
-0.104760453105363),.UNSPECIFIED.);
#1674=B_SPLINE_CURVE_WITH_KNOTS('',3,(#130810,#130811,#130812,#130813,#130814,
#130815,#130816,#130817,#130818,#130819),.UNSPECIFIED.,.F.,.F.,(4,3,3,4),
(15.363686816277,15.5113772250708,15.6590677938146,15.7079632679489),
 .UNSPECIFIED.);
#1675=B_SPLINE_CURVE_WITH_KNOTS('',3,(#130820,#130821,#130822,#130823,#130824,
#130825,#130826,#130827,#130828,#130829,#130830,#130831,#130832,#130833,
#130834,#130835,#130836,#130837,#130838,#130839,#130840,#130841,#130842,
#130843,#130844,#130845,#130846,#130847,#130848,#130849,#130850,#130851,
#130852,#130853,#130854,#130855,#130856,#130857,#130858,#130859,#130860,
#130861,#130862,#130863,#130864,#130865,#130866,#130867,#130868,#130869,
#130870,#130871,#130872,#130873,#130874,#130875,#130876,#130877,#130878,
#130879,#130880,#130881,#130882,#130883,#130884,#130885,#130886,#130887,
#130888,#130889,#130890,#130891,#130892,#130893,#130894,#130895,#130896,
#130897,#130898,#130899,#130900,#130901,#130902,#130903,#130904,#130905,
#130906,#130907,#130908,#130909,#130910,#130911,#130912,#130913,#130914,
#130915,#130916,#130917,#130918,#130919,#130920,#130921,#130922,#130923,
#130924,#130925,#130926,#130927,#130928,#130929,#130930,#130931,#130932,
#130933,#130934,#130935,#130936,#130937,#130938,#130939,#130940,#130941,
#130942,#130943,#130944,#130945,#130946,#130947,#130948,#130949,#130950,
#130951,#130952,#130953,#130954,#130955,#130956,#130957,#130958,#130959,
#130960,#130961,#130962,#130963,#130964,#130965,#130966,#130967,#130968,
#130969,#130970,#130971,#130972,#130973,#130974,#130975,#130976,#130977,
#130978,#130979,#130980,#130981,#130982,#130983,#130984,#130985,#130986,
#130987,#130988,#130989,#130990,#130991,#130992,#130993,#130994,#130995,
#130996,#130997,#130998,#130999,#131000,#131001,#131002,#131003),
 .UNSPECIFIED.,.F.,.F.,(4,3,3,3,3,3,3,3,3,3,3,3,3,3,3,3,3,3,3,3,3,3,3,3,
3,3,3,3,3,3,3,3,3,3,3,3,3,3,3,3,3,3,3,3,3,3,3,3,3,3,3,3,3,3,3,3,3,3,3,3,
3,4),(15.7079658912085,15.8280867104848,15.841693727571,15.9752153053394,
16.1086061050242,16.2433728485283,16.3768229870163,16.5122480330283,16.6373080334116,
16.6476730790403,16.6477295647726,16.7700944172117,16.7825272094377,16.9171733070631,
17.0516855888283,17.1861379983219,17.320704100207,17.4553370592189,17.5902314444273,
17.6362783642661,17.6363374995076,17.7582188619054,17.7707526904591,17.9050109173946,
18.0391283118763,18.1731798518975,18.3073399651891,18.4415634786314,18.5760484224978,
18.6248836494918,18.6249438490354,18.7468947738374,18.7595538646593,18.8940108554107,
19.0283293656656,19.1625838565757,19.296947748702,19.4313757768995,19.5660637510641,
19.6134889347175,19.6135478246836,19.7355858153476,19.7481484855373,19.882595273636,
20.0169040688695,20.1511493591163,20.2855049097021,20.4199250839303,20.5546060391902,
20.6020942199433,20.6021535687792,20.7241240926645,20.7367081159257,20.8711082220163,
21.0053694336211,21.1395663621798,21.2738728468049,21.4082434871058,21.5428748325272,
21.590699505169,21.5907589398938,21.647807050148),.UNSPECIFIED.);
#1676=B_SPLINE_CURVE_WITH_KNOTS('',3,(#131008,#131009,#131010,#131011,#131012,
#131013,#131014,#131015,#131016,#131017,#131018,#131019,#131020,#131021,
#131022,#131023,#131024,#131025,#131026,#131027,#131028,#131029,#131030,
#131031,#131032,#131033,#131034,#131035,#131036,#131037,#131038,#131039,
#131040,#131041,#131042,#131043,#131044,#131045,#131046,#131047,#131048,
#131049,#131050,#131051,#131052,#131053,#131054,#131055,#131056,#131057,
#131058,#131059,#131060,#131061,#131062,#131063,#131064,#131065,#131066,
#131067,#131068,#131069,#131070,#131071,#131072,#131073,#131074,#131075,
#131076,#131077,#131078,#131079,#131080,#131081,#131082,#131083,#131084,
#131085,#131086,#131087,#131088,#131089,#131090,#131091,#131092,#131093,
#131094,#131095,#131096,#131097,#131098,#131099,#131100,#131101,#131102,
#131103,#131104,#131105,#131106,#131107,#131108,#131109,#131110,#131111,
#131112,#131113,#131114,#131115,#131116,#131117,#131118,#131119,#131120,
#131121,#131122,#131123,#131124,#131125,#131126,#131127,#131128,#131129,
#131130,#131131,#131132,#131133,#131134,#131135,#131136,#131137,#131138,
#131139,#131140,#131141,#131142,#131143,#131144,#131145,#131146,#131147,
#131148,#131149,#131150,#131151,#131152,#131153,#131154,#131155,#131156,
#131157,#131158,#131159,#131160,#131161,#131162,#131163,#131164,#131165,
#131166,#131167,#131168,#131169,#131170,#131171,#131172,#131173,#131174,
#131175,#131176,#131177),.UNSPECIFIED.,.F.,.F.,(4,2,2,2,2,2,2,2,2,2,2,2,
2,2,2,2,2,2,2,2,2,2,2,2,2,2,2,2,2,2,2,2,2,2,2,2,2,2,2,2,2,2,2,2,2,2,2,2,
2,2,2,2,2,2,2,2,2,2,2,2,2,2,2,2,2,2,2,2,2,2,2,2,2,2,2,2,2,2,2,2,2,2,2,2,
4),(-1.03737585849936,-1.03227715523834,-1.02055288568758,-1.01644245472727,
-1.01373014153861,-1.01101680205915,-1.00690071747753,-0.994352282923678,
-0.984960736685868,-0.979882995409455,-0.978055814838689,-0.976563310812306,
-0.974805636634147,-0.971209682499858,-0.968429728397085,-0.957358599118677,
-0.945986508622834,-0.942371710140109,-0.939740803116181,-0.936896475627927,
-0.93206541560142,-0.925852120427952,-0.911239208908094,-0.906349691192717,
-0.90454776998583,-0.903059577463341,-0.901282804672542,-0.897577850157911,
-0.894672795136712,-0.882616161424283,-0.872445605120101,-0.868861969007884,
-0.866235418606352,-0.863378884640084,-0.858481184427325,-0.852142709930726,
-0.841290600394485,-0.83351811880258,-0.831243867809716,-0.829752134058528,
-0.828047921811842,-0.824745065367215,-0.822287816452621,-0.813387806769867,
-0.800191053957259,-0.796067738610522,-0.793353303175773,-0.790642555968347,
-0.786540028749658,-0.774878025917806,-0.760452124872451,-0.757980751988692,
-0.75659151167371,-0.755004723175957,-0.752300595641114,-0.743260406000457,
-0.725911196617614,-0.722156862002156,-0.719531349865557,-0.716741732065363,
-0.712206885972953,-0.709173042576224,-0.699616774568612,-0.687345091061038,
-0.684681469399271,-0.683102961308723,-0.681510893710357,-0.678780676240484,
-0.669514983211609,-0.652570346897138,-0.648759312230262,-0.646124914429003,
-0.643351560271103,-0.638904643213751,-0.626777927393997,-0.613798447382564,
-0.611174271553658,-0.609603710601596,-0.608002994647919,-0.605229896782282,
-0.595581753162721,-0.579294642172542,-0.575395519728214,-0.572746825441744,
-0.571051559787927),.UNSPECIFIED.);
#1677=B_SPLINE_CURVE_WITH_KNOTS('',3,(#131179,#131180,#131181,#131182,#131183,
#131184,#131185,#131186,#131187,#131188,#131189,#131190,#131191),
 .UNSPECIFIED.,.F.,.F.,(4,3,3,3,4),(21.6478070511627,21.7809366960148,21.796403000268,
21.9440994851842,21.9911485738921),.UNSPECIFIED.);
#1678=B_SPLINE_CURVE_WITH_KNOTS('',3,(#131192,#131193,#131194,#131195,#131196,
#131197,#131198,#131199,#131200,#131201,#131202,#131203,#131204,#131205,
#131206,#131207,#131208,#131209,#131210,#131211,#131212,#131213,#131214,
#131215,#131216,#131217,#131218,#131219,#131220,#131221,#131222,#131223,
#131224,#131225,#131226,#131227,#131228,#131229,#131230,#131231,#131232,
#131233,#131234,#131235,#131236,#131237,#131238,#131239,#131240,#131241,
#131242,#131243,#131244,#131245,#131246,#131247,#131248,#131249,#131250,
#131251,#131252,#131253,#131254,#131255,#131256,#131257,#131258,#131259,
#131260,#131261,#131262,#131263,#131264,#131265,#131266,#131267,#131268,
#131269,#131270,#131271,#131272,#131273,#131274,#131275,#131276,#131277,
#131278,#131279,#131280,#131281,#131282,#131283,#131284,#131285,#131286,
#131287,#131288,#131289,#131290,#131291,#131292,#131293,#131294,#131295,
#131296,#131297,#131298,#131299,#131300,#131301,#131302,#131303,#131304,
#131305,#131306,#131307,#131308,#131309,#131310,#131311,#131312,#131313,
#131314,#131315,#131316,#131317,#131318,#131319,#131320,#131321,#131322,
#131323,#131324,#131325,#131326,#131327,#131328,#131329,#131330,#131331,
#131332,#131333,#131334,#131335,#131336,#131337,#131338,#131339,#131340,
#131341,#131342,#131343,#131344,#131345,#131346,#131347,#131348,#131349,
#131350,#131351,#131352,#131353,#131354,#131355,#131356,#131357,#131358,
#131359,#131360,#131361,#131362,#131363,#131364,#131365,#131366,#131367,
#131368,#131369,#131370,#131371,#131372),.UNSPECIFIED.,.F.,.F.,(4,3,3,3,
3,3,3,3,3,3,3,3,3,3,3,3,3,3,3,3,3,3,3,3,3,3,3,3,3,3,3,3,3,3,3,3,3,3,3,3,
3,3,3,3,3,3,3,3,3,3,3,3,3,3,3,3,3,3,3,3,4),(21.9911485751285,22.1273195269264,
22.2636884434382,22.4001715837155,22.5369664127769,22.5793047903947,22.579364055752,
22.7013589250348,22.7139431476743,22.84836818408,22.9826547283351,23.1168773261226,
23.2512097396333,23.3856064910885,23.5202638907055,23.5679100756204,23.5679694139317,
23.6899550950555,23.7025432222845,23.8369629207288,23.9712440140535,24.105461062073,
24.2397878306671,24.3741788751869,24.5088305468898,24.5565153608462,24.5565747025817,
24.6785631409001,24.6911525273435,24.8255763143162,24.9598615539257,25.0940827951838,
25.2284137873522,25.3628090781897,25.4974649765261,25.5451206460719,25.545179966661,
25.667169268505,25.6797569161559,25.8141798014757,25.9484641365813,26.0826844728612,
26.2170145679853,26.3514089652749,26.4860639866976,26.5337259312976,26.5337852629189,
26.6557733512449,26.6683616485685,26.8027839659363,26.9370677194846,27.0712874621066,
27.2056169511046,27.3400107343051,27.4746651374359,27.5223312165234,27.5223905474788,
27.6433095975991,27.6553377119416,27.7930166516017,27.9306954395165),
 .UNSPECIFIED.);
#1679=B_SPLINE_CURVE_WITH_KNOTS('',3,(#131377,#131378,#131379,#131380,#131381,
#131382,#131383,#131384,#131385,#131386,#131387,#131388,#131389,#131390,
#131391,#131392,#131393,#131394,#131395,#131396,#131397,#131398,#131399,
#131400,#131401,#131402,#131403,#131404,#131405,#131406,#131407,#131408,
#131409,#131410,#131411,#131412,#131413,#131414,#131415,#131416,#131417,
#131418,#131419,#131420,#131421,#131422,#131423,#131424,#131425,#131426,
#131427,#131428,#131429,#131430,#131431,#131432,#131433,#131434,#131435,
#131436,#131437,#131438,#131439,#131440,#131441,#131442,#131443,#131444,
#131445,#131446,#131447,#131448,#131449,#131450,#131451,#131452,#131453,
#131454,#131455,#131456,#131457,#131458,#131459,#131460,#131461,#131462,
#131463,#131464,#131465,#131466,#131467,#131468,#131469,#131470,#131471,
#131472,#131473,#131474,#131475,#131476,#131477,#131478,#131479,#131480,
#131481,#131482,#131483,#131484,#131485,#131486,#131487,#131488,#131489,
#131490,#131491,#131492,#131493,#131494,#131495,#131496,#131497,#131498,
#131499,#131500,#131501,#131502,#131503,#131504,#131505,#131506,#131507,
#131508,#131509,#131510,#131511,#131512,#131513,#131514,#131515,#131516,
#131517,#131518,#131519,#131520,#131521,#131522,#131523,#131524,#131525,
#131526,#131527,#131528,#131529,#131530,#131531,#131532,#131533,#131534,
#131535,#131536,#131537,#131538,#131539,#131540,#131541,#131542,#131543,
#131544),.UNSPECIFIED.,.F.,.F.,(4,2,2,2,2,2,2,2,2,2,2,2,2,2,2,2,2,2,2,2,
2,2,2,2,2,2,2,2,2,2,2,2,2,2,2,2,2,2,2,2,2,2,2,2,2,2,2,2,2,2,2,2,2,2,2,2,
2,2,2,2,2,2,2,2,2,2,2,2,2,2,2,2,2,2,2,2,2,2,2,2,2,2,2,4),(-1.50364802285674,
-1.49545071073367,-1.49277784300415,-1.4911978096781,-1.48960844249668,
-1.4868897810579,-1.47496652604162,-1.46527405764246,-1.46221455472017,
-1.45765323723645,-1.45485936435662,-1.45223726314951,-1.44850103989386,
-1.43101940449241,-1.42204514007086,-1.41934910384597,-1.41776429307554,
-1.41637445893584,-1.41389802865572,-1.39954388678771,-1.3878576775268,
-1.38375301096247,-1.38104241125083,-1.37832923362657,-1.37421021101463,
-1.36048348501126,-1.35193918668256,-1.34852985676151,-1.34586995600447,
-1.34429248030542,-1.3427002150785,-1.3399675995032,-1.33063809196475,-1.31923800992053,
-1.31222954640053,-1.30902851719769,-1.30646340046811,-1.3033929521827,
-1.29725354033603,-1.28069048066722,-1.2761366571879,-1.27286413065123,
-1.2711658310835,-1.2696722879819,-1.26738524150891,-1.25930306649972,-1.2497418103615,
-1.23966884281241,-1.23613871611966,-1.23351969791668,-1.23064140754522,
-1.22562232784468,-1.20746943500652,-1.20278305642826,-1.19944442040429,
-1.19773360345223,-1.1962442974679,-1.1939857412558,-1.18645885958552,-1.17309565971293,
-1.16786154210746,-1.1635780667853,-1.16083471353968,-1.15818053209682,
-1.15424909030975,-1.13819563253312,-1.12839218039528,-1.12560185975233,
-1.12399763961541,-1.12242998135255,-1.11982066605514,-1.10534886412797,
-1.09505387622202,-1.09042292870394,-1.08761552173897,-1.0849690255242,
-1.08124896820758,-1.06363989104472,-1.0547287558928,-1.05203963558377,
-1.05045587143454,-1.04906446764604,-1.04658085487128,-1.03737585849936),
 .UNSPECIFIED.);
#1680=B_SPLINE_CURVE_WITH_KNOTS('',3,(#131546,#131547,#131548,#131549,#131550,
#131551,#131552,#131553,#131554,#131555,#131556,#131557),.UNSPECIFIED.,
 .F.,.F.,(4,2,2,2,2,4),(-0.025563779166194,-0.0218566744148999,-0.019367166493461,
-0.0166535805597176,-0.0127752645799051,-2.12926712384545E-6),
 .UNSPECIFIED.);
#1681=B_SPLINE_CURVE_WITH_KNOTS('',3,(#131558,#131559,#131560,#131561,#131562,
#131563,#131564,#131565,#131566,#131567,#131568,#131569,#131570,#131571,
#131572,#131573,#131574,#131575,#131576,#131577,#131578,#131579,#131580,
#131581,#131582,#131583,#131584,#131585,#131586,#131587,#131588,#131589,
#131590,#131591,#131592,#131593,#131594,#131595,#131596,#131597,#131598,
#131599,#131600,#131601,#131602,#131603,#131604,#131605,#131606,#131607,
#131608,#131609,#131610,#131611,#131612,#131613,#131614,#131615,#131616,
#131617,#131618,#131619,#131620,#131621,#131622,#131623,#131624,#131625,
#131626,#131627,#131628,#131629,#131630,#131631,#131632,#131633,#131634,
#131635,#131636,#131637,#131638,#131639,#131640,#131641,#131642,#131643,
#131644,#131645,#131646,#131647,#131648,#131649,#131650,#131651,#131652,
#131653,#131654,#131655,#131656,#131657,#131658,#131659,#131660,#131661,
#131662,#131663,#131664,#131665,#131666,#131667,#131668,#131669,#131670,
#131671,#131672,#131673,#131674,#131675,#131676,#131677,#131678,#131679,
#131680,#131681,#131682,#131683,#131684,#131685,#131686,#131687,#131688,
#131689,#131690,#131691,#131692,#131693,#131694,#131695,#131696,#131697,
#131698,#131699,#131700,#131701,#131702,#131703,#131704,#131705,#131706,
#131707,#131708,#131709,#131710,#131711,#131712,#131713,#131714,#131715,
#131716,#131717,#131718,#131719,#131720,#131721,#131722,#131723,#131724,
#131725,#131726,#131727,#131728,#131729,#131730,#131731,#131732,#131733,
#131734,#131735,#131736,#131737,#131738,#131739,#131740,#131741),
 .UNSPECIFIED.,.F.,.F.,(4,3,3,3,3,3,3,3,3,3,3,3,3,3,3,3,3,3,3,3,3,3,3,3,
3,3,3,3,3,3,3,3,3,3,3,3,3,3,3,3,3,3,3,3,3,3,3,3,3,3,3,3,3,3,3,3,3,3,3,3,
3,4),(28.2743338967306,28.4080562857905,28.450661125029,28.5109365017491,
28.5109958301788,28.6329844373678,28.6455726033673,28.7799953133922,28.9142794668526,
29.0484996156028,29.1828295161676,29.3172237145886,29.4518785331719,29.4995417869748,
29.4996011170081,29.6215895690841,29.634177836647,29.7686004930229,29.902884591277,
30.0371046834058,30.1714345257688,30.3058286650014,30.4404834236609,30.4881470722005,
30.4882064019962,30.6101949254426,30.6227831943049,30.757205924499,30.8914900977593,
31.0257102658872,31.1600401850117,31.2944344015414,31.429089237323,31.4767523574263,
31.4768116869338,31.5988002109329,31.6113884523335,31.7458111549967,31.8800953004658,
32.0143154406149,32.1486453317464,32.2830395202408,32.4176943282795,32.465357642652,
32.4654169723847,32.5874054772536,32.5999937338323,32.7344164325919,32.8687005739914,
33.0029207099153,33.1372505966289,33.2716447805881,33.4062995839727,33.4539629278777,
33.4540222575592,33.5760115235183,33.5886145888915,33.7230418399154,33.8573515080313,
33.9915876646927,34.1259133197487,34.2133098071407),.UNSPECIFIED.);
#1682=B_SPLINE_CURVE_WITH_KNOTS('',3,(#131746,#131747,#131748,#131749,#131750,
#131751,#131752,#131753,#131754,#131755,#131756,#131757,#131758,#131759,
#131760,#131761,#131762,#131763,#131764,#131765,#131766,#131767,#131768,
#131769,#131770,#131771,#131772,#131773,#131774,#131775,#131776,#131777,
#131778,#131779,#131780,#131781,#131782,#131783,#131784,#131785,#131786,
#131787,#131788,#131789,#131790,#131791,#131792,#131793,#131794,#131795,
#131796,#131797,#131798,#131799,#131800,#131801,#131802,#131803,#131804,
#131805,#131806,#131807,#131808,#131809,#131810,#131811,#131812,#131813,
#131814,#131815,#131816,#131817,#131818,#131819,#131820,#131821,#131822,
#131823,#131824,#131825,#131826,#131827,#131828,#131829,#131830,#131831,
#131832,#131833,#131834,#131835,#131836,#131837,#131838,#131839,#131840,
#131841,#131842,#131843,#131844,#131845,#131846,#131847,#131848,#131849,
#131850,#131851,#131852,#131853,#131854,#131855,#131856,#131857,#131858,
#131859,#131860,#131861,#131862,#131863,#131864,#131865,#131866,#131867,
#131868,#131869,#131870,#131871,#131872,#131873,#131874,#131875,#131876,
#131877,#131878,#131879,#131880,#131881,#131882,#131883,#131884,#131885,
#131886,#131887,#131888,#131889,#131890,#131891,#131892,#131893,#131894,
#131895,#131896,#131897,#131898,#131899,#131900,#131901,#131902,#131903,
#131904,#131905,#131906,#131907),.UNSPECIFIED.,.F.,.F.,(4,2,2,2,2,2,2,2,
2,2,2,2,2,2,2,2,2,2,2,2,2,2,2,2,2,2,2,2,2,2,2,2,2,2,2,2,2,2,2,2,2,2,2,2,
2,2,2,2,2,2,2,2,2,2,2,2,2,2,2,2,2,2,2,2,2,2,2,2,2,2,2,2,2,2,2,2,2,2,2,2,
4),(-1.96977677123554,-1.96786265403597,-1.96573321501472,-1.96167162230868,
-1.94590146179013,-1.93624742027908,-1.9334745428404,-1.93187453643428,
-1.9303051971168,-1.92768398226965,-1.91471533300402,-1.90557344281115,
-1.90262272335569,-1.89817551750715,-1.89540328859398,-1.8927707361987,
-1.8889638743168,-1.87199495010463,-1.86274083518687,-1.86001273426832,
-1.85842172337792,-1.85703669037491,-1.85458667364288,-1.84001187590523,
-1.82952706152445,-1.82490094155638,-1.82209559134509,-1.81945049171496,
-1.81573146694776,-1.79814113634482,-1.78923083908553,-1.78654279102156,
-1.78495986395928,-1.78356936486571,-1.78108766599658,-1.76678871844126,
-1.75507376823034,-1.75096608606115,-1.74825544400513,-1.74554367041334,
-1.7414297442648,-1.72755468915487,-1.71575230344817,-1.71308828805365,
-1.71151021381858,-1.70991931542362,-1.70719228954269,-1.6955058046255,
-1.682765676323,-1.67807983995417,-1.6752633309225,-1.67262312487704,-1.66893714685131,
-1.65111548551198,-1.6423288844496,-1.63965552390463,-1.63807550252748,
-1.63648647090955,-1.63376891181973,-1.62223508619449,-1.61229347065207,
-1.60772509028122,-1.60384174735595,-1.60116983478843,-1.59873784336122,
-1.59468322794104,-1.57980767462402,-1.56874828801468,-1.56615344533303,
-1.5645891350189,-1.56298240793629,-1.56017760053193,-1.54944854327282,
-1.53908352977955,-1.53589917031369,-1.53120962068263,-1.52839222095618,
-1.52575200079865,-1.52206738819631,-1.504231779604,-1.50364802285674),
 .UNSPECIFIED.);
#1683=B_SPLINE_CURVE_WITH_KNOTS('',3,(#131909,#131910,#131911,#131912,#131913,
#131914,#131915,#131916,#131917,#131918),.UNSPECIFIED.,.F.,.F.,(4,3,3,4),
(34.2133098076447,34.3479491574694,34.4425682131035,34.5575191894877),
 .UNSPECIFIED.);
#1684=B_SPLINE_CURVE_WITH_KNOTS('',3,(#131919,#131920,#131921,#131922,#131923,
#131924,#131925,#131926,#131927,#131928,#131929,#131930,#131931,#131932,
#131933,#131934,#131935,#131936,#131937,#131938,#131939,#131940,#131941,
#131942,#131943,#131944,#131945,#131946,#131947,#131948,#131949,#131950,
#131951,#131952,#131953,#131954,#131955,#131956,#131957,#131958,#131959,
#131960,#131961,#131962,#131963,#131964,#131965,#131966,#131967,#131968,
#131969,#131970,#131971,#131972,#131973,#131974,#131975,#131976,#131977,
#131978,#131979,#131980,#131981,#131982,#131983,#131984,#131985,#131986,
#131987,#131988,#131989,#131990,#131991,#131992,#131993,#131994,#131995,
#131996,#131997,#131998,#131999,#132000,#132001,#132002,#132003,#132004,
#132005,#132006,#132007,#132008,#132009,#132010,#132011,#132012,#132013,
#132014,#132015,#132016,#132017,#132018,#132019,#132020,#132021,#132022,
#132023,#132024,#132025,#132026,#132027,#132028,#132029,#132030,#132031,
#132032,#132033,#132034,#132035,#132036,#132037,#132038,#132039,#132040,
#132041,#132042,#132043,#132044,#132045,#132046,#132047,#132048,#132049,
#132050,#132051,#132052,#132053,#132054,#132055,#132056,#132057,#132058,
#132059,#132060,#132061,#132062,#132063,#132064,#132065,#132066,#132067,
#132068,#132069,#132070,#132071,#132072,#132073,#132074,#132075,#132076,
#132077,#132078,#132079,#132080,#132081,#132082,#132083,#132084,#132085,
#132086,#132087,#132088,#132089,#132090,#132091,#132092,#132093,#132094,
#132095,#132096),.UNSPECIFIED.,.F.,.F.,(4,3,3,3,3,3,3,3,3,3,3,3,3,3,3,3,
3,3,3,3,3,3,3,3,3,3,3,3,3,3,3,3,3,3,3,3,3,3,3,3,3,3,3,3,3,3,3,3,3,3,3,3,
3,3,3,3,3,3,3,4),(34.5575191904757,34.690284217135,34.8228676060756,34.9553479102442,
35.0879023753946,35.2204932902944,35.3533450541945,35.4311734983292,35.431232828011,
35.5532213403015,35.5658095944846,35.7002322983317,35.8345164449174,35.9687365861126,
36.1030664781748,36.2374606675342,36.3721154763276,36.4197787835549,36.4198381132273,
36.5418266270213,36.5544148808533,36.6888375858681,36.8231217336429,36.9573418760459,
37.0916717693317,37.2260659599253,37.3607207699536,37.4083840687806,37.4084433984502,
37.5304319119846,37.5430201654453,37.6774428698166,37.8117270169401,37.9459471586851,
38.0802770513101,38.2146712412402,38.3493260506096,38.3969893540064,38.3970486836801,
38.5190371970041,38.5316254507277,38.6660481551546,38.8003323023324,38.9345524441305,
39.0688823368061,39.2032765267856,39.3379313362016,39.3855946392321,39.3856539689042,
39.507642482419,39.5202307360884,39.6546534406534,39.788937587972,39.9231577299135,
40.0574876227346,40.191881812861,40.3265366224243,40.3741999244578,40.3742592541492,
40.4976061704439),.UNSPECIFIED.);
#1685=B_SPLINE_CURVE_WITH_KNOTS('',3,(#132101,#132102,#132103,#132104,#132105,
#132106,#132107,#132108,#132109,#132110,#132111,#132112,#132113,#132114,
#132115,#132116,#132117,#132118,#132119,#132120,#132121,#132122,#132123,
#132124,#132125,#132126,#132127,#132128,#132129,#132130,#132131,#132132,
#132133,#132134,#132135,#132136,#132137,#132138,#132139,#132140,#132141,
#132142,#132143,#132144,#132145,#132146,#132147,#132148,#132149,#132150,
#132151,#132152,#132153,#132154,#132155,#132156,#132157,#132158,#132159,
#132160,#132161,#132162,#132163,#132164,#132165,#132166,#132167,#132168,
#132169,#132170,#132171,#132172,#132173,#132174,#132175,#132176,#132177,
#132178,#132179,#132180,#132181,#132182,#132183,#132184,#132185,#132186,
#132187,#132188,#132189,#132190,#132191,#132192,#132193,#132194,#132195,
#132196,#132197,#132198,#132199,#132200,#132201,#132202,#132203,#132204,
#132205,#132206,#132207,#132208,#132209,#132210,#132211,#132212,#132213,
#132214,#132215,#132216,#132217,#132218,#132219,#132220,#132221,#132222,
#132223,#132224,#132225,#132226,#132227,#132228,#132229,#132230,#132231,
#132232,#132233,#132234,#132235,#132236,#132237,#132238,#132239,#132240,
#132241,#132242,#132243,#132244,#132245,#132246,#132247,#132248,#132249,
#132250,#132251,#132252,#132253,#132254,#132255,#132256,#132257,#132258,
#132259,#132260,#132261,#132262,#132263,#132264,#132265,#132266,#132267,
#132268),.UNSPECIFIED.,.F.,.F.,(4,2,2,2,2,2,2,2,2,2,2,2,2,2,2,2,2,2,2,2,
2,2,2,2,2,2,2,2,2,2,2,2,2,2,2,2,2,2,2,2,2,2,2,2,2,2,2,2,2,2,2,2,2,2,2,2,
2,2,2,2,2,2,2,2,2,2,2,2,2,2,2,2,2,2,2,2,2,2,2,2,2,2,2,4),(-0.466250456168778,
-0.462515734984742,-0.445730588883325,-0.441898784801489,-0.439261464619427,
-0.43649446551622,-0.432079883083639,-0.426617785213962,-0.411695311933343,
-0.405884200717412,-0.403766921177319,-0.402281904470734,-0.400491247456053,
-0.396703695157635,-0.393701511144969,-0.380802676507036,-0.379744070127349,
-0.37136004070281,-0.367951421616744,-0.365340143971343,-0.362433691182018,
-0.357257584904554,-0.345128280789277,-0.333639195686409,-0.330926536843941,
-0.329338295715798,-0.327756807175644,-0.325077505150332,-0.31624332656241,
-0.298525090081188,-0.294825365477072,-0.292182588200003,-0.289369692793726,
-0.284706163347405,-0.276161052143204,-0.260748214669335,-0.257709982467129,
-0.256056670720635,-0.254524067949552,-0.252096151517043,-0.249084719319112,
-0.242262141963782,-0.225319450037713,-0.221509134334388,-0.218875198296874,
-0.216102303772512,-0.21165606666655,-0.208706575661511,-0.199574142657068,
-0.18655181532208,-0.183931374029539,-0.18236174835175,-0.180760550509001,
-0.177984215355451,-0.168303944602996,-0.152076235965933,-0.148170541648297,
-0.145521082761926,-0.142772488508383,-0.138458287329498,-0.133170235914728,
-0.119468269465196,-0.112395851094886,-0.110129322150004,-0.108639050841957,
-0.106932174794059,-0.103613666894035,-0.0989681538229891,-0.0813009273757189,
-0.0760333798490178,-0.0730831562979099,-0.070480979211169,-0.0670945711654487,
-0.0585896908869579,-0.0402179526002847,-0.0372703646728362,-0.0356348908774732,
-0.0340912886790107,-0.0316043810609119,-0.0284936180620519,-0.0165415942135776,
-0.00491281277194659,-0.00217218770564259,-9.99999999529155E-7),
 .UNSPECIFIED.);
#1686=B_SPLINE_CURVE_WITH_KNOTS('',3,(#132270,#132271,#132272,#132273,#132274,
#132275,#132276,#132277,#132278,#132279),.UNSPECIFIED.,.F.,.F.,(4,2,2,2,
4),(-0.0255223692981158,-0.0128002959747665,-0.00436963811408314,-0.00196112391871313,
-3.26435750072084E-5),.UNSPECIFIED.);
#1687=B_SPLINE_CURVE_WITH_KNOTS('',3,(#132280,#132281,#132282,#132283,#132284,
#132285,#132286,#132287,#132288,#132289,#132290,#132291,#132292,#132293,
#132294,#132295,#132296,#132297,#132298,#132299,#132300,#132301,#132302,
#132303,#132304,#132305,#132306,#132307,#132308,#132309,#132310,#132311,
#132312,#132313,#132314,#132315,#132316,#132317,#132318,#132319,#132320,
#132321,#132322,#132323,#132324,#132325,#132326,#132327,#132328,#132329,
#132330,#132331,#132332,#132333,#132334,#132335,#132336,#132337,#132338,
#132339,#132340,#132341,#132342,#132343,#132344,#132345,#132346,#132347,
#132348,#132349,#132350,#132351,#132352,#132353,#132354,#132355,#132356,
#132357,#132358,#132359,#132360,#132361,#132362,#132363,#132364,#132365,
#132366,#132367,#132368,#132369,#132370,#132371,#132372,#132373,#132374,
#132375,#132376,#132377,#132378,#132379,#132380,#132381,#132382,#132383,
#132384,#132385,#132386,#132387,#132388,#132389,#132390,#132391,#132392,
#132393,#132394,#132395,#132396,#132397,#132398,#132399,#132400,#132401,
#132402,#132403,#132404,#132405,#132406,#132407,#132408,#132409,#132410,
#132411,#132412,#132413,#132414,#132415,#132416,#132417,#132418,#132419,
#132420,#132421,#132422,#132423,#132424,#132425,#132426,#132427,#132428,
#132429,#132430,#132431,#132432,#132433,#132434,#132435,#132436,#132437,
#132438,#132439,#132440,#132441,#132442,#132443,#132444,#132445,#132446,
#132447,#132448,#132449,#132450,#132451,#132452,#132453,#132454,#132455,
#132456,#132457,#132458,#132459,#132460),.UNSPECIFIED.,.F.,.F.,(4,3,3,3,
3,3,3,3,3,3,3,3,3,3,3,3,3,3,3,3,3,3,3,3,3,3,3,3,3,3,3,3,3,3,3,3,3,3,3,3,
3,3,3,3,3,3,3,3,3,3,3,3,3,3,3,3,3,3,3,3,4),(40.8407044966673,40.9798570562274,
41.1191799295957,41.2589299159688,41.3628052096836,41.3628645393561,41.484853052794,
41.4974413064647,41.631864010953,41.7661481581936,41.9003683000561,42.0346981927973,
42.1690923828433,42.3037471923262,42.3514104949093,42.3514698245815,42.4734583380527,
42.4860465917054,42.6204692962091,42.7547534434654,42.8889735853438,43.0233034781013,
43.1576976681637,43.2923524776632,43.340015780135,43.3400751098072,43.4620636232768,
43.4746518769183,43.6090745814091,43.7433587286522,43.8775788705174,44.0119087632615,
44.1463029533105,44.2809577627967,44.3286210653607,44.328680395033,44.4506689084891,
44.4632571621475,44.5976798666417,44.7319640138885,44.8661841557573,45.0005140485049,
45.1349082385574,45.2695630480469,45.3172263505865,45.3172856802588,45.4392741937587,
45.4518624473747,45.5862851518703,45.7205692991184,45.8547894409887,45.9891193337378,
46.1235135237919,46.258168333283,46.3058316358122,46.305890965474,46.4265984044318,
46.4384912255247,46.570943162863,46.7032833103682,46.779979472002),
 .UNSPECIFIED.);
#1688=B_SPLINE_CURVE_WITH_KNOTS('',3,(#132465,#132466,#132467,#132468,#132469,
#132470,#132471,#132472,#132473,#132474,#132475,#132476,#132477,#132478,
#132479,#132480,#132481,#132482,#132483,#132484,#132485,#132486,#132487,
#132488,#132489,#132490,#132491,#132492,#132493,#132494,#132495,#132496,
#132497,#132498,#132499,#132500,#132501,#132502,#132503,#132504,#132505,
#132506,#132507,#132508,#132509,#132510,#132511,#132512,#132513,#132514,
#132515,#132516,#132517,#132518,#132519,#132520,#132521,#132522,#132523,
#132524,#132525,#132526,#132527,#132528,#132529,#132530,#132531,#132532,
#132533,#132534,#132535,#132536,#132537,#132538,#132539,#132540,#132541,
#132542,#132543,#132544,#132545,#132546,#132547,#132548,#132549,#132550,
#132551,#132552,#132553,#132554,#132555,#132556,#132557,#132558,#132559,
#132560,#132561,#132562,#132563,#132564,#132565,#132566,#132567,#132568,
#132569,#132570,#132571,#132572,#132573,#132574,#132575,#132576,#132577,
#132578,#132579,#132580,#132581,#132582,#132583,#132584,#132585,#132586,
#132587,#132588,#132589,#132590,#132591,#132592,#132593,#132594,#132595,
#132596,#132597,#132598,#132599,#132600,#132601,#132602,#132603,#132604,
#132605,#132606,#132607,#132608,#132609,#132610,#132611,#132612,#132613,
#132614,#132615,#132616,#132617,#132618,#132619,#132620,#132621,#132622,
#132623,#132624,#132625,#132626,#132627,#132628,#132629,#132630,#132631,
#132632,#132633,#132634,#132635,#132636,#132637,#132638,#132639,#132640,
#132641,#132642),.UNSPECIFIED.,.F.,.F.,(4,2,2,2,2,2,2,2,2,2,2,2,2,2,2,2,
2,2,2,2,2,2,2,2,2,2,2,2,2,2,2,2,2,2,2,2,2,2,2,2,2,2,2,2,2,2,2,2,2,2,2,2,
2,2,2,2,2,2,2,2,2,2,2,2,2,2,2,2,2,2,2,2,2,2,2,2,2,2,2,2,2,2,2,2,2,2,2,2,
4),(-0.932467505666577,-0.921105747935325,-0.918464980990969,-0.916891263094845,
-0.915294612522539,-0.912540842579777,-0.903064502647796,-0.886491646128297,
-0.882630982376248,-0.879988922634601,-0.877229281849085,-0.872854982099366,
-0.867463089462418,-0.853055583516473,-0.846697212077067,-0.844528271891396,
-0.843037087162468,-0.841276045079259,-0.837659360607389,-0.834855485147031,
-0.823600553081565,-0.812466175294876,-0.808856495507244,-0.806226872714595,
-0.803381701482514,-0.798543225423195,-0.792315325976461,-0.777298511925181,
-0.772795788772797,-0.770841792240485,-0.769366823470256,-0.767483541907558,
-0.763119274852211,-0.756073949260172,-0.739626403985499,-0.735749220046827,
-0.733104484132722,-0.73034902637389,-0.725997334849761,-0.720644589936917,
-0.706509928809678,-0.699835539441193,-0.697648939116865,-0.696155466876677,
-0.694403840692854,-0.690840123623823,-0.685686308592639,-0.674754887130896,
-0.673290579482916,-0.665107060942649,-0.661718394897937,-0.659109506933057,
-0.656192603968386,-0.650958090906618,-0.647216733962562,-0.633123187275598,
-0.626403632275417,-0.624213135146824,-0.622719145109942,-0.620969547162416,
-0.617417166601867,-0.612287486355764,-0.601502005492716,-0.598569062292694,
-0.591338513711225,-0.588035249109525,-0.585440142582493,-0.58243727314326,
-0.57670842578075,-0.568669641253922,-0.554851921879872,-0.551644034815975,
-0.549957970928539,-0.548441872440278,-0.546107790659626,-0.536329351228345,
-0.519020815879315,-0.515261921928018,-0.512636098585077,-0.509848593466414,
-0.505323137240049,-0.502298051767117,-0.492785537236905,-0.480432238417921,
-0.477778735574285,-0.476202475660992,-0.474608669237597,-0.471868825860901,
-0.466250456168778),.UNSPECIFIED.);
#1689=B_SPLINE_CURVE_WITH_KNOTS('',3,(#132644,#132645,#132646,#132647,#132648,
#132649,#132650,#132651,#132652,#132653,#132654,#132655),.UNSPECIFIED.,
 .F.,.F.,(4,2,2,2,2,4),(-0.0255688444182446,-0.0240999659624579,-0.0225373436534429,
-0.019468758913173,-0.0127753173615656,-1.29626833824403E-5),
 .UNSPECIFIED.);
#1690=B_SPLINE_CURVE_WITH_KNOTS('',3,(#132656,#132657,#132658,#132659,#132660,
#132661,#132662,#132663,#132664,#132665,#132666,#132667,#132668,#132669,
#132670,#132671,#132672,#132673,#132674,#132675,#132676,#132677,#132678,
#132679,#132680,#132681,#132682,#132683,#132684,#132685,#132686,#132687,
#132688,#132689,#132690,#132691,#132692,#132693,#132694,#132695,#132696,
#132697,#132698,#132699,#132700,#132701,#132702,#132703,#132704,#132705,
#132706,#132707,#132708,#132709,#132710,#132711,#132712,#132713,#132714,
#132715,#132716,#132717,#132718,#132719,#132720,#132721,#132722,#132723,
#132724,#132725,#132726,#132727,#132728,#132729,#132730,#132731,#132732,
#132733,#132734,#132735,#132736,#132737,#132738,#132739,#132740,#132741,
#132742,#132743,#132744,#132745,#132746,#132747,#132748,#132749,#132750,
#132751,#132752,#132753,#132754,#132755,#132756,#132757,#132758,#132759,
#132760,#132761,#132762,#132763,#132764,#132765,#132766,#132767,#132768,
#132769,#132770,#132771,#132772,#132773,#132774,#132775,#132776,#132777,
#132778,#132779,#132780,#132781,#132782,#132783,#132784,#132785,#132786,
#132787,#132788,#132789,#132790,#132791,#132792,#132793,#132794,#132795,
#132796,#132797,#132798,#132799,#132800,#132801,#132802,#132803,#132804,
#132805,#132806,#132807,#132808,#132809,#132810,#132811,#132812,#132813,
#132814,#132815,#132816,#132817,#132818,#132819,#132820,#132821,#132822,
#132823,#132824,#132825,#132826,#132827,#132828,#132829,#132830,#132831,
#132832,#132833,#132834,#132835,#132836,#132837,#132838,#132839),
 .UNSPECIFIED.,.F.,.F.,(4,3,3,3,3,3,3,3,3,3,3,3,3,3,3,3,3,3,3,3,3,3,3,3,
3,3,3,3,3,3,3,3,3,3,3,3,3,3,3,3,3,3,3,3,3,3,3,3,3,3,3,3,3,3,3,3,3,3,3,3,
3,4),(47.1238898038469,47.2554184151012,47.2944369210379,47.2944962507101,
47.4164847641539,47.4290730178261,47.5634957223218,47.69777986957,47.8320000114401,
47.9663299041892,48.1007240942431,48.2353789037341,48.2830422062637,48.283101535936,
48.4050900493903,48.4176783030504,48.5521010075445,48.6863851547912,48.8206052966598,
48.9549351894075,49.08932937946,49.2239841889496,49.2716474914894,49.2717068211617,
49.3936953346274,49.4062835882727,49.5407062927633,49.6749904400066,49.8092105818717,
49.9435404746159,50.0779346646649,50.212589474151,50.2602527767151,50.2603121063873,
50.382300619854,50.3948888735117,50.5293115780158,50.6635957252724,50.7978158671509,
50.9321457599082,51.0665399499703,51.2011947594692,51.2488580619408,51.248917391613,
51.3709059050861,51.383494158721,51.5179168632087,51.6522010104491,51.7864211523116,
51.9207510450532,52.0551452350999,52.1898000445839,52.2374633471666,52.2375226768391,
52.359511650272,52.3721089837709,52.5065333880661,52.6456211692066,52.7798775652825,
52.914130819089,53.0485201510646,53.0628845114798),.UNSPECIFIED.);
#1691=B_SPLINE_CURVE_WITH_KNOTS('',3,(#132844,#132845,#132846,#132847,#132848,
#132849,#132850,#132851,#132852,#132853,#132854,#132855,#132856,#132857,
#132858,#132859,#132860,#132861,#132862,#132863,#132864,#132865,#132866,
#132867,#132868,#132869,#132870,#132871,#132872,#132873,#132874,#132875,
#132876,#132877,#132878,#132879,#132880,#132881,#132882,#132883,#132884,
#132885,#132886,#132887,#132888,#132889,#132890,#132891,#132892,#132893,
#132894,#132895,#132896,#132897,#132898,#132899,#132900,#132901,#132902,
#132903,#132904,#132905,#132906,#132907,#132908,#132909,#132910,#132911,
#132912,#132913,#132914,#132915,#132916,#132917,#132918,#132919,#132920,
#132921,#132922,#132923,#132924,#132925,#132926,#132927,#132928,#132929,
#132930,#132931,#132932,#132933,#132934,#132935,#132936,#132937,#132938,
#132939,#132940,#132941,#132942,#132943,#132944,#132945,#132946,#132947,
#132948,#132949,#132950,#132951,#132952,#132953,#132954,#132955,#132956,
#132957,#132958,#132959,#132960,#132961,#132962,#132963,#132964,#132965,
#132966,#132967,#132968,#132969,#132970,#132971,#132972,#132973,#132974,
#132975,#132976,#132977,#132978,#132979,#132980,#132981,#132982,#132983,
#132984,#132985,#132986,#132987,#132988,#132989,#132990,#132991,#132992,
#132993,#132994,#132995,#132996,#132997,#132998,#132999,#133000,#133001,
#133002,#133003,#133004,#133005,#133006,#133007,#133008,#133009,#133010,
#133011),.UNSPECIFIED.,.F.,.F.,(4,2,2,2,2,2,2,2,2,2,2,2,2,2,2,2,2,2,2,2,
2,2,2,2,2,2,2,2,2,2,2,2,2,2,2,2,2,2,2,2,2,2,2,2,2,2,2,2,2,2,2,2,2,2,2,2,
2,2,2,2,2,2,2,2,2,2,2,2,2,2,2,2,2,2,2,2,2,2,2,2,2,2,2,4),(-1.39870355738125,
-1.39709323051322,-1.39438139580999,-1.39166930499781,-1.38755669007251,
-1.3736047233822,-1.36520698520691,-1.36182875593005,-1.35918661641566,
-1.35761269078721,-1.35621499900328,-1.3536933908489,-1.33973391704012,
-1.32727511715368,-1.32338833003953,-1.320715499827,-1.31828358701918,-1.31423135284018,
-1.29931765007779,-1.2914916128012,-1.28684221459254,-1.28491723923631,
-1.28344349786372,-1.28153382378389,-1.2773037203214,-1.26076534078919,
-1.25511305432508,-1.25059007762816,-1.24780316922912,-1.24517725477441,
-1.2414171294668,-1.22410020745919,-1.21503416014965,-1.21232723971982,
-1.21074015558069,-1.20935169995419,-1.20688363802996,-1.19245399721653,
-1.18401330010431,-1.17810686102362,-1.17507431121453,-1.17248187027663,
-1.1692198109322,-1.16176295059518,-1.14882582466956,-1.14077648941288,
-1.13848465966282,-1.13699042889687,-1.13529414411419,-1.13203221812217,
-1.12750004796582,-1.11115007077001,-1.10485954630007,-1.10176524853483,
-1.09943519954046,-1.09637016545883,-1.09026444696507,-1.08135125504194,
-1.0678990417944,-1.06531879510893,-1.0637572124499,-1.06214661592754,-1.05932337689066,
-1.05562364911276,-1.04558879054432,-1.03391940752607,-1.02982178401969,
-1.02738263284155,-1.02471646795181,-1.02086990506828,-1.00800276375469,
-0.994426303294931,-0.991859322204321,-0.990453579502622,-0.988889461216315,
-0.986296795370386,-0.975354828504718,-0.960344432689713,-0.956302765445229,
-0.953872476545109,-0.951197830055049,-0.947300943870582,-0.933695294690738,
-0.932467505666577),.UNSPECIFIED.);
#1692=B_SPLINE_CURVE_WITH_KNOTS('',3,(#133013,#133014,#133015,#133016,#133017,
#133018,#133019,#133020,#133021,#133022,#133023,#133024,#133025,#133026,
#133027,#133028),.UNSPECIFIED.,.F.,.F.,(4,3,3,3,3,4),(53.0628845126283,
53.1975485052734,53.2260686323923,53.2261279621233,53.3579672512799,53.4070751110265),
 .UNSPECIFIED.);
#1693=B_SPLINE_CURVE_WITH_KNOTS('',3,(#133029,#133030,#133031,#133032,#133033,
#133034,#133035,#133036,#133037,#133038,#133039,#133040,#133041,#133042,
#133043,#133044,#133045,#133046,#133047,#133048,#133049,#133050,#133051,
#133052,#133053,#133054,#133055,#133056,#133057,#133058,#133059,#133060,
#133061,#133062,#133063,#133064,#133065,#133066,#133067,#133068,#133069,
#133070,#133071,#133072,#133073,#133074,#133075,#133076,#133077,#133078,
#133079,#133080,#133081,#133082,#133083,#133084,#133085,#133086,#133087,
#133088,#133089,#133090,#133091,#133092,#133093,#133094,#133095,#133096,
#133097,#133098,#133099,#133100,#133101,#133102,#133103,#133104,#133105,
#133106,#133107,#133108,#133109,#133110,#133111,#133112,#133113,#133114,
#133115,#133116,#133117,#133118,#133119,#133120,#133121,#133122,#133123,
#133124,#133125,#133126,#133127,#133128,#133129,#133130,#133131,#133132,
#133133,#133134,#133135,#133136,#133137,#133138,#133139,#133140,#133141,
#133142,#133143,#133144,#133145,#133146,#133147,#133148,#133149,#133150,
#133151,#133152,#133153,#133154,#133155,#133156,#133157,#133158,#133159,
#133160,#133161,#133162,#133163,#133164,#133165,#133166,#133167,#133168,
#133169,#133170,#133171,#133172,#133173,#133174,#133175,#133176,#133177,
#133178,#133179,#133180,#133181,#133182,#133183,#133184,#133185,#133186,
#133187,#133188,#133189,#133190,#133191,#133192,#133193,#133194,#133195,
#133196,#133197,#133198,#133199,#133200,#133201,#133202,#133203,#133204,
#133205,#133206,#133207,#133208,#133209,#133210,#133211,#133212),
 .UNSPECIFIED.,.F.,.F.,(4,3,3,3,3,3,3,3,3,3,3,3,3,3,3,3,3,3,3,3,3,3,3,3,
3,3,3,3,3,3,3,3,3,3,3,3,3,3,3,3,3,3,3,3,3,3,3,3,3,3,3,3,3,3,3,3,3,3,3,3,
3,4),(53.407075112124,53.5395748225813,53.6719291179904,53.8076153178973,
53.9400068534946,54.0773403855563,54.2013994567497,54.214673917618,54.2147332472902,
54.3367217607587,54.3493100143317,54.4837327187534,54.6180168659285,54.7522370077264,
54.8865669004053,55.0209610903902,55.1556158998146,55.2032792028438,55.2033385325175,
55.3253270457457,55.3379152995103,55.4723380038829,55.6066221510069,55.740842292752,
55.8751721853761,56.0095663753049,56.1442211846721,56.1918844880695,56.1919438177393,
56.3139323317598,56.3265205853932,56.4609432904251,56.595227438209,56.7294475806129,
56.8637774738881,56.9981716644641,57.132826474465,57.1804897732952,57.1805491029676,
57.3025376163047,57.3151258693894,57.4495485731948,57.5838327197582,57.7180528609505,
57.8523827530386,57.9867769424403,58.1214317513003,58.1690950585209,58.1691543882022,
58.2911428999394,58.3037311547547,58.438153858685,58.5724380053582,58.7066581466454,
58.8409880388054,58.975382228266,59.110037037165,59.1577003437467,59.157759673411,
59.2819978092843,59.2969476030988,59.3472480465758),.UNSPECIFIED.);
#1694=B_SPLINE_CURVE_WITH_KNOTS('',3,(#133217,#133218,#133219,#133220,#133221,
#133222,#133223,#133224,#133225,#133226,#133227,#133228,#133229,#133230,
#133231,#133232,#133233,#133234,#133235,#133236,#133237,#133238,#133239,
#133240,#133241,#133242,#133243,#133244,#133245,#133246,#133247,#133248,
#133249,#133250,#133251,#133252,#133253,#133254,#133255,#133256,#133257,
#133258,#133259,#133260,#133261,#133262,#133263,#133264,#133265,#133266,
#133267,#133268,#133269,#133270,#133271,#133272,#133273,#133274,#133275,
#133276,#133277,#133278,#133279,#133280,#133281,#133282,#133283,#133284,
#133285,#133286,#133287,#133288,#133289,#133290,#133291,#133292,#133293,
#133294,#133295,#133296,#133297,#133298,#133299,#133300,#133301,#133302,
#133303,#133304,#133305,#133306,#133307,#133308,#133309,#133310,#133311,
#133312,#133313,#133314,#133315,#133316,#133317,#133318,#133319,#133320,
#133321,#133322,#133323,#133324,#133325,#133326,#133327,#133328,#133329,
#133330,#133331,#133332,#133333,#133334,#133335,#133336,#133337,#133338,
#133339,#133340,#133341,#133342,#133343,#133344,#133345,#133346,#133347,
#133348,#133349,#133350,#133351,#133352,#133353,#133354,#133355,#133356,
#133357,#133358,#133359,#133360,#133361,#133362,#133363,#133364,#133365,
#133366,#133367,#133368,#133369,#133370,#133371,#133372,#133373,#133374,
#133375,#133376,#133377,#133378),.UNSPECIFIED.,.F.,.F.,(4,2,2,2,2,2,2,2,
2,2,2,2,2,2,2,2,2,2,2,2,2,2,2,2,2,2,2,2,2,2,2,2,2,2,2,2,2,2,2,2,2,2,2,2,
2,2,2,2,2,2,2,2,2,2,2,2,2,2,2,2,2,2,2,2,2,2,2,2,2,2,2,2,2,2,2,2,2,2,2,2,
4),(-1.86488544419714,-1.85365696410191,-1.84188530806308,-1.8377699615751,
-1.83505758284678,-1.83234651493028,-1.8282386120305,-1.81418462147493,
-1.80585531449291,-1.8024919954102,-1.79985847775436,-1.79828636155049,
-1.79668846069849,-1.79392749548157,-1.78371066127597,-1.77295238263045,
-1.76820227091544,-1.76420762745974,-1.76151660859604,-1.75910234343622,
-1.75516109849534,-1.73920378676322,-1.72934771433257,-1.7265523264965,
-1.72494746555782,-1.7233814331193,-1.72077835931069,-1.70757744503926,
-1.69442125350727,-1.69057828212119,-1.68791291387726,-1.68547335476776,
-1.68137238568769,-1.66958280630193,-1.65962674498408,-1.65594067604859,
-1.65312534435754,-1.65151645214735,-1.64995370372793,-1.64736731673291,
-1.63399597602187,-1.62098615509736,-1.61713967660845,-1.61447367123057,
-1.61203467117964,-1.60793749639567,-1.59632334200793,-1.58623232335227,
-1.58252183488291,-1.57969300110081,-1.57808136151013,-1.57652077683416,
-1.57394539094252,-1.56046890246613,-1.54766833468709,-1.54376518407776,
-1.54108971110237,-1.53866078594208,-1.53462673505591,-1.51951620823629,
-1.51179811411383,-1.50718683313568,-1.50526735100317,-1.50379363339642,
-1.50187868174028,-1.49839427370121,-1.48394776240774,-1.47570542619547,
-1.47106081549173,-1.46825151334881,-1.46560719826398,-1.46189699443107,
-1.44423356580635,-1.4353578376186,-1.43267345740897,-1.43109098872612,
-1.42969948523156,-1.4272135118021,-1.41294200199675,-1.40120451120901,
-1.39870355738125),.UNSPECIFIED.);
#1695=B_SPLINE_CURVE_WITH_KNOTS('',3,(#133380,#133381,#133382,#133383,#133384,
#133385,#133386,#133387,#133388,#133389,#133390,#133391),.UNSPECIFIED.,
 .F.,.F.,(4,2,2,2,2,4),(-0.0255459513154411,-0.0128046247359227,-0.00704877268430528,
-0.00400898693505774,-0.00198358349779247,-3.22321518027115E-5),
 .UNSPECIFIED.);
#1696=B_SPLINE_CURVE_WITH_KNOTS('',3,(#133392,#133393,#133394,#133395,#133396,
#133397,#133398,#133399,#133400,#133401,#133402,#133403,#133404,#133405,
#133406,#133407,#133408,#133409,#133410,#133411,#133412,#133413,#133414,
#133415,#133416,#133417,#133418,#133419,#133420,#133421,#133422,#133423,
#133424,#133425,#133426,#133427,#133428,#133429,#133430,#133431,#133432,
#133433,#133434,#133435,#133436,#133437,#133438,#133439,#133440,#133441,
#133442,#133443,#133444,#133445,#133446,#133447,#133448,#133449,#133450,
#133451,#133452,#133453,#133454,#133455,#133456,#133457,#133458,#133459,
#133460,#133461,#133462,#133463,#133464,#133465,#133466,#133467,#133468,
#133469,#133470,#133471,#133472,#133473,#133474,#133475,#133476,#133477,
#133478,#133479,#133480,#133481,#133482,#133483,#133484,#133485,#133486,
#133487,#133488,#133489,#133490,#133491,#133492,#133493,#133494,#133495,
#133496,#133497,#133498,#133499,#133500,#133501,#133502,#133503,#133504,
#133505,#133506,#133507,#133508,#133509,#133510,#133511,#133512,#133513,
#133514,#133515,#133516,#133517,#133518,#133519,#133520,#133521,#133522,
#133523,#133524,#133525,#133526,#133527,#133528,#133529,#133530,#133531,
#133532,#133533,#133534,#133535,#133536,#133537,#133538,#133539,#133540,
#133541,#133542,#133543,#133544,#133545,#133546,#133547,#133548,#133549,
#133550,#133551,#133552,#133553,#133554,#133555,#133556,#133557,#133558,
#133559,#133560,#133561,#133562,#133563,#133564,#133565,#133566,#133567,
#133568,#133569,#133570,#133571,#133572,#133573,#133574,#133575),
 .UNSPECIFIED.,.F.,.F.,(4,3,3,3,3,3,3,3,3,3,3,3,3,3,3,3,3,3,3,3,3,3,3,3,
3,3,3,3,3,3,3,3,3,3,3,3,3,3,3,3,3,3,3,3,3,3,3,3,3,3,3,3,3,3,3,3,3,3,3,3,
3,4),(59.6902604970919,59.833396490693,59.9768904150285,60.1083013831761,
60.1209187781749,60.1463056289724,60.1463649586525,60.2683534696589,60.2809417196825,
60.4153644181217,60.54964855935,60.6838686952516,60.8181985821629,60.9525927664475,
61.0872475703433,61.1349109141981,61.1349702439286,61.2569587469848,61.2695470095179,
61.4039697124623,61.5382538580817,61.6724739982504,61.8068038892084,61.9411980774173,
62.0758528850074,62.1235161994239,62.1235755289416,62.2455640740847,62.2581523224295,
62.3925750532376,62.5268592268259,62.6610793949968,62.7954093137422,62.9298035296484,
63.0644583644501,63.1121214846496,63.1121808144321,63.2341692995476,63.2467575308238,
63.3811801848166,63.5154642817972,63.6496843737593,63.7840142175936,63.9184083592464,
64.053063121709,64.1007267698753,64.1007860998983,64.222774553837,64.2353628755673,
64.3697855883676,64.504069743311,64.6382898922554,64.7726197911066,64.907013986709,
65.041668800863,65.089332055101,65.089391383594,65.2103712287251,65.2243357646258,
65.3570552955892,65.4932010943946,65.6293468932001),.UNSPECIFIED.);
#1697=B_SPLINE_CURVE_WITH_KNOTS('',3,(#133580,#133581,#133582,#133583,#133584,
#133585,#133586,#133587,#133588,#133589,#133590,#133591,#133592,#133593,
#133594,#133595,#133596,#133597,#133598,#133599,#133600,#133601,#133602,
#133603,#133604,#133605,#133606,#133607,#133608,#133609,#133610,#133611,
#133612,#133613,#133614,#133615,#133616,#133617,#133618,#133619,#133620,
#133621,#133622,#133623,#133624,#133625,#133626,#133627,#133628,#133629,
#133630,#133631,#133632,#133633,#133634,#133635,#133636,#133637,#133638,
#133639,#133640,#133641,#133642,#133643,#133644,#133645,#133646,#133647,
#133648,#133649,#133650,#133651,#133652,#133653,#133654,#133655,#133656,
#133657,#133658,#133659,#133660,#133661,#133662,#133663,#133664,#133665,
#133666,#133667,#133668,#133669,#133670,#133671,#133672,#133673,#133674,
#133675,#133676,#133677,#133678,#133679,#133680,#133681,#133682,#133683,
#133684,#133685,#133686,#133687,#133688,#133689,#133690,#133691,#133692,
#133693,#133694,#133695,#133696,#133697,#133698,#133699,#133700,#133701,
#133702,#133703,#133704,#133705,#133706,#133707,#133708,#133709,#133710,
#133711,#133712,#133713,#133714,#133715,#133716,#133717,#133718,#133719,
#133720,#133721,#133722,#133723,#133724,#133725,#133726,#133727,#133728,
#133729,#133730,#133731,#133732,#133733,#133734,#133735,#133736,#133737,
#133738,#133739,#133740,#133741,#133742,#133743,#133744,#133745,#133746,
#133747,#133748,#133749,#133750,#133751,#133752,#133753),.UNSPECIFIED.,
 .F.,.F.,(4,2,2,2,2,2,2,2,2,2,2,2,2,2,2,2,2,2,2,2,2,2,2,2,2,2,2,2,2,2,2,
2,2,2,2,2,2,2,2,2,2,2,2,2,2,2,2,2,2,2,2,2,2,2,2,2,2,2,2,2,2,2,2,2,2,2,2,
2,2,2,2,2,2,2,2,2,2,2,2,2,2,2,2,2,2,2,4),(-2.33098756212136,-2.32770212338009,
-2.31646610862759,-2.31383727485646,-2.31227335927866,-2.3106807241972,
-2.30794645461203,-2.29611141811926,-2.28637100161808,-2.28184644323665,
-2.27798786631659,-2.27531564131121,-2.27287179559994,-2.26876677381099,
-2.25479628646993,-2.24647852907023,-2.24311720114654,-2.24048372665527,
-2.23890820971872,-2.2373051432569,-2.2345233794621,-2.22405370772014,-2.21350214987303,
-2.21028520318969,-2.20556272023435,-2.20273890313631,-2.20010064510374,
-2.19643211268646,-2.17846101382362,-2.16973969810326,-2.16707419053712,
-2.16549600903019,-2.16390710980978,-2.16118601762735,-2.14955060040506,
-2.13967950270808,-2.13512859700862,-2.13125680230042,-2.12858867128916,
-2.12615767250019,-2.12209914607859,-2.11158873066677,-2.10236725326662,
-2.09755506665382,-2.09416608045372,-2.09244206899566,-2.09094186917777,
-2.08870398943557,-2.08144867600362,-2.0678575206045,-2.06258828831665,
-2.05828447768567,-2.05553756358227,-2.0528862316855,-2.04897089413123,
-2.03281880079352,-2.02309300260766,-2.02031147442211,-2.01870894554653,
-2.01713997775017,-2.01452258642402,-2.00149125823969,-1.98821011764705,
-1.98436174964467,-1.98169562380451,-1.97925727365408,-1.97516312319999,
-1.96082692639583,-1.95266821622917,-1.94934204921407,-1.94672994932158,
-1.94516230094211,-1.9437604087264,-1.94121343615269,-1.92520656097234,
-1.91642760513991,-1.91175119696534,-1.90893650509543,-1.90629567161495,
-1.90260492384512,-1.88481387908689,-1.87600911026292,-1.87333356871875,
-1.8717531447419,-1.87036068286077,-1.86786840001739,-1.86488544419714),
 .UNSPECIFIED.);
#1698=B_SPLINE_CURVE_WITH_KNOTS('',3,(#133755,#133756,#133757,#133758,#133759,
#133760,#133761,#133762),.UNSPECIFIED.,.F.,.F.,(4,2,2,4),(-0.025564683553867,
-0.0212145539685123,-0.0127726529739691,-2.44579138260531E-5),
 .UNSPECIFIED.);
#1699=B_SPLINE_CURVE_WITH_KNOTS('',3,(#133763,#133764,#133765,#133766,#133767,
#133768,#133769,#133770,#133771,#133772,#133773,#133774,#133775,#133776,
#133777,#133778,#133779,#133780,#133781,#133782,#133783,#133784,#133785,
#133786,#133787,#133788,#133789,#133790,#133791,#133792,#133793,#133794,
#133795,#133796,#133797,#133798,#133799,#133800,#133801,#133802,#133803,
#133804,#133805,#133806,#133807,#133808,#133809,#133810,#133811,#133812,
#133813,#133814,#133815,#133816,#133817,#133818,#133819,#133820,#133821,
#133822,#133823,#133824,#133825,#133826,#133827,#133828,#133829,#133830,
#133831,#133832,#133833,#133834,#133835,#133836,#133837,#133838,#133839,
#133840,#133841,#133842,#133843,#133844,#133845,#133846,#133847,#133848,
#133849,#133850,#133851,#133852,#133853,#133854,#133855,#133856,#133857,
#133858,#133859,#133860,#133861,#133862,#133863,#133864,#133865,#133866,
#133867,#133868,#133869,#133870,#133871,#133872,#133873,#133874,#133875,
#133876,#133877,#133878,#133879,#133880,#133881,#133882,#133883,#133884,
#133885,#133886,#133887,#133888,#133889,#133890,#133891,#133892,#133893,
#133894,#133895,#133896,#133897,#133898,#133899,#133900,#133901,#133902,
#133903,#133904,#133905,#133906,#133907,#133908,#133909,#133910,#133911,
#133912,#133913,#133914,#133915,#133916,#133917,#133918,#133919,#133920,
#133921,#133922,#133923,#133924,#133925,#133926,#133927,#133928,#133929,
#133930,#133931,#133932,#133933,#133934,#133935,#133936,#133937,#133938,
#133939,#133940,#133941,#133942,#133943),.UNSPECIFIED.,.F.,.F.,(4,3,3,3,
3,3,3,3,3,3,3,3,3,3,3,3,3,3,3,3,3,3,3,3,3,3,3,3,3,3,3,3,3,3,3,3,3,3,3,3,
3,3,3,3,3,3,3,3,3,3,3,3,3,3,3,3,3,3,3,3,4),(65.9734457253856,66.0779373403268,
66.0779966711752,66.1999849066616,66.2125730323752,66.3469953325592,66.4812790769259,
66.6154988183458,66.7498283179537,66.8842221186058,67.0188765491595,67.0665426255525,
67.0666019571481,67.1885901731476,67.2011789324032,67.3356018427714,67.469886191261,
67.6041065292935,67.7384366089515,67.8728309808017,68.0074859622503,68.0551479107782,
68.055207231863,68.1771974382781,68.1897850942651,68.3242088928125,68.4584941386067,
68.5927153806746,68.7270463656961,68.8614416447783,68.9960975246431,69.0437531960039,
69.0438125367751,69.1657985521766,69.1783861667009,69.3128057452608,69.4470867745264,
69.5813038141547,69.7156306567655,69.8500218230336,69.9846736860503,70.0323584812297,
70.0324178197249,70.1544052585737,70.1669971512239,70.3014224006743,70.4357090587619,
70.5699316714495,70.7042639534098,70.8386604884861,70.973317548102,71.0209637664554,
71.0210230350765,71.1430235684413,71.1556109739712,71.2900401917198,71.4243262573423,
71.558617078649,71.6929036281056,71.827384909386,71.9125675619089),
 .UNSPECIFIED.);
#1700=B_SPLINE_CURVE_WITH_KNOTS('',3,(#133946,#133947,#133948,#133949,#133950,
#133951,#133952,#133953,#133954,#133955,#133956,#133957,#133958,#133959,
#133960,#133961),.UNSPECIFIED.,.F.,.F.,(4,3,3,3,3,4),(71.9125675627573,
72.0095690516811,72.0096284787209,72.1412543016073,72.1828455385974,72.2566310313772),
 .UNSPECIFIED.);
#1701=B_SPLINE_CURVE_WITH_KNOTS('',3,(#133963,#133964,#133965,#133966,#133967,
#133968,#133969,#133970,#133971,#133972,#133973,#133974,#133975,#133976,
#133977,#133978,#133979,#133980,#133981,#133982,#133983,#133984,#133985,
#133986,#133987,#133988,#133989,#133990,#133991,#133992,#133993,#133994,
#133995,#133996,#133997,#133998,#133999,#134000,#134001,#134002,#134003,
#134004,#134005,#134006,#134007,#134008,#134009,#134010,#134011,#134012,
#134013,#134014,#134015,#134016,#134017,#134018,#134019,#134020,#134021,
#134022,#134023,#134024,#134025,#134026,#134027,#134028,#134029,#134030,
#134031,#134032,#134033,#134034,#134035,#134036,#134037,#134038,#134039,
#134040,#134041,#134042,#134043,#134044,#134045,#134046,#134047,#134048,
#134049,#134050,#134051,#134052,#134053,#134054,#134055,#134056,#134057,
#134058,#134059,#134060,#134061,#134062,#134063,#134064,#134065,#134066,
#134067,#134068,#134069,#134070,#134071,#134072,#134073,#134074,#134075,
#134076,#134077,#134078,#134079,#134080,#134081,#134082,#134083,#134084,
#134085,#134086,#134087,#134088,#134089,#134090,#134091,#134092,#134093,
#134094,#134095,#134096,#134097,#134098,#134099,#134100,#134101,#134102,
#134103,#134104,#134105,#134106,#134107,#134108,#134109,#134110,#134111,
#134112,#134113,#134114,#134115,#134116,#134117,#134118,#134119,#134120,
#134121,#134122,#134123,#134124,#134125,#134126,#134127,#134128),
 .UNSPECIFIED.,.F.,.F.,(4,3,3,3,3,3,3,3,3,3,3,3,3,3,3,3,3,3,3,3,3,3,3,3,
3,3,3,3,3,3,3,3,3,3,3,3,3,3,3,3,3,3,3,3,3,3,3,3,3,3,3,3,3,3,3,4),(72.2566310325653,
72.3894374467591,72.5221457062876,72.6549339998429,72.7877622859877,72.9208549495036,
72.9981743369069,72.9982336898363,73.1202228277463,73.1328364350279,73.2672849584092,
73.4015946806294,73.5358400918455,73.6701945703871,73.8046129814629,73.9392911666892,
73.9867796221326,73.9868385324179,74.108906242501,74.1214488825271,74.255905222884,
74.390223385728,74.5244778313572,74.6588421253742,74.793270814519,74.9279598270099,
74.9753849073583,74.9754450466518,75.0972621653067,75.1098516883196,75.2441047719449,
75.3782194139114,75.5122705854141,75.6464338624038,75.7806625836947,75.9151557208552,
75.963990192584,75.9640493770624,76.0861045734201,76.0988646685781,76.2335246164758,
76.3680442827096,76.5024976289655,76.6370551344828,76.7716739686609,76.9065461955451,
76.9525954778098,76.9526520815709,77.0740905315279,77.0857383232952,77.2186728465627,
77.351477171386,77.4843223777113,77.6171794272965,77.7502847484,77.8457368347758),
 .UNSPECIFIED.);
#1702=B_SPLINE_CURVE_WITH_KNOTS('',3,(#134132,#134133,#134134,#134135,#134136,
#134137,#134138,#134139,#134140,#134141,#134142,#134143,#134144,#134145,
#134146,#134147,#134148,#134149,#134150,#134151,#134152,#134153,#134154,
#134155,#134156,#134157,#134158,#134159,#134160,#134161,#134162,#134163,
#134164,#134165,#134166,#134167,#134168,#134169,#134170,#134171,#134172,
#134173,#134174,#134175,#134176,#134177,#134178,#134179,#134180,#134181,
#134182,#134183,#134184,#134185,#134186,#134187,#134188,#134189,#134190,
#134191,#134192,#134193,#134194,#134195,#134196,#134197,#134198,#134199,
#134200,#134201,#134202,#134203,#134204,#134205,#134206,#134207,#134208,
#134209,#134210,#134211,#134212,#134213,#134214,#134215,#134216,#134217,
#134218,#134219,#134220,#134221,#134222,#134223,#134224,#134225,#134226,
#134227,#134228,#134229,#134230,#134231,#134232,#134233,#134234,#134235,
#134236,#134237,#134238,#134239,#134240,#134241,#134242,#134243,#134244,
#134245,#134246,#134247,#134248,#134249,#134250,#134251,#134252,#134253,
#134254,#134255,#134256,#134257,#134258,#134259,#134260,#134261,#134262,
#134263,#134264,#134265,#134266,#134267,#134268,#134269,#134270,#134271,
#134272,#134273),.UNSPECIFIED.,.F.,.F.,(4,3,3,3,3,3,3,3,3,3,3,3,3,3,3,3,
3,3,3,3,3,3,3,3,3,3,3,3,3,3,3,3,3,3,3,3,3,3,3,3,3,3,3,3,3,3,3,4),(72.2566314741396,
72.4045609950112,72.5414579617111,72.5535140284593,72.6517127398032,72.651772204656,
72.7769482243648,72.7866266109606,72.9212659463293,73.0557645182426,73.1901963484967,
73.3247324131253,73.4593295146966,73.5865318565016,73.5941811307337,73.6415997214062,
73.6416565254697,73.7672874375975,73.7764261693097,73.9109853627333,74.0454085321108,
74.1797698262172,74.3142431103432,74.44878183488,74.5751854586477,74.5835822859716,
74.6314745352144,74.6315408462834,74.7551941928077,74.7648000454726,74.8978457776245,
75.0307559072255,75.1636079962241,75.2965913886114,75.429648976824,75.5630004736777,
75.6213694876214,75.6214251670971,75.748251875531,75.7596541443398,75.8976295032126,
76.0354124773744,76.1793867300085,76.3170070392934,76.4546118871423,76.5830703015199,
76.5923159523675,76.6113094879108),.UNSPECIFIED.);
#1703=B_SPLINE_CURVE_WITH_KNOTS('',3,(#134274,#134275,#134276,#134277,#134278,
#134279,#134280,#134281,#134282,#134283,#134284,#134285,#134286,#134287),
 .UNSPECIFIED.,.F.,.F.,(4,2,2,2,2,2,4),(-2.35651538611015,-2.35375456035493,
-2.3513626252777,-2.34892223761256,-2.3465069901102,-2.34248392432371,-2.33098756212136),
 .UNSPECIFIED.);
#1704=B_SPLINE_CURVE_WITH_KNOTS('',3,(#134290,#134291,#134292,#134293,#134294,
#134295,#134296,#134297,#134298,#134299,#134300,#134301,#134302,#134303,
#134304,#134305,#134306,#134307,#134308,#134309,#134310,#134311,#134312,
#134313,#134314,#134315,#134316,#134317,#134318,#134319,#134320,#134321,
#134322,#134323,#134324,#134325,#134326,#134327,#134328,#134329,#134330,
#134331,#134332,#134333,#134334,#134335,#134336,#134337,#134338,#134339,
#134340,#134341,#134342,#134343,#134344,#134345,#134346,#134347),
 .UNSPECIFIED.,.F.,.F.,(4,3,3,3,3,3,3,3,3,3,3,3,3,3,3,3,3,3,3,4),(63.947346022237,
64.0856677806405,64.2249239385586,64.3424808528907,64.468575806381,64.5944806171026,
64.7202560417844,64.8459626123754,64.971755226253,65.0975842562297,65.2236618847116,
65.3323651737044,65.4568633156543,65.5811766710722,65.7053691135383,65.8295042784497,
65.9537253005869,66.0779993018877,66.2024833656448,66.2363314693039),
 .UNSPECIFIED.);
#1705=B_SPLINE_CURVE_WITH_KNOTS('',3,(#134350,#134351,#134352,#134353,#134354,
#134355,#134356,#134357,#134358,#134359,#134360,#134361,#134362,#134363,
#134364,#134365,#134366,#134367,#134368,#134369,#134370,#134371,#134372,
#134373,#134374,#134375,#134376,#134377,#134378,#134379,#134380,#134381,
#134382,#134383),.UNSPECIFIED.,.F.,.F.,(4,3,3,3,3,3,3,3,3,3,3,4),(-68.3020181361455,
-68.1732359894119,-68.0445307062512,-67.9158529349099,-67.7871533887138,
-67.6582664075924,-67.5292846492219,-67.4000115996097,-67.3134128509198,
-67.1758788210711,-67.0392397108572,-66.9234304578509),.UNSPECIFIED.);
#1706=B_SPLINE_CURVE_WITH_KNOTS('',3,(#134673,#134674,#134675,#134676,#134677,
#134678,#134679,#134680,#134681,#134682,#134683,#134684,#134685,#134686,
#134687,#134688,#134689,#134690,#134691,#134692,#134693,#134694,#134695,
#134696,#134697,#134698),.UNSPECIFIED.,.F.,.F.,(4,2,2,2,2,2,2,2,2,2,2,2,
4),(0.105663848425438,0.141373353833559,0.175486205805465,0.215538764100116,
0.275546330497321,0.326160459620167,0.383983207715567,0.434851934495649,
0.488868806433905,0.539980848713981,0.589887233590854,0.654795876329018,
0.744278844687171),.UNSPECIFIED.);
#1707=B_SPLINE_CURVE_WITH_KNOTS('',3,(#134700,#134701,#134702,#134703,#134704,
#134705,#134706,#134707,#134708,#134709,#134710,#134711,#134712,#134713,
#134714,#134715,#134716,#134717,#134718,#134719,#134720,#134721,#134722,
#134723,#134724,#134725,#134726,#134727,#134728,#134729,#134730,#134731,
#134732,#134733,#134734,#134735,#134736,#134737,#134738,#134739,#134740,
#134741,#134742,#134743,#134744,#134745,#134746,#134747,#134748,#134749,
#134750,#134751,#134752,#134753,#134754,#134755,#134756,#134757,#134758,
#134759,#134760,#134761,#134762,#134763,#134764,#134765,#134766,#134767,
#134768,#134769,#134770,#134771,#134772,#134773,#134774,#134775),
 .UNSPECIFIED.,.F.,.F.,(4,3,3,3,3,3,3,3,3,3,3,3,3,3,3,3,3,3,3,3,3,3,3,3,
3,4),(-0.176229339719688,-0.16930135536687,-0.158068822610707,-0.153210440573506,
-0.14999874865766,-0.137539014752818,-0.130276774573411,-0.127219505533131,
-0.124662971108758,-0.112718638611185,-0.101066870224045,-0.0953479689548292,
-0.0930447645920619,-0.0906327597761066,-0.0794410933175649,-0.0687205266155614,
-0.0632054306857541,-0.060455489415314,-0.058082450533308,-0.0468942590722208,
-0.0358420032534035,-0.0306121296933921,-0.0277796741820399,-0.0172857919180543,
-0.00699398448747527,0.),.UNSPECIFIED.);
#1708=B_SPLINE_CURVE_WITH_KNOTS('',3,(#134776,#134777,#134778,#134779,#134780,
#134781),.UNSPECIFIED.,.F.,.F.,(4,2,4),(-0.0013480645929508,-0.000678455957808124,
-1.00000007721593E-6),.UNSPECIFIED.);
#1709=B_SPLINE_CURVE_WITH_KNOTS('',3,(#134782,#134783,#134784,#134785,#134786,
#134787,#134788,#134789,#134790,#134791,#134792,#134793),.UNSPECIFIED.,
 .F.,.F.,(4,2,2,2,2,4),(1.80267612534286E-5,0.030912223860268,0.0584819346422233,
0.0746239839028914,0.10502074371225,0.105663848425438),.UNSPECIFIED.);
#1710=B_SPLINE_CURVE_WITH_KNOTS('',3,(#134798,#134799,#134800,#134801),
 .UNSPECIFIED.,.F.,.F.,(4,4),(0.,0.00718622469090485),.UNSPECIFIED.);
#1711=B_SPLINE_CURVE_WITH_KNOTS('',3,(#134802,#134803,#134804,#134805,#134806,
#134807,#134808,#134809,#134810,#134811,#134812,#134813,#134814,#134815,
#134816,#134817,#134818,#134819,#134820,#134821,#134822,#134823,#134824,
#134825,#134826,#134827,#134828,#134829,#134830,#134831,#134832,#134833,
#134834,#134835,#134836,#134837,#134838,#134839,#134840,#134841,#134842,
#134843,#134844,#134845,#134846,#134847,#134848,#134849,#134850,#134851,
#134852,#134853,#134854,#134855,#134856,#134857,#134858,#134859,#134860,
#134861,#134862,#134863,#134864,#134865,#134866,#134867,#134868,#134869,
#134870,#134871,#134872,#134873,#134874,#134875,#134876,#134877),
 .UNSPECIFIED.,.F.,.F.,(4,3,3,3,3,3,3,3,3,3,3,3,3,3,3,3,3,3,3,3,3,3,3,3,
3,4),(-0.178587760439507,-0.171910820567902,-0.161828334105325,-0.158626626042432,
-0.155662350564125,-0.144861472649272,-0.140141558931839,-0.137336962197544,
-0.134642654294749,-0.123288481409911,-0.111857928729176,-0.105498830583136,
-0.103071300928935,-0.0912509288672889,-0.0798445627588778,-0.0745908481568186,
-0.07199198364724,-0.0695034129914027,-0.0574052630533521,-0.0453071131153016,
-0.0394332477820004,-0.0367368004707021,-0.0343156904617242,-0.0216249730003383,
-0.00901663940650531,0.),.UNSPECIFIED.);
#1712=B_SPLINE_CURVE_WITH_KNOTS('',3,(#135159,#135160,#135161,#135162,#135163,
#135164,#135165,#135166,#135167,#135168,#135169,#135170),.UNSPECIFIED.,
 .F.,.F.,(4,2,2,2,2,4),(-0.106753670550095,-0.0847951227008117,-0.0660598735029805,
-0.0401729541102252,-0.0191044959439433,0.),.UNSPECIFIED.);
#1725=SHAPE_REPRESENTATION_RELATIONSHIP('SRR','None',#135349,#1738);
#1738=ADVANCED_BREP_SHAPE_REPRESENTATION('',(#1764),#135281);
#1751=STYLED_ITEM('',(#135423),#1764);
#1764=MANIFOLD_SOLID_BREP('Body1',#32087);
#1992=CYLINDRICAL_SURFACE('',#34150,0.96675);
#1993=CYLINDRICAL_SURFACE('',#34152,0.96675);
#1994=CYLINDRICAL_SURFACE('',#34153,0.96675);
#1995=CYLINDRICAL_SURFACE('',#34154,0.96675);
#1996=CYLINDRICAL_SURFACE('',#34155,0.96675);
#1997=CYLINDRICAL_SURFACE('',#34156,0.96675);
#1998=CYLINDRICAL_SURFACE('',#34157,0.96675);
#1999=CYLINDRICAL_SURFACE('',#34158,0.96675);
#2000=CYLINDRICAL_SURFACE('',#34159,0.96675);
#2001=CYLINDRICAL_SURFACE('',#34160,0.96675);
#2002=CYLINDRICAL_SURFACE('',#34161,0.96675);
#2003=CYLINDRICAL_SURFACE('',#34162,0.739000000000001);
#2004=CYLINDRICAL_SURFACE('',#34164,0.739000000000001);
#2005=CYLINDRICAL_SURFACE('',#34165,0.739000000000001);
#2006=CYLINDRICAL_SURFACE('',#34166,0.739000000000001);
#2007=CYLINDRICAL_SURFACE('',#34167,0.739000000000001);
#2008=CYLINDRICAL_SURFACE('',#34168,0.739000000000001);
#2009=CYLINDRICAL_SURFACE('',#34169,0.739000000000001);
#2010=CYLINDRICAL_SURFACE('',#34170,0.739000000000001);
#2011=CYLINDRICAL_SURFACE('',#34171,0.739000000000001);
#2012=CYLINDRICAL_SURFACE('',#34172,0.739000000000001);
#2013=CYLINDRICAL_SURFACE('',#34173,0.739000000000001);
#2014=CYLINDRICAL_SURFACE('',#34175,0.96675);
#2015=CYLINDRICAL_SURFACE('',#34191,1.9);
#2231=FACE_BOUND('',#7059,.T.);
#3338=PLANE('',#34177);
#3339=PLANE('',#34183);
#3340=PLANE('',#34185);
#3341=PLANE('',#34189);
#3342=PLANE('',#34190);
#3343=PLANE('',#34194);
#3344=PLANE('',#34196);
#3345=PLANE('',#34199);
#5062=FACE_OUTER_BOUND('',#7031,.T.);
#5063=FACE_OUTER_BOUND('',#7032,.T.);
#5064=FACE_OUTER_BOUND('',#7033,.T.);
#5065=FACE_OUTER_BOUND('',#7034,.T.);
#5066=FACE_OUTER_BOUND('',#7035,.T.);
#5067=FACE_OUTER_BOUND('',#7036,.T.);
#5068=FACE_OUTER_BOUND('',#7037,.T.);
#5069=FACE_OUTER_BOUND('',#7038,.T.);
#5070=FACE_OUTER_BOUND('',#7039,.T.);
#5071=FACE_OUTER_BOUND('',#7040,.T.);
#5072=FACE_OUTER_BOUND('',#7041,.T.);
#5073=FACE_OUTER_BOUND('',#7042,.T.);
#5074=FACE_OUTER_BOUND('',#7043,.T.);
#5075=FACE_OUTER_BOUND('',#7044,.T.);
#5076=FACE_OUTER_BOUND('',#7045,.T.);
#5077=FACE_OUTER_BOUND('',#7046,.T.);
#5078=FACE_OUTER_BOUND('',#7047,.T.);
#5079=FACE_OUTER_BOUND('',#7048,.T.);
#5080=FACE_OUTER_BOUND('',#7049,.T.);
#5081=FACE_OUTER_BOUND('',#7050,.T.);
#5082=FACE_OUTER_BOUND('',#7051,.T.);
#5083=FACE_OUTER_BOUND('',#7052,.T.);
#5084=FACE_OUTER_BOUND('',#7053,.T.);
#5085=FACE_OUTER_BOUND('',#7054,.T.);
#5086=FACE_OUTER_BOUND('',#7055,.T.);
#5087=FACE_OUTER_BOUND('',#7056,.T.);
#5088=FACE_OUTER_BOUND('',#7057,.T.);
#5089=FACE_OUTER_BOUND('',#7058,.T.);
#5090=FACE_OUTER_BOUND('',#7060,.T.);
#5091=FACE_OUTER_BOUND('',#7061,.T.);
#5092=FACE_OUTER_BOUND('',#7062,.T.);
#5093=FACE_OUTER_BOUND('',#7063,.T.);
#5094=FACE_OUTER_BOUND('',#7064,.T.);
#5095=FACE_OUTER_BOUND('',#7065,.T.);
#5096=FACE_OUTER_BOUND('',#7066,.T.);
#5097=FACE_OUTER_BOUND('',#7067,.T.);
#5098=FACE_OUTER_BOUND('',#7068,.T.);
#5099=FACE_OUTER_BOUND('',#7069,.T.);
#7031=EDGE_LOOP('',(#30018,#30019,#30020,#30021));
#7032=EDGE_LOOP('',(#30022,#30023,#30024,#30025));
#7033=EDGE_LOOP('',(#30026,#30027,#30028,#30029));
#7034=EDGE_LOOP('',(#30030,#30031,#30032,#30033));
#7035=EDGE_LOOP('',(#30034,#30035,#30036,#30037));
#7036=EDGE_LOOP('',(#30038,#30039,#30040,#30041));
#7037=EDGE_LOOP('',(#30042,#30043,#30044,#30045));
#7038=EDGE_LOOP('',(#30046,#30047,#30048,#30049));
#7039=EDGE_LOOP('',(#30050,#30051,#30052,#30053));
#7040=EDGE_LOOP('',(#30054,#30055,#30056,#30057));
#7041=EDGE_LOOP('',(#30058,#30059,#30060,#30061));
#7042=EDGE_LOOP('',(#30062,#30063,#30064,#30065));
#7043=EDGE_LOOP('',(#30066,#30067,#30068,#30069,#30070));
#7044=EDGE_LOOP('',(#30071,#30072,#30073,#30074,#30075));
#7045=EDGE_LOOP('',(#30076,#30077,#30078,#30079,#30080));
#7046=EDGE_LOOP('',(#30081,#30082,#30083,#30084,#30085));
#7047=EDGE_LOOP('',(#30086,#30087,#30088,#30089,#30090));
#7048=EDGE_LOOP('',(#30091,#30092,#30093,#30094,#30095));
#7049=EDGE_LOOP('',(#30096,#30097,#30098,#30099,#30100));
#7050=EDGE_LOOP('',(#30101,#30102,#30103,#30104,#30105));
#7051=EDGE_LOOP('',(#30106,#30107,#30108,#30109,#30110));
#7052=EDGE_LOOP('',(#30111,#30112,#30113,#30114,#30115,#30116));
#7053=EDGE_LOOP('',(#30117,#30118,#30119,#30120));
#7054=EDGE_LOOP('',(#30121,#30122,#30123,#30124,#30125,#30126,#30127,#30128,
#30129,#30130,#30131,#30132,#30133,#30134,#30135,#30136,#30137,#30138,#30139,
#30140,#30141,#30142,#30143,#30144,#30145,#30146,#30147,#30148));
#7055=EDGE_LOOP('',(#30149,#30150,#30151,#30152,#30153,#30154));
#7056=EDGE_LOOP('',(#30155,#30156,#30157,#30158,#30159,#30160,#30161,#30162,
#30163,#30164,#30165,#30166,#30167,#30168,#30169,#30170,#30171,#30172,#30173,
#30174,#30175,#30176,#30177,#30178,#30179,#30180,#30181,#30182,#30183,#30184,
#30185,#30186,#30187,#30188,#30189,#30190));
#7057=EDGE_LOOP('',(#30191,#30192,#30193,#30194,#30195,#30196,#30197));
#7058=EDGE_LOOP('',(#30198));
#7059=EDGE_LOOP('',(#30199));
#7060=EDGE_LOOP('',(#30200,#30201,#30202,#30203,#30204));
#7061=EDGE_LOOP('',(#30205,#30206,#30207,#30208,#30209,#30210));
#7062=EDGE_LOOP('',(#30211,#30212,#30213,#30214,#30215,#30216));
#7063=EDGE_LOOP('',(#30217,#30218,#30219,#30220,#30221,#30222,#30223,#30224,
#30225,#30226,#30227,#30228));
#7064=EDGE_LOOP('',(#30229,#30230));
#7065=EDGE_LOOP('',(#30231,#30232));
#7066=EDGE_LOOP('',(#30233,#30234,#30235,#30236));
#7067=EDGE_LOOP('',(#30237));
#7068=EDGE_LOOP('',(#30238,#30239,#30240,#30241,#30242,#30243,#30244,#30245));
#7069=EDGE_LOOP('',(#30246,#30247,#30248,#30249));
#9876=LINE('',#126909,#12713);
#9877=LINE('',#126996,#12714);
#9878=LINE('',#127369,#12715);
#9879=LINE('',#127731,#12716);
#9880=LINE('',#128103,#12717);
#9881=LINE('',#128439,#12718);
#9882=LINE('',#128795,#12719);
#9883=LINE('',#129163,#12720);
#9884=LINE('',#129519,#12721);
#9885=LINE('',#129871,#12722);
#9886=LINE('',#130211,#12723);
#9887=LINE('',#130587,#12724);
#9888=LINE('',#130642,#12725);
#9889=LINE('',#131007,#12726);
#9890=LINE('',#131376,#12727);
#9891=LINE('',#131745,#12728);
#9892=LINE('',#132100,#12729);
#9893=LINE('',#132464,#12730);
#9894=LINE('',#132843,#12731);
#9895=LINE('',#133216,#12732);
#9896=LINE('',#133579,#12733);
#9897=LINE('',#135183,#12734);
#9898=LINE('',#135187,#12735);
#9899=LINE('',#135191,#12736);
#9900=LINE('',#135193,#12737);
#9901=LINE('',#135199,#12738);
#9902=LINE('',#135205,#12739);
#9903=LINE('',#135211,#12740);
#9904=LINE('',#135216,#12741);
#9905=LINE('',#135218,#12742);
#9906=LINE('',#135230,#12743);
#12713=VECTOR('',#40868,0.96675);
#12714=VECTOR('',#40873,0.96675);
#12715=VECTOR('',#40876,0.96675);
#12716=VECTOR('',#40879,0.96675);
#12717=VECTOR('',#40882,0.96675);
#12718=VECTOR('',#40885,0.96675);
#12719=VECTOR('',#40888,0.96675);
#12720=VECTOR('',#40891,0.96675);
#12721=VECTOR('',#40894,0.96675);
#12722=VECTOR('',#40897,0.96675);
#12723=VECTOR('',#40900,0.96675);
#12724=VECTOR('',#40903,0.739000000000001);
#12725=VECTOR('',#40908,0.739000000000001);
#12726=VECTOR('',#40911,0.739000000000001);
#12727=VECTOR('',#40914,0.739000000000001);
#12728=VECTOR('',#40917,0.739000000000001);
#12729=VECTOR('',#40920,0.739000000000001);
#12730=VECTOR('',#40923,0.739000000000001);
#12731=VECTOR('',#40926,0.739000000000001);
#12732=VECTOR('',#40929,0.739000000000001);
#12733=VECTOR('',#40932,0.739000000000001);
#12734=VECTOR('',#40961,10.);
#12735=VECTOR('',#40964,10.);
#12736=VECTOR('',#40969,10.);
#12737=VECTOR('',#40970,10.);
#12738=VECTOR('',#40971,10.);
#12739=VECTOR('',#40974,10.);
#12740=VECTOR('',#40975,10.);
#12741=VECTOR('',#40976,10.);
#12742=VECTOR('',#40979,1.9);
#12743=VECTOR('',#41000,0.825);
#13227=CIRCLE('',#34151,0.96675);
#13228=CIRCLE('',#34163,0.739000000000001);
#13229=CIRCLE('',#34174,0.739000000000001);
#13230=CIRCLE('',#34176,0.96675);
#13231=CIRCLE('',#34178,0.96675);
#13232=CIRCLE('',#34179,0.96675);
#13233=CIRCLE('',#34181,1.06675);
#13234=CIRCLE('',#34182,0.1);
#13235=CIRCLE('',#34184,1.9);
#13236=CIRCLE('',#34186,1.9);
#13237=CIRCLE('',#34187,1.9);
#13238=CIRCLE('',#34188,1.9);
#13239=CIRCLE('',#34192,1.9);
#13240=CIRCLE('',#34193,1.9);
#13241=CIRCLE('',#34195,1.5);
#13242=CIRCLE('',#34197,1.5);
#13243=CIRCLE('',#34200,0.649999999999999);
#16258=VERTEX_POINT('',#126907);
#16259=VERTEX_POINT('',#126908);
#16260=VERTEX_POINT('',#126910);
#16261=VERTEX_POINT('',#126963);
#16262=VERTEX_POINT('',#126994);
#16263=VERTEX_POINT('',#126995);
#16264=VERTEX_POINT('',#127367);
#16265=VERTEX_POINT('',#127368);
#16266=VERTEX_POINT('',#127729);
#16267=VERTEX_POINT('',#127730);
#16268=VERTEX_POINT('',#128101);
#16269=VERTEX_POINT('',#128102);
#16270=VERTEX_POINT('',#128437);
#16271=VERTEX_POINT('',#128438);
#16272=VERTEX_POINT('',#128793);
#16273=VERTEX_POINT('',#128794);
#16274=VERTEX_POINT('',#129161);
#16275=VERTEX_POINT('',#129162);
#16276=VERTEX_POINT('',#129517);
#16277=VERTEX_POINT('',#129518);
#16278=VERTEX_POINT('',#129869);
#16279=VERTEX_POINT('',#129870);
#16280=VERTEX_POINT('',#130209);
#16281=VERTEX_POINT('',#130210);
#16282=VERTEX_POINT('',#130585);
#16283=VERTEX_POINT('',#130586);
#16284=VERTEX_POINT('',#130588);
#16285=VERTEX_POINT('',#130629);
#16286=VERTEX_POINT('',#130640);
#16287=VERTEX_POINT('',#130641);
#16288=VERTEX_POINT('',#130809);
#16289=VERTEX_POINT('',#131005);
#16290=VERTEX_POINT('',#131006);
#16291=VERTEX_POINT('',#131178);
#16292=VERTEX_POINT('',#131374);
#16293=VERTEX_POINT('',#131375);
#16294=VERTEX_POINT('',#131545);
#16295=VERTEX_POINT('',#131743);
#16296=VERTEX_POINT('',#131744);
#16297=VERTEX_POINT('',#131908);
#16298=VERTEX_POINT('',#132098);
#16299=VERTEX_POINT('',#132099);
#16300=VERTEX_POINT('',#132269);
#16301=VERTEX_POINT('',#132462);
#16302=VERTEX_POINT('',#132463);
#16303=VERTEX_POINT('',#132643);
#16304=VERTEX_POINT('',#132841);
#16305=VERTEX_POINT('',#132842);
#16306=VERTEX_POINT('',#133012);
#16307=VERTEX_POINT('',#133214);
#16308=VERTEX_POINT('',#133215);
#16309=VERTEX_POINT('',#133379);
#16310=VERTEX_POINT('',#133577);
#16311=VERTEX_POINT('',#133578);
#16312=VERTEX_POINT('',#133754);
#16313=VERTEX_POINT('',#133945);
#16314=VERTEX_POINT('',#133962);
#16315=VERTEX_POINT('',#134129);
#16316=VERTEX_POINT('',#134131);
#16317=VERTEX_POINT('',#134289);
#16318=VERTEX_POINT('',#134348);
#16319=VERTEX_POINT('',#134672);
#16320=VERTEX_POINT('',#134699);
#16321=VERTEX_POINT('',#134795);
#16322=VERTEX_POINT('',#134797);
#16323=VERTEX_POINT('',#135172);
#16324=VERTEX_POINT('',#135176);
#16325=VERTEX_POINT('',#135179);
#16326=VERTEX_POINT('',#135180);
#16327=VERTEX_POINT('',#135182);
#16328=VERTEX_POINT('',#135184);
#16329=VERTEX_POINT('',#135186);
#16330=VERTEX_POINT('',#135190);
#16331=VERTEX_POINT('',#135192);
#16332=VERTEX_POINT('',#135194);
#16333=VERTEX_POINT('',#135198);
#16334=VERTEX_POINT('',#135204);
#16335=VERTEX_POINT('',#135206);
#16336=VERTEX_POINT('',#135210);
#16337=VERTEX_POINT('',#135212);
#16338=VERTEX_POINT('',#135227);
#20860=EDGE_CURVE('',#16258,#16259,#9876,.T.);
#20861=EDGE_CURVE('',#16258,#16260,#1649,.T.);
#20862=EDGE_CURVE('',#16260,#16261,#13227,.T.);
#20863=EDGE_CURVE('',#16261,#16259,#1650,.T.);
#20864=EDGE_CURVE('',#16262,#16263,#9877,.T.);
#20865=EDGE_CURVE('',#16262,#16258,#1651,.T.);
#20866=EDGE_CURVE('',#16259,#16263,#1652,.T.);
#20867=EDGE_CURVE('',#16264,#16265,#9878,.T.);
#20868=EDGE_CURVE('',#16264,#16262,#1653,.T.);
#20869=EDGE_CURVE('',#16263,#16265,#1654,.T.);
#20870=EDGE_CURVE('',#16266,#16267,#9879,.T.);
#20871=EDGE_CURVE('',#16266,#16264,#1655,.T.);
#20872=EDGE_CURVE('',#16265,#16267,#1656,.T.);
#20873=EDGE_CURVE('',#16268,#16269,#9880,.T.);
#20874=EDGE_CURVE('',#16268,#16266,#1657,.T.);
#20875=EDGE_CURVE('',#16267,#16269,#1658,.T.);
#20876=EDGE_CURVE('',#16270,#16271,#9881,.T.);
#20877=EDGE_CURVE('',#16270,#16268,#1659,.T.);
#20878=EDGE_CURVE('',#16269,#16271,#1660,.T.);
#20879=EDGE_CURVE('',#16272,#16273,#9882,.T.);
#20880=EDGE_CURVE('',#16272,#16270,#1661,.T.);
#20881=EDGE_CURVE('',#16271,#16273,#1662,.T.);
#20882=EDGE_CURVE('',#16274,#16275,#9883,.T.);
#20883=EDGE_CURVE('',#16274,#16272,#1663,.T.);
#20884=EDGE_CURVE('',#16273,#16275,#1664,.T.);
#20885=EDGE_CURVE('',#16276,#16277,#9884,.T.);
#20886=EDGE_CURVE('',#16276,#16274,#1665,.T.);
#20887=EDGE_CURVE('',#16275,#16277,#1666,.T.);
#20888=EDGE_CURVE('',#16278,#16279,#9885,.T.);
#20889=EDGE_CURVE('',#16278,#16276,#1667,.T.);
#20890=EDGE_CURVE('',#16277,#16279,#1668,.T.);
#20891=EDGE_CURVE('',#16280,#16281,#9886,.T.);
#20892=EDGE_CURVE('',#16280,#16278,#1669,.T.);
#20893=EDGE_CURVE('',#16279,#16281,#1670,.T.);
#20894=EDGE_CURVE('',#16282,#16283,#9887,.T.);
#20895=EDGE_CURVE('',#16284,#16282,#1671,.F.);
#20896=EDGE_CURVE('',#16285,#16284,#13228,.T.);
#20897=EDGE_CURVE('',#16285,#16283,#1672,.T.);
#20898=EDGE_CURVE('',#16286,#16287,#9888,.T.);
#20899=EDGE_CURVE('',#16282,#16286,#1673,.F.);
#20900=EDGE_CURVE('',#16283,#16288,#1674,.T.);
#20901=EDGE_CURVE('',#16288,#16287,#1675,.T.);
#20902=EDGE_CURVE('',#16289,#16290,#9889,.T.);
#20903=EDGE_CURVE('',#16286,#16289,#1676,.F.);
#20904=EDGE_CURVE('',#16287,#16291,#1677,.T.);
#20905=EDGE_CURVE('',#16291,#16290,#1678,.T.);
#20906=EDGE_CURVE('',#16292,#16293,#9890,.T.);
#20907=EDGE_CURVE('',#16289,#16292,#1679,.F.);
#20908=EDGE_CURVE('',#16290,#16294,#1680,.T.);
#20909=EDGE_CURVE('',#16294,#16293,#1681,.T.);
#20910=EDGE_CURVE('',#16295,#16296,#9891,.T.);
#20911=EDGE_CURVE('',#16292,#16295,#1682,.F.);
#20912=EDGE_CURVE('',#16293,#16297,#1683,.T.);
#20913=EDGE_CURVE('',#16297,#16296,#1684,.T.);
#20914=EDGE_CURVE('',#16298,#16299,#9892,.T.);
#20915=EDGE_CURVE('',#16295,#16298,#1685,.F.);
#20916=EDGE_CURVE('',#16296,#16300,#1686,.T.);
#20917=EDGE_CURVE('',#16300,#16299,#1687,.T.);
#20918=EDGE_CURVE('',#16301,#16302,#9893,.T.);
#20919=EDGE_CURVE('',#16298,#16301,#1688,.F.);
#20920=EDGE_CURVE('',#16299,#16303,#1689,.T.);
#20921=EDGE_CURVE('',#16303,#16302,#1690,.T.);
#20922=EDGE_CURVE('',#16304,#16305,#9894,.T.);
#20923=EDGE_CURVE('',#16301,#16304,#1691,.F.);
#20924=EDGE_CURVE('',#16302,#16306,#1692,.T.);
#20925=EDGE_CURVE('',#16306,#16305,#1693,.T.);
#20926=EDGE_CURVE('',#16307,#16308,#9895,.T.);
#20927=EDGE_CURVE('',#16304,#16307,#1694,.F.);
#20928=EDGE_CURVE('',#16305,#16309,#1695,.T.);
#20929=EDGE_CURVE('',#16309,#16308,#1696,.T.);
#20930=EDGE_CURVE('',#16310,#16311,#9896,.T.);
#20931=EDGE_CURVE('',#16307,#16310,#1697,.F.);
#20932=EDGE_CURVE('',#16308,#16312,#1698,.T.);
#20933=EDGE_CURVE('',#16312,#16311,#1699,.T.);
#20934=EDGE_CURVE('',#16311,#16313,#1700,.T.);
#20935=EDGE_CURVE('',#16313,#16314,#1701,.T.);
#20936=EDGE_CURVE('',#16315,#16314,#13229,.T.);
#20937=EDGE_CURVE('',#16316,#16315,#1702,.T.);
#20938=EDGE_CURVE('',#16310,#16316,#1703,.F.);
#20939=EDGE_CURVE('',#16281,#16317,#1704,.T.);
#20940=EDGE_CURVE('',#16318,#16317,#13230,.T.);
#20941=EDGE_CURVE('',#16318,#16280,#1705,.T.);
#20942=EDGE_CURVE('',#16284,#16319,#1706,.F.);
#20943=EDGE_CURVE('',#16320,#16315,#1707,.T.);
#20944=EDGE_CURVE('',#16317,#16320,#1708,.T.);
#20945=EDGE_CURVE('',#16319,#16261,#1709,.F.);
#20946=EDGE_CURVE('',#16320,#16321,#13231,.T.);
#20947=EDGE_CURVE('',#16314,#16322,#1710,.T.);
#20948=EDGE_CURVE('',#16322,#16318,#1711,.T.);
#20949=EDGE_CURVE('',#16321,#16318,#13232,.T.);
#20950=EDGE_CURVE('',#16260,#16285,#1712,.T.);
#20951=EDGE_CURVE('',#16323,#16323,#13233,.T.);
#20952=EDGE_CURVE('',#16323,#16321,#13234,.T.);
#20953=EDGE_CURVE('',#16324,#16324,#13235,.T.);
#20954=EDGE_CURVE('',#16325,#16326,#13236,.T.);
#20955=EDGE_CURVE('',#16327,#16325,#9897,.T.);
#20956=EDGE_CURVE('',#16328,#16327,#13237,.T.);
#20957=EDGE_CURVE('',#16329,#16328,#9898,.T.);
#20958=EDGE_CURVE('',#16326,#16329,#13238,.T.);
#20959=EDGE_CURVE('',#16329,#16330,#9899,.T.);
#20960=EDGE_CURVE('',#16331,#16328,#9900,.T.);
#20961=EDGE_CURVE('',#16332,#16331,#284,.T.);
#20962=EDGE_CURVE('',#16333,#16332,#9901,.T.);
#20963=EDGE_CURVE('',#16330,#16333,#285,.T.);
#20964=EDGE_CURVE('',#16334,#16325,#9902,.T.);
#20965=EDGE_CURVE('',#16335,#16334,#286,.T.);
#20966=EDGE_CURVE('',#16336,#16335,#9903,.T.);
#20967=EDGE_CURVE('',#16337,#16336,#287,.T.);
#20968=EDGE_CURVE('',#16327,#16337,#9904,.T.);
#20969=EDGE_CURVE('',#16326,#16324,#9905,.T.);
#20970=EDGE_CURVE('',#16331,#16330,#13239,.T.);
#20971=EDGE_CURVE('',#16334,#16337,#13240,.T.);
#20972=EDGE_CURVE('',#16332,#16333,#13241,.T.);
#20973=EDGE_CURVE('',#16335,#16336,#13242,.T.);
#20974=EDGE_CURVE('',#16338,#16338,#13243,.T.);
#20975=EDGE_CURVE('',#16338,#16319,#9906,.T.);
#30018=ORIENTED_EDGE('',*,*,#20860,.F.);
#30019=ORIENTED_EDGE('',*,*,#20861,.T.);
#30020=ORIENTED_EDGE('',*,*,#20862,.T.);
#30021=ORIENTED_EDGE('',*,*,#20863,.T.);
#30022=ORIENTED_EDGE('',*,*,#20864,.F.);
#30023=ORIENTED_EDGE('',*,*,#20865,.T.);
#30024=ORIENTED_EDGE('',*,*,#20860,.T.);
#30025=ORIENTED_EDGE('',*,*,#20866,.T.);
#30026=ORIENTED_EDGE('',*,*,#20867,.F.);
#30027=ORIENTED_EDGE('',*,*,#20868,.T.);
#30028=ORIENTED_EDGE('',*,*,#20864,.T.);
#30029=ORIENTED_EDGE('',*,*,#20869,.T.);
#30030=ORIENTED_EDGE('',*,*,#20870,.F.);
#30031=ORIENTED_EDGE('',*,*,#20871,.T.);
#30032=ORIENTED_EDGE('',*,*,#20867,.T.);
#30033=ORIENTED_EDGE('',*,*,#20872,.T.);
#30034=ORIENTED_EDGE('',*,*,#20873,.F.);
#30035=ORIENTED_EDGE('',*,*,#20874,.T.);
#30036=ORIENTED_EDGE('',*,*,#20870,.T.);
#30037=ORIENTED_EDGE('',*,*,#20875,.T.);
#30038=ORIENTED_EDGE('',*,*,#20876,.F.);
#30039=ORIENTED_EDGE('',*,*,#20877,.T.);
#30040=ORIENTED_EDGE('',*,*,#20873,.T.);
#30041=ORIENTED_EDGE('',*,*,#20878,.T.);
#30042=ORIENTED_EDGE('',*,*,#20879,.F.);
#30043=ORIENTED_EDGE('',*,*,#20880,.T.);
#30044=ORIENTED_EDGE('',*,*,#20876,.T.);
#30045=ORIENTED_EDGE('',*,*,#20881,.T.);
#30046=ORIENTED_EDGE('',*,*,#20882,.F.);
#30047=ORIENTED_EDGE('',*,*,#20883,.T.);
#30048=ORIENTED_EDGE('',*,*,#20879,.T.);
#30049=ORIENTED_EDGE('',*,*,#20884,.T.);
#30050=ORIENTED_EDGE('',*,*,#20885,.F.);
#30051=ORIENTED_EDGE('',*,*,#20886,.T.);
#30052=ORIENTED_EDGE('',*,*,#20882,.T.);
#30053=ORIENTED_EDGE('',*,*,#20887,.T.);
#30054=ORIENTED_EDGE('',*,*,#20888,.F.);
#30055=ORIENTED_EDGE('',*,*,#20889,.T.);
#30056=ORIENTED_EDGE('',*,*,#20885,.T.);
#30057=ORIENTED_EDGE('',*,*,#20890,.T.);
#30058=ORIENTED_EDGE('',*,*,#20891,.F.);
#30059=ORIENTED_EDGE('',*,*,#20892,.T.);
#30060=ORIENTED_EDGE('',*,*,#20888,.T.);
#30061=ORIENTED_EDGE('',*,*,#20893,.T.);
#30062=ORIENTED_EDGE('',*,*,#20894,.F.);
#30063=ORIENTED_EDGE('',*,*,#20895,.F.);
#30064=ORIENTED_EDGE('',*,*,#20896,.F.);
#30065=ORIENTED_EDGE('',*,*,#20897,.T.);
#30066=ORIENTED_EDGE('',*,*,#20898,.F.);
#30067=ORIENTED_EDGE('',*,*,#20899,.F.);
#30068=ORIENTED_EDGE('',*,*,#20894,.T.);
#30069=ORIENTED_EDGE('',*,*,#20900,.T.);
#30070=ORIENTED_EDGE('',*,*,#20901,.T.);
#30071=ORIENTED_EDGE('',*,*,#20902,.F.);
#30072=ORIENTED_EDGE('',*,*,#20903,.F.);
#30073=ORIENTED_EDGE('',*,*,#20898,.T.);
#30074=ORIENTED_EDGE('',*,*,#20904,.T.);
#30075=ORIENTED_EDGE('',*,*,#20905,.T.);
#30076=ORIENTED_EDGE('',*,*,#20906,.F.);
#30077=ORIENTED_EDGE('',*,*,#20907,.F.);
#30078=ORIENTED_EDGE('',*,*,#20902,.T.);
#30079=ORIENTED_EDGE('',*,*,#20908,.T.);
#30080=ORIENTED_EDGE('',*,*,#20909,.T.);
#30081=ORIENTED_EDGE('',*,*,#20910,.F.);
#30082=ORIENTED_EDGE('',*,*,#20911,.F.);
#30083=ORIENTED_EDGE('',*,*,#20906,.T.);
#30084=ORIENTED_EDGE('',*,*,#20912,.T.);
#30085=ORIENTED_EDGE('',*,*,#20913,.T.);
#30086=ORIENTED_EDGE('',*,*,#20914,.F.);
#30087=ORIENTED_EDGE('',*,*,#20915,.F.);
#30088=ORIENTED_EDGE('',*,*,#20910,.T.);
#30089=ORIENTED_EDGE('',*,*,#20916,.T.);
#30090=ORIENTED_EDGE('',*,*,#20917,.T.);
#30091=ORIENTED_EDGE('',*,*,#20918,.F.);
#30092=ORIENTED_EDGE('',*,*,#20919,.F.);
#30093=ORIENTED_EDGE('',*,*,#20914,.T.);
#30094=ORIENTED_EDGE('',*,*,#20920,.T.);
#30095=ORIENTED_EDGE('',*,*,#20921,.T.);
#30096=ORIENTED_EDGE('',*,*,#20922,.F.);
#30097=ORIENTED_EDGE('',*,*,#20923,.F.);
#30098=ORIENTED_EDGE('',*,*,#20918,.T.);
#30099=ORIENTED_EDGE('',*,*,#20924,.T.);
#30100=ORIENTED_EDGE('',*,*,#20925,.T.);
#30101=ORIENTED_EDGE('',*,*,#20926,.F.);
#30102=ORIENTED_EDGE('',*,*,#20927,.F.);
#30103=ORIENTED_EDGE('',*,*,#20922,.T.);
#30104=ORIENTED_EDGE('',*,*,#20928,.T.);
#30105=ORIENTED_EDGE('',*,*,#20929,.T.);
#30106=ORIENTED_EDGE('',*,*,#20930,.F.);
#30107=ORIENTED_EDGE('',*,*,#20931,.F.);
#30108=ORIENTED_EDGE('',*,*,#20926,.T.);
#30109=ORIENTED_EDGE('',*,*,#20932,.T.);
#30110=ORIENTED_EDGE('',*,*,#20933,.T.);
#30111=ORIENTED_EDGE('',*,*,#20930,.T.);
#30112=ORIENTED_EDGE('',*,*,#20934,.T.);
#30113=ORIENTED_EDGE('',*,*,#20935,.T.);
#30114=ORIENTED_EDGE('',*,*,#20936,.F.);
#30115=ORIENTED_EDGE('',*,*,#20937,.F.);
#30116=ORIENTED_EDGE('',*,*,#20938,.F.);
#30117=ORIENTED_EDGE('',*,*,#20891,.T.);
#30118=ORIENTED_EDGE('',*,*,#20939,.T.);
#30119=ORIENTED_EDGE('',*,*,#20940,.F.);
#30120=ORIENTED_EDGE('',*,*,#20941,.T.);
#30121=ORIENTED_EDGE('',*,*,#20942,.F.);
#30122=ORIENTED_EDGE('',*,*,#20895,.T.);
#30123=ORIENTED_EDGE('',*,*,#20899,.T.);
#30124=ORIENTED_EDGE('',*,*,#20903,.T.);
#30125=ORIENTED_EDGE('',*,*,#20907,.T.);
#30126=ORIENTED_EDGE('',*,*,#20911,.T.);
#30127=ORIENTED_EDGE('',*,*,#20915,.T.);
#30128=ORIENTED_EDGE('',*,*,#20919,.T.);
#30129=ORIENTED_EDGE('',*,*,#20923,.T.);
#30130=ORIENTED_EDGE('',*,*,#20927,.T.);
#30131=ORIENTED_EDGE('',*,*,#20931,.T.);
#30132=ORIENTED_EDGE('',*,*,#20938,.T.);
#30133=ORIENTED_EDGE('',*,*,#20937,.T.);
#30134=ORIENTED_EDGE('',*,*,#20943,.F.);
#30135=ORIENTED_EDGE('',*,*,#20944,.F.);
#30136=ORIENTED_EDGE('',*,*,#20939,.F.);
#30137=ORIENTED_EDGE('',*,*,#20893,.F.);
#30138=ORIENTED_EDGE('',*,*,#20890,.F.);
#30139=ORIENTED_EDGE('',*,*,#20887,.F.);
#30140=ORIENTED_EDGE('',*,*,#20884,.F.);
#30141=ORIENTED_EDGE('',*,*,#20881,.F.);
#30142=ORIENTED_EDGE('',*,*,#20878,.F.);
#30143=ORIENTED_EDGE('',*,*,#20875,.F.);
#30144=ORIENTED_EDGE('',*,*,#20872,.F.);
#30145=ORIENTED_EDGE('',*,*,#20869,.F.);
#30146=ORIENTED_EDGE('',*,*,#20866,.F.);
#30147=ORIENTED_EDGE('',*,*,#20863,.F.);
#30148=ORIENTED_EDGE('',*,*,#20945,.F.);
#30149=ORIENTED_EDGE('',*,*,#20946,.F.);
#30150=ORIENTED_EDGE('',*,*,#20943,.T.);
#30151=ORIENTED_EDGE('',*,*,#20936,.T.);
#30152=ORIENTED_EDGE('',*,*,#20947,.T.);
#30153=ORIENTED_EDGE('',*,*,#20948,.T.);
#30154=ORIENTED_EDGE('',*,*,#20949,.F.);
#30155=ORIENTED_EDGE('',*,*,#20950,.F.);
#30156=ORIENTED_EDGE('',*,*,#20861,.F.);
#30157=ORIENTED_EDGE('',*,*,#20865,.F.);
#30158=ORIENTED_EDGE('',*,*,#20868,.F.);
#30159=ORIENTED_EDGE('',*,*,#20871,.F.);
#30160=ORIENTED_EDGE('',*,*,#20874,.F.);
#30161=ORIENTED_EDGE('',*,*,#20877,.F.);
#30162=ORIENTED_EDGE('',*,*,#20880,.F.);
#30163=ORIENTED_EDGE('',*,*,#20883,.F.);
#30164=ORIENTED_EDGE('',*,*,#20886,.F.);
#30165=ORIENTED_EDGE('',*,*,#20889,.F.);
#30166=ORIENTED_EDGE('',*,*,#20892,.F.);
#30167=ORIENTED_EDGE('',*,*,#20941,.F.);
#30168=ORIENTED_EDGE('',*,*,#20948,.F.);
#30169=ORIENTED_EDGE('',*,*,#20947,.F.);
#30170=ORIENTED_EDGE('',*,*,#20935,.F.);
#30171=ORIENTED_EDGE('',*,*,#20934,.F.);
#30172=ORIENTED_EDGE('',*,*,#20933,.F.);
#30173=ORIENTED_EDGE('',*,*,#20932,.F.);
#30174=ORIENTED_EDGE('',*,*,#20929,.F.);
#30175=ORIENTED_EDGE('',*,*,#20928,.F.);
#30176=ORIENTED_EDGE('',*,*,#20925,.F.);
#30177=ORIENTED_EDGE('',*,*,#20924,.F.);
#30178=ORIENTED_EDGE('',*,*,#20921,.F.);
#30179=ORIENTED_EDGE('',*,*,#20920,.F.);
#30180=ORIENTED_EDGE('',*,*,#20917,.F.);
#30181=ORIENTED_EDGE('',*,*,#20916,.F.);
#30182=ORIENTED_EDGE('',*,*,#20913,.F.);
#30183=ORIENTED_EDGE('',*,*,#20912,.F.);
#30184=ORIENTED_EDGE('',*,*,#20909,.F.);
#30185=ORIENTED_EDGE('',*,*,#20908,.F.);
#30186=ORIENTED_EDGE('',*,*,#20905,.F.);
#30187=ORIENTED_EDGE('',*,*,#20904,.F.);
#30188=ORIENTED_EDGE('',*,*,#20901,.F.);
#30189=ORIENTED_EDGE('',*,*,#20900,.F.);
#30190=ORIENTED_EDGE('',*,*,#20897,.F.);
#30191=ORIENTED_EDGE('',*,*,#20951,.T.);
#30192=ORIENTED_EDGE('',*,*,#20952,.T.);
#30193=ORIENTED_EDGE('',*,*,#20949,.T.);
#30194=ORIENTED_EDGE('',*,*,#20940,.T.);
#30195=ORIENTED_EDGE('',*,*,#20944,.T.);
#30196=ORIENTED_EDGE('',*,*,#20946,.T.);
#30197=ORIENTED_EDGE('',*,*,#20952,.F.);
#30198=ORIENTED_EDGE('',*,*,#20953,.F.);
#30199=ORIENTED_EDGE('',*,*,#20951,.F.);
#30200=ORIENTED_EDGE('',*,*,#20954,.F.);
#30201=ORIENTED_EDGE('',*,*,#20955,.F.);
#30202=ORIENTED_EDGE('',*,*,#20956,.F.);
#30203=ORIENTED_EDGE('',*,*,#20957,.F.);
#30204=ORIENTED_EDGE('',*,*,#20958,.F.);
#30205=ORIENTED_EDGE('',*,*,#20959,.F.);
#30206=ORIENTED_EDGE('',*,*,#20957,.T.);
#30207=ORIENTED_EDGE('',*,*,#20960,.F.);
#30208=ORIENTED_EDGE('',*,*,#20961,.F.);
#30209=ORIENTED_EDGE('',*,*,#20962,.F.);
#30210=ORIENTED_EDGE('',*,*,#20963,.F.);
#30211=ORIENTED_EDGE('',*,*,#20964,.F.);
#30212=ORIENTED_EDGE('',*,*,#20965,.F.);
#30213=ORIENTED_EDGE('',*,*,#20966,.F.);
#30214=ORIENTED_EDGE('',*,*,#20967,.F.);
#30215=ORIENTED_EDGE('',*,*,#20968,.F.);
#30216=ORIENTED_EDGE('',*,*,#20955,.T.);
#30217=ORIENTED_EDGE('',*,*,#20954,.T.);
#30218=ORIENTED_EDGE('',*,*,#20969,.T.);
#30219=ORIENTED_EDGE('',*,*,#20953,.T.);
#30220=ORIENTED_EDGE('',*,*,#20969,.F.);
#30221=ORIENTED_EDGE('',*,*,#20958,.T.);
#30222=ORIENTED_EDGE('',*,*,#20959,.T.);
#30223=ORIENTED_EDGE('',*,*,#20970,.F.);
#30224=ORIENTED_EDGE('',*,*,#20960,.T.);
#30225=ORIENTED_EDGE('',*,*,#20956,.T.);
#30226=ORIENTED_EDGE('',*,*,#20968,.T.);
#30227=ORIENTED_EDGE('',*,*,#20971,.F.);
#30228=ORIENTED_EDGE('',*,*,#20964,.T.);
#30229=ORIENTED_EDGE('',*,*,#20962,.T.);
#30230=ORIENTED_EDGE('',*,*,#20972,.T.);
#30231=ORIENTED_EDGE('',*,*,#20966,.T.);
#30232=ORIENTED_EDGE('',*,*,#20973,.T.);
#30233=ORIENTED_EDGE('',*,*,#20963,.T.);
#30234=ORIENTED_EDGE('',*,*,#20972,.F.);
#30235=ORIENTED_EDGE('',*,*,#20961,.T.);
#30236=ORIENTED_EDGE('',*,*,#20970,.T.);
#30237=ORIENTED_EDGE('',*,*,#20974,.F.);
#30238=ORIENTED_EDGE('',*,*,#20974,.T.);
#30239=ORIENTED_EDGE('',*,*,#20975,.T.);
#30240=ORIENTED_EDGE('',*,*,#20945,.T.);
#30241=ORIENTED_EDGE('',*,*,#20862,.F.);
#30242=ORIENTED_EDGE('',*,*,#20950,.T.);
#30243=ORIENTED_EDGE('',*,*,#20896,.T.);
#30244=ORIENTED_EDGE('',*,*,#20942,.T.);
#30245=ORIENTED_EDGE('',*,*,#20975,.F.);
#30246=ORIENTED_EDGE('',*,*,#20965,.T.);
#30247=ORIENTED_EDGE('',*,*,#20971,.T.);
#30248=ORIENTED_EDGE('',*,*,#20967,.T.);
#30249=ORIENTED_EDGE('',*,*,#20973,.F.);
#30318=CONICAL_SURFACE('',#34198,1.7,0.785398163397451);
#30319=CONICAL_SURFACE('',#34201,0.825,0.785398163397448);
#30320=CONICAL_SURFACE('',#34202,1.7,0.785398163397451);
#32037=ADVANCED_FACE('',(#5062),#1992,.T.);
#32038=ADVANCED_FACE('',(#5063),#1993,.T.);
#32039=ADVANCED_FACE('',(#5064),#1994,.T.);
#32040=ADVANCED_FACE('',(#5065),#1995,.T.);
#32041=ADVANCED_FACE('',(#5066),#1996,.T.);
#32042=ADVANCED_FACE('',(#5067),#1997,.T.);
#32043=ADVANCED_FACE('',(#5068),#1998,.T.);
#32044=ADVANCED_FACE('',(#5069),#1999,.T.);
#32045=ADVANCED_FACE('',(#5070),#2000,.T.);
#32046=ADVANCED_FACE('',(#5071),#2001,.T.);
#32047=ADVANCED_FACE('',(#5072),#2002,.T.);
#32048=ADVANCED_FACE('',(#5073),#2003,.T.);
#32049=ADVANCED_FACE('',(#5074),#2004,.T.);
#32050=ADVANCED_FACE('',(#5075),#2005,.T.);
#32051=ADVANCED_FACE('',(#5076),#2006,.T.);
#32052=ADVANCED_FACE('',(#5077),#2007,.T.);
#32053=ADVANCED_FACE('',(#5078),#2008,.T.);
#32054=ADVANCED_FACE('',(#5079),#2009,.T.);
#32055=ADVANCED_FACE('',(#5080),#2010,.T.);
#32056=ADVANCED_FACE('',(#5081),#2011,.T.);
#32057=ADVANCED_FACE('',(#5082),#2012,.T.);
#32058=ADVANCED_FACE('',(#5083),#2013,.T.);
#32059=ADVANCED_FACE('',(#5084),#2014,.T.);
#32060=ADVANCED_FACE('',(#5085),#615,.F.);
#32061=ADVANCED_FACE('',(#5086),#3338,.F.);
#32062=ADVANCED_FACE('',(#5087),#616,.F.);
#32063=ADVANCED_FACE('',(#5088),#99,.F.);
#32064=ADVANCED_FACE('',(#5089,#2231),#3339,.T.);
#32065=ADVANCED_FACE('',(#5090),#3340,.F.);
#32066=ADVANCED_FACE('',(#5091),#3341,.F.);
#32067=ADVANCED_FACE('',(#5092),#3342,.F.);
#32068=ADVANCED_FACE('',(#5093),#2015,.T.);
#32069=ADVANCED_FACE('',(#5094),#3343,.T.);
#32070=ADVANCED_FACE('',(#5095),#3344,.T.);
#32071=ADVANCED_FACE('',(#5096),#30318,.T.);
#32072=ADVANCED_FACE('',(#5097),#3345,.T.);
#32073=ADVANCED_FACE('',(#5098),#30319,.F.);
#32074=ADVANCED_FACE('',(#5099),#30320,.T.);
#32087=CLOSED_SHELL('',(#32037,#32038,#32039,#32040,#32041,#32042,#32043,
#32044,#32045,#32046,#32047,#32048,#32049,#32050,#32051,#32052,#32053,#32054,
#32055,#32056,#32057,#32058,#32059,#32060,#32061,#32062,#32063,#32064,#32065,
#32066,#32067,#32068,#32069,#32070,#32071,#32072,#32073,#32074));
#34149=AXIS2_PLACEMENT_3D('',#126905,#40864,#40865);
#34150=AXIS2_PLACEMENT_3D('',#126906,#40866,#40867);
#34151=AXIS2_PLACEMENT_3D('',#126964,#40869,#40870);
#34152=AXIS2_PLACEMENT_3D('',#126993,#40871,#40872);
#34153=AXIS2_PLACEMENT_3D('',#127366,#40874,#40875);
#34154=AXIS2_PLACEMENT_3D('',#127728,#40877,#40878);
#34155=AXIS2_PLACEMENT_3D('',#128100,#40880,#40881);
#34156=AXIS2_PLACEMENT_3D('',#128436,#40883,#40884);
#34157=AXIS2_PLACEMENT_3D('',#128792,#40886,#40887);
#34158=AXIS2_PLACEMENT_3D('',#129160,#40889,#40890);
#34159=AXIS2_PLACEMENT_3D('',#129516,#40892,#40893);
#34160=AXIS2_PLACEMENT_3D('',#129868,#40895,#40896);
#34161=AXIS2_PLACEMENT_3D('',#130208,#40898,#40899);
#34162=AXIS2_PLACEMENT_3D('',#130584,#40901,#40902);
#34163=AXIS2_PLACEMENT_3D('',#130630,#40904,#40905);
#34164=AXIS2_PLACEMENT_3D('',#130639,#40906,#40907);
#34165=AXIS2_PLACEMENT_3D('',#131004,#40909,#40910);
#34166=AXIS2_PLACEMENT_3D('',#131373,#40912,#40913);
#34167=AXIS2_PLACEMENT_3D('',#131742,#40915,#40916);
#34168=AXIS2_PLACEMENT_3D('',#132097,#40918,#40919);
#34169=AXIS2_PLACEMENT_3D('',#132461,#40921,#40922);
#34170=AXIS2_PLACEMENT_3D('',#132840,#40924,#40925);
#34171=AXIS2_PLACEMENT_3D('',#133213,#40927,#40928);
#34172=AXIS2_PLACEMENT_3D('',#133576,#40930,#40931);
#34173=AXIS2_PLACEMENT_3D('',#133944,#40933,#40934);
#34174=AXIS2_PLACEMENT_3D('',#134130,#40935,#40936);
#34175=AXIS2_PLACEMENT_3D('',#134288,#40937,#40938);
#34176=AXIS2_PLACEMENT_3D('',#134349,#40939,#40940);
#34177=AXIS2_PLACEMENT_3D('',#134794,#40941,#40942);
#34178=AXIS2_PLACEMENT_3D('',#134796,#40943,#40944);
#34179=AXIS2_PLACEMENT_3D('',#134878,#40945,#40946);
#34180=AXIS2_PLACEMENT_3D('',#135171,#40947,#40948);
#34181=AXIS2_PLACEMENT_3D('',#135173,#40949,#40950);
#34182=AXIS2_PLACEMENT_3D('',#135174,#40951,#40952);
#34183=AXIS2_PLACEMENT_3D('',#135175,#40953,#40954);
#34184=AXIS2_PLACEMENT_3D('',#135177,#40955,#40956);
#34185=AXIS2_PLACEMENT_3D('',#135178,#40957,#40958);
#34186=AXIS2_PLACEMENT_3D('',#135181,#40959,#40960);
#34187=AXIS2_PLACEMENT_3D('',#135185,#40962,#40963);
#34188=AXIS2_PLACEMENT_3D('',#135188,#40965,#40966);
#34189=AXIS2_PLACEMENT_3D('',#135189,#40967,#40968);
#34190=AXIS2_PLACEMENT_3D('',#135203,#40972,#40973);
#34191=AXIS2_PLACEMENT_3D('',#135217,#40977,#40978);
#34192=AXIS2_PLACEMENT_3D('',#135219,#40980,#40981);
#34193=AXIS2_PLACEMENT_3D('',#135220,#40982,#40983);
#34194=AXIS2_PLACEMENT_3D('',#135221,#40984,#40985);
#34195=AXIS2_PLACEMENT_3D('',#135222,#40986,#40987);
#34196=AXIS2_PLACEMENT_3D('',#135223,#40988,#40989);
#34197=AXIS2_PLACEMENT_3D('',#135224,#40990,#40991);
#34198=AXIS2_PLACEMENT_3D('',#135225,#40992,#40993);
#34199=AXIS2_PLACEMENT_3D('',#135226,#40994,#40995);
#34200=AXIS2_PLACEMENT_3D('',#135228,#40996,#40997);
#34201=AXIS2_PLACEMENT_3D('',#135229,#40998,#40999);
#34202=AXIS2_PLACEMENT_3D('',#135231,#41001,#41002);
#40864=DIRECTION('axis',(0.,0.,1.));
#40865=DIRECTION('refdir',(1.,0.,0.));
#40866=DIRECTION('center_axis',(1.,0.,0.));
#40867=DIRECTION('ref_axis',(0.,1.,0.));
#40868=DIRECTION('',(-1.,0.,0.));
#40869=DIRECTION('center_axis',(1.,0.,0.));
#40870=DIRECTION('ref_axis',(0.,1.,0.));
#40871=DIRECTION('center_axis',(1.,0.,0.));
#40872=DIRECTION('ref_axis',(0.,1.,0.));
#40873=DIRECTION('',(-1.,0.,0.));
#40874=DIRECTION('center_axis',(1.,0.,0.));
#40875=DIRECTION('ref_axis',(0.,1.,0.));
#40876=DIRECTION('',(-1.,0.,0.));
#40877=DIRECTION('center_axis',(1.,0.,0.));
#40878=DIRECTION('ref_axis',(0.,1.,0.));
#40879=DIRECTION('',(-1.,0.,0.));
#40880=DIRECTION('center_axis',(1.,0.,0.));
#40881=DIRECTION('ref_axis',(0.,1.,0.));
#40882=DIRECTION('',(-1.,0.,0.));
#40883=DIRECTION('center_axis',(1.,0.,0.));
#40884=DIRECTION('ref_axis',(0.,1.,0.));
#40885=DIRECTION('',(-1.,0.,0.));
#40886=DIRECTION('center_axis',(1.,0.,0.));
#40887=DIRECTION('ref_axis',(0.,1.,0.));
#40888=DIRECTION('',(-1.,0.,0.));
#40889=DIRECTION('center_axis',(1.,0.,0.));
#40890=DIRECTION('ref_axis',(0.,1.,0.));
#40891=DIRECTION('',(-1.,0.,0.));
#40892=DIRECTION('center_axis',(1.,0.,0.));
#40893=DIRECTION('ref_axis',(0.,1.,0.));
#40894=DIRECTION('',(-1.,0.,0.));
#40895=DIRECTION('center_axis',(1.,0.,0.));
#40896=DIRECTION('ref_axis',(0.,1.,0.));
#40897=DIRECTION('',(-1.,0.,0.));
#40898=DIRECTION('center_axis',(1.,0.,0.));
#40899=DIRECTION('ref_axis',(0.,1.,0.));
#40900=DIRECTION('',(-1.,0.,0.));
#40901=DIRECTION('center_axis',(1.,0.,0.));
#40902=DIRECTION('ref_axis',(0.,0.941532254165013,-0.336922861152149));
#40903=DIRECTION('',(-1.,0.,0.));
#40904=DIRECTION('center_axis',(-1.,0.,0.));
#40905=DIRECTION('ref_axis',(0.,1.,6.6102588746288E-14));
#40906=DIRECTION('center_axis',(1.,0.,0.));
#40907=DIRECTION('ref_axis',(0.,0.941532254165013,-0.336922861152149));
#40908=DIRECTION('',(-1.,0.,0.));
#40909=DIRECTION('center_axis',(1.,0.,0.));
#40910=DIRECTION('ref_axis',(0.,0.941532254165013,-0.336922861152149));
#40911=DIRECTION('',(-1.,0.,0.));
#40912=DIRECTION('center_axis',(1.,0.,0.));
#40913=DIRECTION('ref_axis',(0.,0.941532254165013,-0.336922861152149));
#40914=DIRECTION('',(-1.,0.,0.));
#40915=DIRECTION('center_axis',(1.,0.,0.));
#40916=DIRECTION('ref_axis',(0.,0.941532254165013,-0.336922861152149));
#40917=DIRECTION('',(-1.,0.,0.));
#40918=DIRECTION('center_axis',(1.,0.,0.));
#40919=DIRECTION('ref_axis',(0.,0.941532254165013,-0.336922861152149));
#40920=DIRECTION('',(-1.,0.,0.));
#40921=DIRECTION('center_axis',(1.,0.,0.));
#40922=DIRECTION('ref_axis',(0.,0.941532254165013,-0.336922861152149));
#40923=DIRECTION('',(-1.,0.,0.));
#40924=DIRECTION('center_axis',(1.,0.,0.));
#40925=DIRECTION('ref_axis',(0.,0.941532254165013,-0.336922861152149));
#40926=DIRECTION('',(-1.,0.,0.));
#40927=DIRECTION('center_axis',(1.,0.,0.));
#40928=DIRECTION('ref_axis',(0.,0.941532254165013,-0.336922861152149));
#40929=DIRECTION('',(-1.,0.,0.));
#40930=DIRECTION('center_axis',(1.,0.,0.));
#40931=DIRECTION('ref_axis',(0.,0.941532254165013,-0.336922861152149));
#40932=DIRECTION('',(-1.,0.,0.));
#40933=DIRECTION('center_axis',(1.,0.,0.));
#40934=DIRECTION('ref_axis',(0.,0.941532254165013,-0.336922861152149));
#40935=DIRECTION('center_axis',(1.,0.,0.));
#40936=DIRECTION('ref_axis',(0.,1.,6.6102588746288E-14));
#40937=DIRECTION('center_axis',(1.,0.,0.));
#40938=DIRECTION('ref_axis',(0.,1.,0.));
#40939=DIRECTION('center_axis',(1.,0.,0.));
#40940=DIRECTION('ref_axis',(0.,1.,0.));
#40941=DIRECTION('center_axis',(1.,0.,0.));
#40942=DIRECTION('ref_axis',(0.,0.,-1.));
#40943=DIRECTION('center_axis',(1.,0.,0.));
#40944=DIRECTION('ref_axis',(0.,1.,0.));
#40945=DIRECTION('center_axis',(1.,0.,0.));
#40946=DIRECTION('ref_axis',(0.,1.,0.));
#40947=DIRECTION('center_axis',(1.,0.,0.));
#40948=DIRECTION('ref_axis',(0.,0.,-1.));
#40949=DIRECTION('center_axis',(-1.,0.,0.));
#40950=DIRECTION('ref_axis',(0.,1.,0.));
#40951=DIRECTION('center_axis',(0.,1.,0.));
#40952=DIRECTION('ref_axis',(0.,0.,1.));
#40953=DIRECTION('center_axis',(-1.,0.,0.));
#40954=DIRECTION('ref_axis',(0.,0.,1.));
#40955=DIRECTION('center_axis',(1.,0.,0.));
#40956=DIRECTION('ref_axis',(0.,0.,-1.));
#40957=DIRECTION('center_axis',(-1.,0.,0.));
#40958=DIRECTION('ref_axis',(0.,0.,1.));
#40959=DIRECTION('center_axis',(-1.,0.,0.));
#40960=DIRECTION('ref_axis',(0.,1.,0.));
#40961=DIRECTION('',(0.,-1.,0.));
#40962=DIRECTION('center_axis',(-1.,0.,0.));
#40963=DIRECTION('ref_axis',(0.,1.,0.));
#40964=DIRECTION('',(0.,1.,0.));
#40965=DIRECTION('center_axis',(-1.,0.,0.));
#40966=DIRECTION('ref_axis',(0.,1.,0.));
#40967=DIRECTION('center_axis',(0.,0.,1.));
#40968=DIRECTION('ref_axis',(0.,1.,0.));
#40969=DIRECTION('',(1.,0.,0.));
#40970=DIRECTION('',(-1.,0.,0.));
#40971=DIRECTION('',(0.,1.,0.));
#40972=DIRECTION('center_axis',(0.,0.,-1.));
#40973=DIRECTION('ref_axis',(0.,-1.,0.));
#40974=DIRECTION('',(-1.,0.,0.));
#40975=DIRECTION('',(0.,-1.,0.));
#40976=DIRECTION('',(1.,0.,0.));
#40977=DIRECTION('center_axis',(1.,0.,0.));
#40978=DIRECTION('ref_axis',(0.,1.,0.));
#40979=DIRECTION('',(-1.,0.,0.));
#40980=DIRECTION('center_axis',(1.,0.,0.));
#40981=DIRECTION('ref_axis',(0.,0.,-1.));
#40982=DIRECTION('center_axis',(1.,0.,0.));
#40983=DIRECTION('ref_axis',(0.,0.,-1.));
#40984=DIRECTION('center_axis',(1.,0.,0.));
#40985=DIRECTION('ref_axis',(0.,0.,-1.));
#40986=DIRECTION('center_axis',(1.,0.,0.));
#40987=DIRECTION('ref_axis',(0.,0.,-1.));
#40988=DIRECTION('center_axis',(1.,0.,0.));
#40989=DIRECTION('ref_axis',(0.,0.,-1.));
#40990=DIRECTION('center_axis',(1.,0.,0.));
#40991=DIRECTION('ref_axis',(0.,0.,-1.));
#40992=DIRECTION('center_axis',(-1.,0.,0.));
#40993=DIRECTION('ref_axis',(0.,1.,0.));
#40994=DIRECTION('center_axis',(-1.,0.,0.));
#40995=DIRECTION('ref_axis',(0.,0.,1.));
#40996=DIRECTION('center_axis',(1.,0.,0.));
#40997=DIRECTION('ref_axis',(0.,0.,-1.));
#40998=DIRECTION('center_axis',(-1.,0.,0.));
#40999=DIRECTION('ref_axis',(0.,1.,0.));
#41000=DIRECTION('',(-0.707106781186548,-0.707106781186547,8.65956056235493E-17));
#41001=DIRECTION('center_axis',(-1.,0.,0.));
#41002=DIRECTION('ref_axis',(0.,1.,0.));
#126905=CARTESIAN_POINT('',(0.,0.,0.));
#126906=CARTESIAN_POINT('Origin',(16.125,15.,5.5));
#126907=CARTESIAN_POINT('',(14.1122359168897,14.0332500271131,5.50022896121196));
#126908=CARTESIAN_POINT('',(14.0542640831103,14.0332504905991,5.50097394714278));
#126909=CARTESIAN_POINT('',(16.125,14.03325,5.5));
#126910=CARTESIAN_POINT('',(13.98325,15.4251191285151,6.36826222368048));
#126911=CARTESIAN_POINT('Ctrl Pts',(14.1122359168897,14.0332500271131,5.50022896121196));
#126912=CARTESIAN_POINT('Ctrl Pts',(14.1111983227026,14.0332537377696,5.51589658043436));
#126913=CARTESIAN_POINT('Ctrl Pts',(14.1101607285155,14.0336383013732,5.53155887807419));
#126914=CARTESIAN_POINT('Ctrl Pts',(14.1091231343284,14.0344030805415,5.54720330107296));
#126915=CARTESIAN_POINT('Ctrl Pts',(14.1064784426769,14.0363524024504,5.58707888577847));
#126916=CARTESIAN_POINT('Ctrl Pts',(14.1038337510254,14.0407811038833,5.62693592160445));
#126917=CARTESIAN_POINT('Ctrl Pts',(14.1011890593739,14.0476849049741,5.66643774297254));
#126918=CARTESIAN_POINT('Ctrl Pts',(14.0985483650438,14.0545782713088,5.7058798592786));
#126919=CARTESIAN_POINT('Ctrl Pts',(14.0959076707138,14.0639392494708,5.74496723770123));
#126920=CARTESIAN_POINT('Ctrl Pts',(14.0932669763837,14.0757117090939,5.78336675492011));
#126921=CARTESIAN_POINT('Ctrl Pts',(14.0906289292766,14.0874723671522,5.82172777768616));
#126922=CARTESIAN_POINT('Ctrl Pts',(14.0879908821695,14.1016395563674,5.85940173231856));
#126923=CARTESIAN_POINT('Ctrl Pts',(14.0853528350624,14.1181064745837,5.89606738357096));
#126924=CARTESIAN_POINT('Ctrl Pts',(14.0827160901279,14.1345652645259,5.93271493620557));
#126925=CARTESIAN_POINT('Ctrl Pts',(14.0800793451934,14.1533212931685,5.96835462533446));
#126926=CARTESIAN_POINT('Ctrl Pts',(14.0774426002589,14.1742196360123,6.00268514295958));
#126927=CARTESIAN_POINT('Ctrl Pts',(14.0748035134053,14.1951365404644,6.03704615245806));
#126928=CARTESIAN_POINT('Ctrl Pts',(14.0721644265518,14.2181992557027,6.07009515110953));
#126929=CARTESIAN_POINT('Ctrl Pts',(14.0695253396983,14.2432080435773,6.10155755933573));
#126930=CARTESIAN_POINT('Ctrl Pts',(14.0668852468224,14.2682263648249,6.13303196106091));
#126931=CARTESIAN_POINT('Ctrl Pts',(14.0642451539465,14.2951918386584,6.16291811904539));
#126932=CARTESIAN_POINT('Ctrl Pts',(14.0616050610706,14.3238654659778,6.19097587107123));
#126933=CARTESIAN_POINT('Ctrl Pts',(14.0589588945366,14.3526050583283,6.21909817127799));
#126934=CARTESIAN_POINT('Ctrl Pts',(14.0563127280027,14.3830602017073,6.24538326799888));
#126935=CARTESIAN_POINT('Ctrl Pts',(14.0536665614687,14.4149576099238,6.26963040760742));
#126936=CARTESIAN_POINT('Ctrl Pts',(14.0511732300339,14.4450127140055,6.29247710097102));
#126937=CARTESIAN_POINT('Ctrl Pts',(14.048679898599,14.4763476453378,6.31351461671014));
#126938=CARTESIAN_POINT('Ctrl Pts',(14.0461865671642,14.5087133853044,6.3326121694528));
#126939=CARTESIAN_POINT('Ctrl Pts',(14.0434435871445,14.5443197939875,6.3536218935779));
#126940=CARTESIAN_POINT('Ctrl Pts',(14.0407006071248,14.5813433744591,6.3723835458022));
#126941=CARTESIAN_POINT('Ctrl Pts',(14.0379576271051,14.6194779862857,6.38871174155561));
#126942=CARTESIAN_POINT('Ctrl Pts',(14.0352193759872,14.6575468539824,6.40501178747424));
#126943=CARTESIAN_POINT('Ctrl Pts',(14.0324811248693,14.6967224595233,6.41888647636587));
#126944=CARTESIAN_POINT('Ctrl Pts',(14.0297428737515,14.7366742891112,6.43019628707327));
#126945=CARTESIAN_POINT('Ctrl Pts',(14.0270082901897,14.7765726080571,6.4414909496576));
#126946=CARTESIAN_POINT('Ctrl Pts',(14.0242737066278,14.8172445670197,6.4502273957799));
#126947=CARTESIAN_POINT('Ctrl Pts',(14.021539123066,14.8583423608962,6.45631515505274));
#126948=CARTESIAN_POINT('Ctrl Pts',(14.0188071523524,14.8994008865283,6.46239709757493));
#126949=CARTESIAN_POINT('Ctrl Pts',(14.0160751816388,14.9408839010166,6.46583529299521));
#126950=CARTESIAN_POINT('Ctrl Pts',(14.0133432109251,14.9824337948278,6.46659039460148));
#126951=CARTESIAN_POINT('Ctrl Pts',(14.0106119531324,15.0239728459946,6.46734529916036));
#126952=CARTESIAN_POINT('Ctrl Pts',(14.0078806953396,15.065578196097,6.46541847609278));
#126953=CARTESIAN_POINT('Ctrl Pts',(14.0051494375469,15.1068898107475,6.46082263236164));
#126954=CARTESIAN_POINT('Ctrl Pts',(14.0024188047339,15.148191972273,6.45622784027387));
#126955=CARTESIAN_POINT('Ctrl Pts',(13.9996881719209,15.1891999892098,6.44896530702385));
#126956=CARTESIAN_POINT('Ctrl Pts',(13.9969575391078,15.2295595518161,6.43909955524959));
#126957=CARTESIAN_POINT('Ctrl Pts',(13.9942248485379,15.26994952868,6.42922636881807));
#126958=CARTESIAN_POINT('Ctrl Pts',(13.9914921579679,15.309689544406,6.41674617983749));
#126959=CARTESIAN_POINT('Ctrl Pts',(13.988759467398,15.3484380403758,6.40177408175168));
#126960=CARTESIAN_POINT('Ctrl Pts',(13.9869229782653,15.3744787463884,6.39171216851125));
#126961=CARTESIAN_POINT('Ctrl Pts',(13.9850864891327,15.4000719306852,6.38052584937186));
#126962=CARTESIAN_POINT('Ctrl Pts',(13.98325,15.4251191285151,6.36826222368047));
#126963=CARTESIAN_POINT('',(13.98325,14.5748808714849,6.36826222368045));
#126964=CARTESIAN_POINT('Origin',(13.98325,15.,5.5));
#126965=CARTESIAN_POINT('Ctrl Pts',(13.98325,14.5748808714849,6.36826222368047));
#126966=CARTESIAN_POINT('Ctrl Pts',(13.9859825949665,14.5376120167465,6.35001462218978));
#126967=CARTESIAN_POINT('Ctrl Pts',(13.9887151899329,14.5014867905651,6.32934731978482));
#126968=CARTESIAN_POINT('Ctrl Pts',(13.9914477848994,14.466822900776,6.30642900701992));
#126969=CARTESIAN_POINT('Ctrl Pts',(13.9941787447248,14.4321797533039,6.28352440820663));
#126970=CARTESIAN_POINT('Ctrl Pts',(13.9969097045501,14.3989966643142,6.25837177022466));
#126971=CARTESIAN_POINT('Ctrl Pts',(13.9996406643755,14.3675639083938,6.23118407568403));
#126972=CARTESIAN_POINT('Ctrl Pts',(14.002371037551,14.3361379046864,6.2040022214554));
#126973=CARTESIAN_POINT('Ctrl Pts',(14.0051014107265,14.3064619012838,6.17478653584945));
#126974=CARTESIAN_POINT('Ctrl Pts',(14.0078317839019,14.2787924412534,6.14378973252666));
#126975=CARTESIAN_POINT('Ctrl Pts',(14.0105626175321,14.2511183149989,6.11278770185105));
#126976=CARTESIAN_POINT('Ctrl Pts',(14.0132934511623,14.2254517655684,6.0800043671736));
#126977=CARTESIAN_POINT('Ctrl Pts',(14.0160242847925,14.2020100731701,6.04572670740766));
#126978=CARTESIAN_POINT('Ctrl Pts',(14.0187591076052,14.1785341373134,6.01139897507887));
#126979=CARTESIAN_POINT('Ctrl Pts',(14.0214939304178,14.1572898554751,5.9755730130028));
#126980=CARTESIAN_POINT('Ctrl Pts',(14.0242287532304,14.1384510620468,5.93856469307472));
#126981=CARTESIAN_POINT('Ctrl Pts',(14.0269655875177,14.1195984126002,5.90152915335883));
#126982=CARTESIAN_POINT('Ctrl Pts',(14.029702421805,14.1031549952832,5.86331002558253));
#126983=CARTESIAN_POINT('Ctrl Pts',(14.0324392560923,14.0892468712491,5.82424419959424));
#126984=CARTESIAN_POINT('Ctrl Pts',(14.035182303232,14.075307174561,5.78508969077501));
#126985=CARTESIAN_POINT('Ctrl Pts',(14.0379253503717,14.0639144231692,5.74508517045302));
#126986=CARTESIAN_POINT('Ctrl Pts',(14.0406683975114,14.0551446589734,5.70458237224525));
#126987=CARTESIAN_POINT('Ctrl Pts',(14.0425349293738,14.0491771916046,5.67702186762344));
#126988=CARTESIAN_POINT('Ctrl Pts',(14.0444014612362,14.0444231647546,5.64923090555547));
#126989=CARTESIAN_POINT('Ctrl Pts',(14.0462679930987,14.0408928035711,5.62132167266533));
#126990=CARTESIAN_POINT('Ctrl Pts',(14.0489333564359,14.0358515313298,5.58146794843325));
#126991=CARTESIAN_POINT('Ctrl Pts',(14.0515987197731,14.0332910885869,5.54127190906272));
#126992=CARTESIAN_POINT('Ctrl Pts',(14.0542640831103,14.0332504905991,5.50097394714278));
#126993=CARTESIAN_POINT('Origin',(16.125,15.,5.5));
#126994=CARTESIAN_POINT('',(14.5114930218304,14.0332500860612,5.50040792073653));
#126995=CARTESIAN_POINT('',(14.4551338463882,14.0332500192795,5.50019307213798));
#126996=CARTESIAN_POINT('',(16.125,14.03325,5.5));
#126997=CARTESIAN_POINT('Ctrl Pts',(14.5116785698828,14.0335723061034,5.50041943332155));
#126998=CARTESIAN_POINT('Ctrl Pts',(14.5088403565566,14.033538001356,5.54511906159122));
#126999=CARTESIAN_POINT('Ctrl Pts',(14.5060695122599,14.0365700498625,5.58972837050457));
#127000=CARTESIAN_POINT('Ctrl Pts',(14.5033211490731,14.0426309602475,5.63384343118924));
#127001=CARTESIAN_POINT('Ctrl Pts',(14.5007334695076,14.0483375182553,5.67537929574192));
#127002=CARTESIAN_POINT('Ctrl Pts',(14.4981651521549,14.0567300004624,5.71647784890844));
#127003=CARTESIAN_POINT('Ctrl Pts',(14.4955573715337,14.0677447980235,5.75679634653785));
#127004=CARTESIAN_POINT('Ctrl Pts',(14.4953774892451,14.0685045885435,5.75957747911091));
#127005=CARTESIAN_POINT('Ctrl Pts',(14.4951974191857,14.0692768613978,5.76235492004761));
#127006=CARTESIAN_POINT('Ctrl Pts',(14.4950171420486,14.0700615983275,5.76512856562658));
#127007=CARTESIAN_POINT('Ctrl Pts',(14.4925397852085,14.0808454028149,5.80324382503531));
#127008=CARTESIAN_POINT('Ctrl Pts',(14.490022367042,14.0939818279592,5.84063784347691));
#127009=CARTESIAN_POINT('Ctrl Pts',(14.4874062601009,14.1093818608135,5.87701664459744));
#127010=CARTESIAN_POINT('Ctrl Pts',(14.4874052936255,14.1093875500886,5.87703008411471));
#127011=CARTESIAN_POINT('Ctrl Pts',(14.4874043271367,14.1093932396726,5.87704352349411));
#127012=CARTESIAN_POINT('Ctrl Pts',(14.4874033606344,14.1093989295655,5.87705696273564));
#127013=CARTESIAN_POINT('Ctrl Pts',(14.4849361871077,14.1239234199081,5.91136308009952));
#127014=CARTESIAN_POINT('Ctrl Pts',(14.4823758020564,14.1405099798208,5.94487254352574));
#127015=CARTESIAN_POINT('Ctrl Pts',(14.4797777976776,14.1590269386098,5.97734260524887));
#127016=CARTESIAN_POINT('Ctrl Pts',(14.47956279882,14.1605593166989,5.98002967776994));
#127017=CARTESIAN_POINT('Ctrl Pts',(14.4793475423282,14.1621048891765,5.98270961773312));
#127018=CARTESIAN_POINT('Ctrl Pts',(14.4791320597088,14.1636635672483,5.98538228026991));
#127019=CARTESIAN_POINT('Ctrl Pts',(14.4763169539401,14.1840264329138,6.02029845006232));
#127020=CARTESIAN_POINT('Ctrl Pts',(14.4734638889733,14.2066307295246,6.05397573758949));
#127021=CARTESIAN_POINT('Ctrl Pts',(14.470628262562,14.2312768890253,6.08613865119781));
#127022=CARTESIAN_POINT('Ctrl Pts',(14.4677955122579,14.2558980505222,6.1182689427404));
#127023=CARTESIAN_POINT('Ctrl Pts',(14.4649804629347,14.2825567348882,6.14888817681659));
#127024=CARTESIAN_POINT('Ctrl Pts',(14.4622166564524,14.3110285961508,6.17774935316013));
#127025=CARTESIAN_POINT('Ctrl Pts',(14.4594543129969,14.3394853857735,6.206595251779));
#127026=CARTESIAN_POINT('Ctrl Pts',(14.4567432386662,14.3697533971121,6.23368500019935));
#127027=CARTESIAN_POINT('Ctrl Pts',(14.4540924994083,14.4015849102876,6.2587974481407));
#127028=CARTESIAN_POINT('Ctrl Pts',(14.4514398306896,14.4334395934721,6.28392817531496));
#127029=CARTESIAN_POINT('Ctrl Pts',(14.4488475087101,14.4668601036537,6.30707858920841));
#127030=CARTESIAN_POINT('Ctrl Pts',(14.4463001328731,14.5015742709219,6.32805323402867));
#127031=CARTESIAN_POINT('Ctrl Pts',(14.4437519600193,14.5362992994732,6.34903444134405));
#127032=CARTESIAN_POINT('Ctrl Pts',(14.4412485066232,14.5723188931445,6.36783820572832));
#127033=CARTESIAN_POINT('Ctrl Pts',(14.4387523046875,14.6093355894634,6.38429837617079));
#127034=CARTESIAN_POINT('Ctrl Pts',(14.4362510339094,14.6464274526973,6.40079197099611));
#127035=CARTESIAN_POINT('Ctrl Pts',(14.4337565422159,14.6845205677269,6.41493187379764));
#127036=CARTESIAN_POINT('Ctrl Pts',(14.4312145763807,14.723288942022,6.42658707969176));
#127037=CARTESIAN_POINT('Ctrl Pts',(14.4290152593111,14.7568314649641,6.43667120156187));
#127038=CARTESIAN_POINT('Ctrl Pts',(14.4267797932423,14.7908789865304,6.44489554530127));
#127039=CARTESIAN_POINT('Ctrl Pts',(14.424468769591,14.8252041506766,6.45120324226616));
#127040=CARTESIAN_POINT('Ctrl Pts',(14.4244678046359,14.8252184829579,6.45120587600994));
#127041=CARTESIAN_POINT('Ctrl Pts',(14.4244668396677,14.8252328152881,6.45120850942005));
#127042=CARTESIAN_POINT('Ctrl Pts',(14.4244658746863,14.8252471476672,6.45121114249652));
#127043=CARTESIAN_POINT('Ctrl Pts',(14.4219984901291,14.861893957556,6.45794372000282));
#127044=CARTESIAN_POINT('Ctrl Pts',(14.4194378465614,14.8990090466855,6.46251513142114));
#127045=CARTESIAN_POINT('Ctrl Pts',(14.4168395113487,14.9363172191443,6.46490193969772));
#127046=CARTESIAN_POINT('Ctrl Pts',(14.4166239691842,14.9394120793466,6.46509993486765));
#127047=CARTESIAN_POINT('Ctrl Pts',(14.4164081676501,14.9425082419749,6.46528291083921));
#127048=CARTESIAN_POINT('Ctrl Pts',(14.4161921384662,14.9456055359566,6.4654508621258));
#127049=CARTESIAN_POINT('Ctrl Pts',(14.413376132906,14.9859796970517,6.4676401577952));
#127050=CARTESIAN_POINT('Ctrl Pts',(14.4105220809119,15.0265513156988,6.46727432489245));
#127051=CARTESIAN_POINT('Ctrl Pts',(14.4076853995713,15.0669803348007,6.46436865337555));
#127052=CARTESIAN_POINT('Ctrl Pts',(14.4048515996756,15.1073682869015,6.46146593338254));
#127053=CARTESIAN_POINT('Ctrl Pts',(14.4020354334159,15.1476140253573,6.45602883499858));
#127054=CARTESIAN_POINT('Ctrl Pts',(14.3992704634175,15.1873876882495,6.44810901078328));
#127055=CARTESIAN_POINT('Ctrl Pts',(14.3965069638831,15.227140198748,6.4401933984818));
#127056=CARTESIAN_POINT('Ctrl Pts',(14.3937946868122,15.2664211557774,6.42979775620122));
#127057=CARTESIAN_POINT('Ctrl Pts',(14.3911427161659,15.3049094453059,6.41700746938872));
#127058=CARTESIAN_POINT('Ctrl Pts',(14.3884888357345,15.3434254517178,6.40420797180351));
#127059=CARTESIAN_POINT('Ctrl Pts',(14.3858952722682,15.3811475644302,6.38901026555577));
#127060=CARTESIAN_POINT('Ctrl Pts',(14.383346641176,15.417762688279,6.37153428391848));
#127061=CARTESIAN_POINT('Ctrl Pts',(14.3807972220512,15.4543891334649,6.35405289873591));
#127062=CARTESIAN_POINT('Ctrl Pts',(14.3782925079189,15.4899076987036,6.33429157452673));
#127063=CARTESIAN_POINT('Ctrl Pts',(14.3757950489659,15.524015849635,6.31240749055365));
#127064=CARTESIAN_POINT('Ctrl Pts',(14.3732925477779,15.5581928630837,6.29047922379516));
#127065=CARTESIAN_POINT('Ctrl Pts',(14.3707968286401,15.5909533370189,6.26641922298146));
#127066=CARTESIAN_POINT('Ctrl Pts',(14.3682536676265,15.6220084037581,6.24042783540193));
#127067=CARTESIAN_POINT('Ctrl Pts',(14.366060413606,15.6487906836117,6.21801253609562));
#127068=CARTESIAN_POINT('Ctrl Pts',(14.3638312674251,15.6743044740454,6.19416128864694));
#127069=CARTESIAN_POINT('Ctrl Pts',(14.3615272302636,15.6983787715834,6.16903122376138));
#127070=CARTESIAN_POINT('Ctrl Pts',(14.3615262729411,15.6983887744026,6.16902078227308));
#127071=CARTESIAN_POINT('Ctrl Pts',(14.3615253156056,15.698398776974,6.16901034056392));
#127072=CARTESIAN_POINT('Ctrl Pts',(14.3615243582573,15.6984087792974,6.16899989863392));
#127073=CARTESIAN_POINT('Ctrl Pts',(14.3590557745127,15.724200407049,6.14207471742743));
#127074=CARTESIAN_POINT('Ctrl Pts',(14.3564941307412,15.7484423252867,6.11356820325169));
#127075=CARTESIAN_POINT('Ctrl Pts',(14.3538950518424,15.7709633825522,6.08369774166327));
#127076=CARTESIAN_POINT('Ctrl Pts',(14.3536810497184,15.7728177141348,6.08123827718705));
#127077=CARTESIAN_POINT('Ctrl Pts',(14.3534667938033,15.7746603762586,6.07876959493171));
#127078=CARTESIAN_POINT('Ctrl Pts',(14.3532523151472,15.7764912722831,6.07629183189533));
#127079=CARTESIAN_POINT('Ctrl Pts',(14.3504371854622,15.8005226134114,6.04377006770674));
#127080=CARTESIAN_POINT('Ctrl Pts',(14.3475843160472,15.8225280060186,6.00967836065559));
#127081=CARTESIAN_POINT('Ctrl Pts',(14.3447490096124,15.8423332260637,5.97430917337171));
#127082=CARTESIAN_POINT('Ctrl Pts',(14.3419165707059,15.8621184158121,5.93897575722877));
#127083=CARTESIAN_POINT('Ctrl Pts',(14.3391019560053,15.8797081859031,5.90236752879608));
#127084=CARTESIAN_POINT('Ctrl Pts',(14.3363385738576,15.8949642554464,5.86478844189219));
#127085=CARTESIAN_POINT('Ctrl Pts',(14.3335766497244,15.9102122755886,5.82722918245047));
#127086=CARTESIAN_POINT('Ctrl Pts',(14.3308659836563,15.9231291137436,5.78870010211487));
#127087=CARTESIAN_POINT('Ctrl Pts',(14.3282154840765,15.9336094584268,5.74951641888195));
#127088=CARTESIAN_POINT('Ctrl Pts',(14.3255630606859,15.9440974100534,5.7103042949754));
#127089=CARTESIAN_POINT('Ctrl Pts',(14.3229708137538,15.9521451873804,5.6704366245497));
#127090=CARTESIAN_POINT('Ctrl Pts',(14.320423176276,15.9576807446635,5.63024095734538));
#127091=CARTESIAN_POINT('Ctrl Pts',(14.3178747428045,15.9632180314978,5.59003273124878));
#127092=CARTESIAN_POINT('Ctrl Pts',(14.3153706899478,15.9662412003968,5.54949633524583));
#127093=CARTESIAN_POINT('Ctrl Pts',(14.3128733974786,15.9667151448827,5.50897101865864));
#127094=CARTESIAN_POINT('Ctrl Pts',(14.3103710528751,15.9671900481795,5.46836371754517));
#127095=CARTESIAN_POINT('Ctrl Pts',(14.3078749910923,15.9651048371898,5.42776767871473));
#127096=CARTESIAN_POINT('Ctrl Pts',(14.3053308585778,15.9604680307702,5.3875345185831));
#127097=CARTESIAN_POINT('Ctrl Pts',(14.303138146851,15.9564717059903,5.35285876112074));
#127098=CARTESIAN_POINT('Ctrl Pts',(14.3009091203456,15.9505804056575,5.31845292054379));
#127099=CARTESIAN_POINT('Ctrl Pts',(14.2986048211183,15.942831329532,5.28454592146491));
#127100=CARTESIAN_POINT('Ctrl Pts',(14.2986038416525,15.9428280357083,5.28453150894942));
#127101=CARTESIAN_POINT('Ctrl Pts',(14.298602862173,15.9428247415491,5.28451709652346));
#127102=CARTESIAN_POINT('Ctrl Pts',(14.2986018826799,15.9428214470546,5.28450268418704));
#127103=CARTESIAN_POINT('Ctrl Pts',(14.2961366610282,15.9345297506763,5.24822922312637));
#127104=CARTESIAN_POINT('Ctrl Pts',(14.2935781335832,15.924073286213,5.21237753911605));
#127105=CARTESIAN_POINT('Ctrl Pts',(14.2909818963397,15.9115388193728,5.17720913033834));
#127106=CARTESIAN_POINT('Ctrl Pts',(14.2907666596865,15.9104996706205,5.17429355294933));
#127107=CARTESIAN_POINT('Ctrl Pts',(14.2905511638554,15.9094462629078,5.17138269029546));
#127108=CARTESIAN_POINT('Ctrl Pts',(14.2903354405245,15.9083786584267,5.16847670107737));
#127109=CARTESIAN_POINT('Ctrl Pts',(14.2875218445659,15.8944543061485,5.13057500779491));
#127110=CARTESIAN_POINT('Ctrl Pts',(14.2846701831178,15.87811090771,5.09349839386361));
#127111=CARTESIAN_POINT('Ctrl Pts',(14.2818359302662,15.8594963284814,5.05755251441345));
#127112=CARTESIAN_POINT('Ctrl Pts',(14.2790045544142,15.8409006445809,5.02164312298594));
#127113=CARTESIAN_POINT('Ctrl Pts',(14.2761908500345,15.8200386295198,4.98686196663159));
#127114=CARTESIAN_POINT('Ctrl Pts',(14.2734284767015,15.7970875597742,4.95349099618714));
#127115=CARTESIAN_POINT('Ctrl Pts',(14.2706675599086,15.7741485916347,4.9201376215387));
#127116=CARTESIAN_POINT('Ctrl Pts',(14.2679580014553,15.7491228171391,4.88819290788565));
#127117=CARTESIAN_POINT('Ctrl Pts',(14.2653090168416,15.7222150559174,4.85791742985194));
#127118=CARTESIAN_POINT('Ctrl Pts',(14.2626580642003,15.695287303936,4.82761945905849));
#127119=CARTESIAN_POINT('Ctrl Pts',(14.2600677008402,15.666474700163,4.79899332828456));
#127120=CARTESIAN_POINT('Ctrl Pts',(14.2575226891931,15.6360106072016,4.77227856898802));
#127121=CARTESIAN_POINT('Ctrl Pts',(14.2549768648779,15.6055367865065,4.74555527918762));
#127122=CARTESIAN_POINT('Ctrl Pts',(14.2524761691731,15.5734102739615,4.72074487036412));
#127123=CARTESIAN_POINT('Ctrl Pts',(14.2499832776,15.5398943800745,4.69806242359263));
#127124=CARTESIAN_POINT('Ctrl Pts',(14.2474852548137,15.5063094991516,4.6753332886804));
#127125=CARTESIAN_POINT('Ctrl Pts',(14.2449945709537,15.4713293200612,4.6547414257863));
#127126=CARTESIAN_POINT('Ctrl Pts',(14.242457039379,15.4352512774438,4.63647233143748));
#127127=CARTESIAN_POINT('Ctrl Pts',(14.2402402023742,15.4037327967545,4.62051209480407));
#127128=CARTESIAN_POINT('Ctrl Pts',(14.2379869886449,15.3713769033494,4.60632454098609));
#127129=CARTESIAN_POINT('Ctrl Pts',(14.235656781393,15.3384033970721,4.59400783432258));
#127130=CARTESIAN_POINT('Ctrl Pts',(14.2356558203857,15.3383897983766,4.59400275475534));
#127131=CARTESIAN_POINT('Ctrl Pts',(14.2356548593654,15.3383761995759,4.59399767550574));
#127132=CARTESIAN_POINT('Ctrl Pts',(14.2356538983319,15.3383626006697,4.59399259657377));
#127133=CARTESIAN_POINT('Ctrl Pts',(14.2331860372601,15.3034416400178,4.5809502841007));
#127134=CARTESIAN_POINT('Ctrl Pts',(14.2306246417521,15.2676820685573,4.56995633681078));
#127135=CARTESIAN_POINT('Ctrl Pts',(14.2280251500428,15.231350777683,4.56108170256948));
#127136=CARTESIAN_POINT('Ctrl Pts',(14.2278066760094,15.2282973177971,4.56033583477878));
#127137=CARTESIAN_POINT('Ctrl Pts',(14.2275879328817,15.2252398485238,4.55960492749181));
#127138=CARTESIAN_POINT('Ctrl Pts',(14.2273689535708,15.2221785440531,4.5588890172329));
#127139=CARTESIAN_POINT('Ctrl Pts',(14.2245487183885,15.1827519948523,4.54966880692146));
#127140=CARTESIAN_POINT('Ctrl Pts',(14.2216899483003,15.1426837765983,4.54293735587022));
#127141=CARTESIAN_POINT('Ctrl Pts',(14.2188481867355,15.1023123613639,4.53873890097382));
#127142=CARTESIAN_POINT('Ctrl Pts',(14.2160093354378,15.0619822907662,4.5345447457432));
#127143=CARTESIAN_POINT('Ctrl Pts',(14.2131877587133,15.0213495988083,4.53287808223543));
#127144=CARTESIAN_POINT('Ctrl Pts',(14.2104171666861,14.9807489761677,4.53374553378922));
#127145=CARTESIAN_POINT('Ctrl Pts',(14.2076480828385,14.9401704545925,4.53461251314327));
#127146=CARTESIAN_POINT('Ctrl Pts',(14.2049300097636,14.899623953611,4.53801078983452));
#127147=CARTESIAN_POINT('Ctrl Pts',(14.2022721750058,14.859441399294,4.54391225339522));
#127148=CARTESIAN_POINT('Ctrl Pts',(14.1996125229251,14.8192313697284,4.54981775214436));
#127149=CARTESIAN_POINT('Ctrl Pts',(14.1970131149593,14.7793858445733,4.55822998985528));
#127150=CARTESIAN_POINT('Ctrl Pts',(14.1944587042042,14.7402348772394,4.56908545335078));
#127151=CARTESIAN_POINT('Ctrl Pts',(14.1919035486396,14.7010724943514,4.57994408205877));
#127152=CARTESIAN_POINT('Ctrl Pts',(14.1893931603709,14.6626052316451,4.5932476505405));
#127153=CARTESIAN_POINT('Ctrl Pts',(14.1868902327606,14.6251592912233,4.60889411841261));
#127154=CARTESIAN_POINT('Ctrl Pts',(14.1843823843619,14.5876397315939,4.6245713474448));
#127155=CARTESIAN_POINT('Ctrl Pts',(14.1818815218484,14.5511458636003,4.64260116181636));
#127156=CARTESIAN_POINT('Ctrl Pts',(14.1793335983198,14.5159979928109,4.6628366008176));
#127157=CARTESIAN_POINT('Ctrl Pts',(14.1771666143414,14.4861050733328,4.68004664327771));
#127158=CARTESIAN_POINT('Ctrl Pts',(14.1749649995716,14.4571859046301,4.69885152483509));
#127159=CARTESIAN_POINT('Ctrl Pts',(14.1726914868891,14.4294289454477,4.71913157462172));
#127160=CARTESIAN_POINT('Ctrl Pts',(14.1726905696894,14.4294177475014,4.71913975617028));
#127161=CARTESIAN_POINT('Ctrl Pts',(14.1726896524781,14.4294065497437,4.7191479379589));
#127162=CARTESIAN_POINT('Ctrl Pts',(14.1726887352551,14.4293953521745,4.71915611998757));
#127163=CARTESIAN_POINT('Ctrl Pts',(14.1702276700408,14.3993503723837,4.7411098925167));
#127164=CARTESIAN_POINT('Ctrl Pts',(14.1676751843725,14.3705448742591,4.7648871771113));
#127165=CARTESIAN_POINT('Ctrl Pts',(14.1650863475534,14.3431869183278,4.79030482883998));
#127166=CARTESIAN_POINT('Ctrl Pts',(14.1648865805999,14.3410758484172,4.79226617565611));
#127167=CARTESIAN_POINT('Ctrl Pts',(14.164686597197,14.338973404483,4.79423726507427));
#127168=CARTESIAN_POINT('Ctrl Pts',(14.1644864226476,14.3368796851395,4.79621800045316));
#127169=CARTESIAN_POINT('Ctrl Pts',(14.1616962574177,14.3076960405111,4.82382679987533));
#127170=CARTESIAN_POINT('Ctrl Pts',(14.1588695674215,14.2802055500566,4.85331483920632));
#127171=CARTESIAN_POINT('Ctrl Pts',(14.156060252777,14.2546295215275,4.88442864994626));
#127172=CARTESIAN_POINT('Ctrl Pts',(14.1532536793199,14.2290784487964,4.91551210139964));
#127173=CARTESIAN_POINT('Ctrl Pts',(14.1504647355591,14.2054378478206,4.94821799952283));
#127174=CARTESIAN_POINT('Ctrl Pts',(14.1477259358544,14.183895624954,4.98227469858544));
#127175=CARTESIAN_POINT('Ctrl Pts',(14.1449884348389,14.1623636170198,5.01631524857737));
#127176=CARTESIAN_POINT('Ctrl Pts',(14.1423011064742,14.1429279597531,5.05170527324956));
#127177=CARTESIAN_POINT('Ctrl Pts',(14.1396725517865,14.1257457157262,5.08815597903113));
#127178=CARTESIAN_POINT('Ctrl Pts',(14.1370420635292,14.1085508324096,5.12463349801744));
#127179=CARTESIAN_POINT('Ctrl Pts',(14.1344703559481,14.0936128247948,5.16217325154629));
#127180=CARTESIAN_POINT('Ctrl Pts',(14.1319421762138,14.0810576269801,5.20046860430385));
#127181=CARTESIAN_POINT('Ctrl Pts',(14.1294129994541,14.0684974778359,5.23877905940494));
#127182=CARTESIAN_POINT('Ctrl Pts',(14.1269271291977,14.0583223397542,5.27784570733791));
#127183=CARTESIAN_POINT('Ctrl Pts',(14.1244478852292,14.0506233282853,5.31734438360384));
#127184=CARTESIAN_POINT('Ctrl Pts',(14.1219640356409,14.0429100145852,5.35691643541916));
#127185=CARTESIAN_POINT('Ctrl Pts',(14.1194863411734,14.0376825908161,5.39692205552027));
#127186=CARTESIAN_POINT('Ctrl Pts',(14.1169619848924,14.0349910449687,5.43701843224845));
#127187=CARTESIAN_POINT('Ctrl Pts',(14.1156350303954,14.0335762055133,5.45809551546768));
#127188=CARTESIAN_POINT('Ctrl Pts',(14.1142949564463,14.032861337069,5.47919739534369));
#127189=CARTESIAN_POINT('Ctrl Pts',(14.1129332120935,14.0328481709776,5.50027263358238));
#127190=CARTESIAN_POINT('Ctrl Pts',(14.0538074365636,14.033250458383,5.50094142621558));
#127191=CARTESIAN_POINT('Ctrl Pts',(14.0562298969709,14.0332173341493,5.46692618718686));
#127192=CARTESIAN_POINT('Ctrl Pts',(14.0586822435128,14.0349794725945,5.43293283883328));
#127193=CARTESIAN_POINT('Ctrl Pts',(14.0648394380835,14.0439380481791,5.34756452147048));
#127194=CARTESIAN_POINT('Ctrl Pts',(14.0685139854803,14.0534823431676,5.29653817716552));
#127195=CARTESIAN_POINT('Ctrl Pts',(14.073292532037,14.0717735384525,5.22921867651981));
#127196=CARTESIAN_POINT('Ctrl Pts',(14.0745054503242,14.0769541103416,5.21205339106437));
#127197=CARTESIAN_POINT('Ctrl Pts',(14.0763431736832,14.0856359270963,5.18593637599146));
#127198=CARTESIAN_POINT('Ctrl Pts',(14.0769792030934,14.0887979658629,5.17687698556369));
#127199=CARTESIAN_POINT('Ctrl Pts',(14.0781476880215,14.0948982604325,5.16020151974847));
#127200=CARTESIAN_POINT('Ctrl Pts',(14.0786813697705,14.0977990797569,5.15257278058654));
#127201=CARTESIAN_POINT('Ctrl Pts',(14.0798616675843,14.1044689192757,5.13567916947201));
#127202=CARTESIAN_POINT('Ctrl Pts',(14.0805065495745,14.1082858432902,5.12643412964555));
#127203=CARTESIAN_POINT('Ctrl Pts',(14.0823886423087,14.1199291866492,5.09942846028579));
#127204=CARTESIAN_POINT('Ctrl Pts',(14.0836120505354,14.1281479705073,5.08184175657311));
#127205=CARTESIAN_POINT('Ctrl Pts',(14.0898489125388,14.1732929774851,4.99236700713743));
#127206=CARTESIAN_POINT('Ctrl Pts',(14.0945506468488,14.2185943630929,4.92507303055884));
#127207=CARTESIAN_POINT('Ctrl Pts',(14.100891051039,14.2876979893702,4.845920389463));
#127208=CARTESIAN_POINT('Ctrl Pts',(14.1023712695334,14.304336948238,4.82825075003465));
#127209=CARTESIAN_POINT('Ctrl Pts',(14.1048548421149,14.3326635447107,4.80035165159155));
#127210=CARTESIAN_POINT('Ctrl Pts',(14.1058369951912,14.343964587907,4.78974425133705));
#127211=CARTESIAN_POINT('Ctrl Pts',(14.1072458427187,14.3602143297748,4.77521064450908));
#127212=CARTESIAN_POINT('Ctrl Pts',(14.1076564355509,14.3649546192145,4.77105372452122));
#127213=CARTESIAN_POINT('Ctrl Pts',(14.108379896014,14.373306426234,4.76387303393529));
#127214=CARTESIAN_POINT('Ctrl Pts',(14.1086912360883,14.3768999623784,4.7608287852438));
#127215=CARTESIAN_POINT('Ctrl Pts',(14.109386972226,14.384930810515,4.75412565978937));
#127216=CARTESIAN_POINT('Ctrl Pts',(14.109772260729,14.3893787892095,4.75047990547109));
#127217=CARTESIAN_POINT('Ctrl Pts',(14.110887089195,14.4022581175886,4.740114186977));
#127218=CARTESIAN_POINT('Ctrl Pts',(14.1116228582927,14.4107694325652,4.73349551720651));
#127219=CARTESIAN_POINT('Ctrl Pts',(14.1154811581633,14.4555444676834,4.69986347141738));
#127220=CARTESIAN_POINT('Ctrl Pts',(14.118712859258,14.4935576325376,4.6752783834827));
#127221=CARTESIAN_POINT('Ctrl Pts',(14.1254702415451,14.5761740704372,4.62971762131015));
#127222=CARTESIAN_POINT('Ctrl Pts',(14.1289861315741,14.6209502950831,4.60930256375851));
#127223=CARTESIAN_POINT('Ctrl Pts',(14.1344617560915,14.6946508693338,4.58226941888499));
#127224=CARTESIAN_POINT('Ctrl Pts',(14.1364765865886,14.7226624763879,4.57341934839747));
#127225=CARTESIAN_POINT('Ctrl Pts',(14.1392511245881,14.7625124044787,4.56279870544198));
#127226=CARTESIAN_POINT('Ctrl Pts',(14.140043589744,14.7740445547766,4.55995171285887));
#127227=CARTESIAN_POINT('Ctrl Pts',(14.1414148525698,14.7942535674138,4.55535602478808));
#127228=CARTESIAN_POINT('Ctrl Pts',(14.141996514414,14.8029072034539,4.55351266648904));
#127229=CARTESIAN_POINT('Ctrl Pts',(14.1432016613457,14.8209996978987,4.54991758918165));
#127230=CARTESIAN_POINT('Ctrl Pts',(14.1438244356717,14.8304418250294,4.54818713429662));
#127231=CARTESIAN_POINT('Ctrl Pts',(14.1454695678927,14.8556156080642,4.54396005235854));
#127232=CARTESIAN_POINT('Ctrl Pts',(14.1464844010567,14.8713861882827,4.54171102193587));
#127233=CARTESIAN_POINT('Ctrl Pts',(14.1508445664755,14.9400366908152,4.53364624476629));
#127234=CARTESIAN_POINT('Ctrl Pts',(14.1540735081881,14.9932916363082,4.53181049264748));
#127235=CARTESIAN_POINT('Ctrl Pts',(14.1598362811027,15.0884752531637,4.53638728429054));
#127236=CARTESIAN_POINT('Ctrl Pts',(14.1623702637541,15.130339926785,4.54115253636299));
#127237=CARTESIAN_POINT('Ctrl Pts',(14.1663312027684,15.1931919320012,4.55249970137794));
#127238=CARTESIAN_POINT('Ctrl Pts',(14.1677015580241,15.2144870976862,4.55709222244319));
#127239=CARTESIAN_POINT('Ctrl Pts',(14.1695863090062,15.2428444032365,4.5642180588735));
#127240=CARTESIAN_POINT('Ctrl Pts',(14.1700711776451,15.2500599526167,4.5661203195351));
#127241=CARTESIAN_POINT('Ctrl Pts',(14.1708942699946,15.2621593251666,4.56946039176176));
#127242=CARTESIAN_POINT('Ctrl Pts',(14.1712301225547,15.2670552952967,4.57085364870826));
#127243=CARTESIAN_POINT('Ctrl Pts',(14.1719411960869,15.2773292754341,4.57386524977325));
#127244=CARTESIAN_POINT('Ctrl Pts',(14.1723168407206,15.2827045380052,4.57549189133028));
#127245=CARTESIAN_POINT('Ctrl Pts',(14.1733863088937,15.2978695982969,4.58022570243608));
#127246=CARTESIAN_POINT('Ctrl Pts',(14.1740856867667,15.3076241825002,4.58344209223064));
#127247=CARTESIAN_POINT('Ctrl Pts',(14.1786600515643,15.3704941391684,4.60528890325809));
#127248=CARTESIAN_POINT('Ctrl Pts',(14.1827078615811,15.421943866773,4.62837146042055));
#127249=CARTESIAN_POINT('Ctrl Pts',(14.1911444005081,15.5249886555182,4.68587331240808));
#127250=CARTESIAN_POINT('Ctrl Pts',(14.195505187317,15.5758914854332,4.72104774407341));
#127251=CARTESIAN_POINT('Ctrl Pts',(14.2006519395827,15.6339492893575,4.7699895313703));
#127252=CARTESIAN_POINT('Ctrl Pts',(14.2016046648137,15.6445981934798,4.77937513898573));
#127253=CARTESIAN_POINT('Ctrl Pts',(14.2031586635232,15.6617952939285,4.79521847992429));
#127254=CARTESIAN_POINT('Ctrl Pts',(14.2037653420745,15.6684645990472,4.80154091628627));
#127255=CARTESIAN_POINT('Ctrl Pts',(14.2049450575848,15.6813407454673,4.8141007718935));
#127256=CARTESIAN_POINT('Ctrl Pts',(14.2055183698493,15.6875545619149,4.82032971576615));
#127257=CARTESIAN_POINT('Ctrl Pts',(14.2069026431817,15.7024437741181,4.83566836223354));
#127258=CARTESIAN_POINT('Ctrl Pts',(14.2077097247531,15.7110282107699,4.84486437490422));
#127259=CARTESIAN_POINT('Ctrl Pts',(14.2106425099764,15.7418240337471,4.87917275436612));
#127260=CARTESIAN_POINT('Ctrl Pts',(14.2127233586005,15.7629056182872,4.90526920859455));
#127261=CARTESIAN_POINT('Ctrl Pts',(14.2150217214187,15.7849707871205,4.93569257943748));
#127262=CARTESIAN_POINT('Ctrl Pts',(14.2152692219312,15.787330577067,4.93898969316743));
#127263=CARTESIAN_POINT('Ctrl Pts',(14.2188786518254,15.8214967901948,4.98736712741556));
#127264=CARTESIAN_POINT('Ctrl Pts',(14.2221530407581,15.8494069651619,5.03507306952823));
#127265=CARTESIAN_POINT('Ctrl Pts',(14.2275518021116,15.8874656116362,5.11512289154344));
#127266=CARTESIAN_POINT('Ctrl Pts',(14.2296198384497,15.9002550104573,5.14607054801264));
#127267=CARTESIAN_POINT('Ctrl Pts',(14.2323007783964,15.9141898787153,5.18546579218286));
#127268=CARTESIAN_POINT('Ctrl Pts',(14.232839792009,15.9168650652493,5.1933514336952));
#127269=CARTESIAN_POINT('Ctrl Pts',(14.2337230818305,15.9210382703056,5.20619583261487));
#127270=CARTESIAN_POINT('Ctrl Pts',(14.2340639359194,15.9225989396651,5.21113397979167));
#127271=CARTESIAN_POINT('Ctrl Pts',(14.2347501019306,15.925639860556,5.22103190062307));
#127272=CARTESIAN_POINT('Ctrl Pts',(14.2350954089997,15.9271200976424,5.22599147306835));
#127273=CARTESIAN_POINT('Ctrl Pts',(14.2360079109081,15.9309029679066,5.2390477339749));
#127274=CARTESIAN_POINT('Ctrl Pts',(14.2365785600612,15.9331397498161,5.24716286591365));
#127275=CARTESIAN_POINT('Ctrl Pts',(14.2394144071364,15.9436398845298,5.28729648574071));
#127276=CARTESIAN_POINT('Ctrl Pts',(14.2417455464504,15.9503619509647,5.31969259336735));
#127277=CARTESIAN_POINT('Ctrl Pts',(14.2484337760382,15.9646979021073,5.41246738656664));
#127278=CARTESIAN_POINT('Ctrl Pts',(14.2528257146872,15.9682938845111,5.47331688320412));
#127279=CARTESIAN_POINT('Ctrl Pts',(14.2593574026124,15.9650055546371,5.56647811701911));
#127280=CARTESIAN_POINT('Ctrl Pts',(14.261588860755,15.9622360533886,5.59877870816187));
#127281=CARTESIAN_POINT('Ctrl Pts',(14.2645866769297,15.9562115238328,5.64286859119123));
#127282=CARTESIAN_POINT('Ctrl Pts',(14.2653947411797,15.9543488134276,5.65482337484774));
#127283=CARTESIAN_POINT('Ctrl Pts',(14.2667737312296,15.9507568693147,5.67533711894123));
#127284=CARTESIAN_POINT('Ctrl Pts',(14.2673479363237,15.9491352300182,5.68391316794778));
#127285=CARTESIAN_POINT('Ctrl Pts',(14.2685199265679,15.9455662090536,5.70148134278337));
#127286=CARTESIAN_POINT('Ctrl Pts',(14.2691172484402,15.9436061537407,5.71047000585123));
#127287=CARTESIAN_POINT('Ctrl Pts',(14.2706524219015,15.9382040773192,5.73364897897117));
#127288=CARTESIAN_POINT('Ctrl Pts',(14.271584093476,15.9345682870344,5.74779202658948));
#127289=CARTESIAN_POINT('Ctrl Pts',(14.2773436026378,15.9098805000807,5.83553297934397));
#127290=CARTESIAN_POINT('Ctrl Pts',(14.2818839662849,15.8804705215952,5.90649425481911));
#127291=CARTESIAN_POINT('Ctrl Pts',(14.2883263767746,15.8282079114558,5.99958963713148));
#127292=CARTESIAN_POINT('Ctrl Pts',(14.2901616680309,15.8121941481268,6.02522241750458));
#127293=CARTESIAN_POINT('Ctrl Pts',(14.2931641365855,15.7847834849569,6.06483923095255));
#127294=CARTESIAN_POINT('Ctrl Pts',(14.2943002889114,15.7741497210443,6.07932770744158));
#127295=CARTESIAN_POINT('Ctrl Pts',(14.2959033858421,15.7589086727182,6.09892422491411));
#127296=CARTESIAN_POINT('Ctrl Pts',(14.2963497249731,15.7546407704728,6.10429289395318));
#127297=CARTESIAN_POINT('Ctrl Pts',(14.2971210819535,15.7472319858605,6.11341164415223));
#127298=CARTESIAN_POINT('Ctrl Pts',(14.2974441824521,15.7441191560303,6.11718406180125));
#127299=CARTESIAN_POINT('Ctrl Pts',(14.2981480058826,15.7373200442749,6.12529764501526));
#127300=CARTESIAN_POINT('Ctrl Pts',(14.2985293648129,15.7336239914721,6.12962991330551));
#127301=CARTESIAN_POINT('Ctrl Pts',(14.2996216634735,15.7229976900521,6.14186476824886));
#127302=CARTESIAN_POINT('Ctrl Pts',(14.3003384686996,15.7159767534749,6.14968708430807));
#127303=CARTESIAN_POINT('Ctrl Pts',(14.3044085354346,15.6757742429175,6.19303519951512));
#127304=CARTESIAN_POINT('Ctrl Pts',(14.3078899126151,15.640079903932,6.22613054288866));
#127305=CARTESIAN_POINT('Ctrl Pts',(14.3147129407198,15.5655382584345,6.28546161181057));
#127306=CARTESIAN_POINT('Ctrl Pts',(14.3180456350148,15.5269651067212,6.31184477239251));
#127307=CARTESIAN_POINT('Ctrl Pts',(14.3232772103154,15.4620851176591,6.34964115626188));
#127308=CARTESIAN_POINT('Ctrl Pts',(14.3252253721968,15.4369156463575,6.3628544131446));
#127309=CARTESIAN_POINT('Ctrl Pts',(14.3279202225422,15.4006491977218,6.3798986582361));
#127310=CARTESIAN_POINT('Ctrl Pts',(14.3286977110921,15.3900108241399,6.38466547652845));
#127311=CARTESIAN_POINT('Ctrl Pts',(14.3300457407502,15.3712655780084,6.39266091520018));
#127312=CARTESIAN_POINT('Ctrl Pts',(14.3306190435817,15.363196562391,6.39597427657361));
#127313=CARTESIAN_POINT('Ctrl Pts',(14.3318087705913,15.346254832935,6.4026645309419));
#127314=CARTESIAN_POINT('Ctrl Pts',(14.3324244689336,15.3373749684169,6.40602086387693));
#127315=CARTESIAN_POINT('Ctrl Pts',(14.3340532461462,15.3135977422034,6.4146099094455));
#127316=CARTESIAN_POINT('Ctrl Pts',(14.3350587781171,15.2986188613529,6.41960950940615));
#127317=CARTESIAN_POINT('Ctrl Pts',(14.3401981095314,15.2206754135691,6.44351974746627));
#127318=CARTESIAN_POINT('Ctrl Pts',(14.3441366015729,15.1560237701942,6.45633922979636));
#127319=CARTESIAN_POINT('Ctrl Pts',(14.3510961220375,15.0410709992831,6.46715574788448));
#127320=CARTESIAN_POINT('Ctrl Pts',(14.35410137129,14.9912954059873,6.46798768348413));
#127321=CARTESIAN_POINT('Ctrl Pts',(14.3579027833784,14.9317812315508,6.46439108698719));
#127322=CARTESIAN_POINT('Ctrl Pts',(14.3585416376089,14.9218895376033,6.46364034094103));
#127323=CARTESIAN_POINT('Ctrl Pts',(14.3595482136472,14.9065113741516,6.46223486976764));
#127324=CARTESIAN_POINT('Ctrl Pts',(14.3599106000204,14.9010157121724,6.46168507055188));
#127325=CARTESIAN_POINT('Ctrl Pts',(14.3606016758154,14.8906198245719,6.4605549890717));
#127326=CARTESIAN_POINT('Ctrl Pts',(14.3609298642706,14.8857188557905,6.45998423188809));
#127327=CARTESIAN_POINT('Ctrl Pts',(14.3617487697514,14.8735745741501,6.45847562269793));
#127328=CARTESIAN_POINT('Ctrl Pts',(14.3622417891364,14.866337211546,6.45749316379624));
#127329=CARTESIAN_POINT('Ctrl Pts',(14.3640750732588,14.8396716374609,6.45356515508447));
#127330=CARTESIAN_POINT('Ctrl Pts',(14.3654381198333,14.8203245545211,6.45010962946027));
#127331=CARTESIAN_POINT('Ctrl Pts',(14.371967727122,14.7293121834208,6.43097508460043));
#127332=CARTESIAN_POINT('Ctrl Pts',(14.3773037500281,14.6594765869179,6.40776175072064));
#127333=CARTESIAN_POINT('Ctrl Pts',(14.384909787144,14.5612826379397,6.36217770800166));
#127334=CARTESIAN_POINT('Ctrl Pts',(14.3873192278779,14.5304465306348,6.34577972707653));
#127335=CARTESIAN_POINT('Ctrl Pts',(14.3905103992866,14.4899251778128,6.32133036014429));
#127336=CARTESIAN_POINT('Ctrl Pts',(14.3913408313173,14.4794129864875,6.31470796619853));
#127337=CARTESIAN_POINT('Ctrl Pts',(14.3927489294437,14.4616531781826,6.30303561884774));
#127338=CARTESIAN_POINT('Ctrl Pts',(14.3933301394323,14.4543419954351,6.29808574499851));
#127339=CARTESIAN_POINT('Ctrl Pts',(14.3945090759668,14.4395576050809,6.28777814870805));
#127340=CARTESIAN_POINT('Ctrl Pts',(14.3951064302479,14.4320909619195,6.28241256606969));
#127341=CARTESIAN_POINT('Ctrl Pts',(14.396626734096,14.4131618440449,6.26839620454434));
#127342=CARTESIAN_POINT('Ctrl Pts',(14.3975438698829,14.4018132770824,6.25959490953729));
#127343=CARTESIAN_POINT('Ctrl Pts',(14.4033927086036,14.3300346616598,6.20132080991892));
#127344=CARTESIAN_POINT('Ctrl Pts',(14.4080240120743,14.275593022949,6.14493406245014));
#127345=CARTESIAN_POINT('Ctrl Pts',(14.4145133974075,14.2108923797592,6.0592591840226));
#127346=CARTESIAN_POINT('Ctrl Pts',(14.4162947064593,14.1943295068235,6.03512289845086));
#127347=CARTESIAN_POINT('Ctrl Pts',(14.4192203826514,14.1695835970152,5.99530281122447));
#127348=CARTESIAN_POINT('Ctrl Pts',(14.4203360031198,14.1606914331173,5.98008053510531));
#127349=CARTESIAN_POINT('Ctrl Pts',(14.4219165073331,14.1489337304065,5.9586268082552));
#127350=CARTESIAN_POINT('Ctrl Pts',(14.4223618035421,14.1457103794684,5.95259427997009));
#127351=CARTESIAN_POINT('Ctrl Pts',(14.423133118597,14.1402855927444,5.94217730081682));
#127352=CARTESIAN_POINT('Ctrl Pts',(14.4234572622124,14.1380530602517,5.9378094326138));
#127353=CARTESIAN_POINT('Ctrl Pts',(14.4241647359729,14.1332838695781,5.928300793185));
#127354=CARTESIAN_POINT('Ctrl Pts',(14.4245487248028,14.1307596602008,5.92315440185414));
#127355=CARTESIAN_POINT('Ctrl Pts',(14.4256571491854,14.1236521900996,5.90833162511792));
#127356=CARTESIAN_POINT('Ctrl Pts',(14.4263877194663,14.1191838667779,5.89860145106974));
#127357=CARTESIAN_POINT('Ctrl Pts',(14.4301212655879,14.0973870322842,5.84897986492439));
#127358=CARTESIAN_POINT('Ctrl Pts',(14.4332254534356,14.0826042506681,5.80802844442641));
#127359=CARTESIAN_POINT('Ctrl Pts',(14.4391598882848,14.0597802042454,5.72835150250859));
#127360=CARTESIAN_POINT('Ctrl Pts',(14.4419832177582,14.0512557819224,5.68984829087294));
#127361=CARTESIAN_POINT('Ctrl Pts',(14.4474218957436,14.0392090698258,5.61363227443366));
#127362=CARTESIAN_POINT('Ctrl Pts',(14.4500365217652,14.0355034701813,5.5760167974511));
#127363=CARTESIAN_POINT('Ctrl Pts',(14.4534425855343,14.0335053004661,5.52558891189949));
#127364=CARTESIAN_POINT('Ctrl Pts',(14.4542920249362,14.0332525553951,5.51289190225747));
#127365=CARTESIAN_POINT('Ctrl Pts',(14.4551338463912,14.0332500192795,5.50019307209264));
#127366=CARTESIAN_POINT('Origin',(16.125,15.,5.5));
#127367=CARTESIAN_POINT('',(14.9122050450034,14.0332503695598,5.49915468993569));
#127368=CARTESIAN_POINT('',(14.8539665893558,14.0332503192036,5.49922960238524));
#127369=CARTESIAN_POINT('',(16.125,14.03325,5.5));
#127370=CARTESIAN_POINT('Ctrl Pts',(14.9122050445523,14.0332503695571,5.49915469624611));
#127371=CARTESIAN_POINT('Ctrl Pts',(14.9082502315315,14.0332019940531,5.55448037106382));
#127372=CARTESIAN_POINT('Ctrl Pts',(14.9043425918772,14.0379029547454,5.60971498880857));
#127373=CARTESIAN_POINT('Ctrl Pts',(14.899465079513,14.050066977222,5.68026935697303));
#127374=CARTESIAN_POINT('Ctrl Pts',(14.8983696073238,14.0532324042794,5.69621661959429));
#127375=CARTESIAN_POINT('Ctrl Pts',(14.8966351867929,14.0589431604573,5.72161487145916));
#127376=CARTESIAN_POINT('Ctrl Pts',(14.8959884324965,14.0612322696413,5.73111963710856));
#127377=CARTESIAN_POINT('Ctrl Pts',(14.8947549069735,14.0659050797534,5.74930553296568));
#127378=CARTESIAN_POINT('Ctrl Pts',(14.8941675098451,14.0682666184343,5.75799124682317));
#127379=CARTESIAN_POINT('Ctrl Pts',(14.8928007927342,14.0740800376407,5.77825101499658));
#127380=CARTESIAN_POINT('Ctrl Pts',(14.8920246108413,14.077628225723,5.7897960224413));
#127381=CARTESIAN_POINT('Ctrl Pts',(14.8893424690424,14.0907416551355,5.82978017153723));
#127382=CARTESIAN_POINT('Ctrl Pts',(14.887471616334,14.1014139303266,5.85783938413386));
#127383=CARTESIAN_POINT('Ctrl Pts',(14.8824737577382,14.1338351668622,5.93243344243876));
#127384=CARTESIAN_POINT('Ctrl Pts',(14.8794103816961,14.158011932621,5.97780380570704));
#127385=CARTESIAN_POINT('Ctrl Pts',(14.8738290093159,14.2078040631002,6.05562276626686));
#127386=CARTESIAN_POINT('Ctrl Pts',(14.8713285836058,14.2321092845856,6.08875650907772));
#127387=CARTESIAN_POINT('Ctrl Pts',(14.8680391683436,14.2653117869397,6.12845317398805));
#127388=CARTESIAN_POINT('Ctrl Pts',(14.8673515195187,14.2723155091575,6.13654962252689));
#127389=CARTESIAN_POINT('Ctrl Pts',(14.8662747045411,14.2833481443383,6.14888352908781));
#127390=CARTESIAN_POINT('Ctrl Pts',(14.8658917949038,14.2872837060635,6.15320379413745));
#127391=CARTESIAN_POINT('Ctrl Pts',(14.8651692104273,14.2947274045547,6.16122776019404));
#127392=CARTESIAN_POINT('Ctrl Pts',(14.8648301958532,14.29822606158,6.16493978621154));
#127393=CARTESIAN_POINT('Ctrl Pts',(14.8640013338561,14.3067975837921,6.17389105620963));
#127394=CARTESIAN_POINT('Ctrl Pts',(14.8635093366963,14.311900593296,6.17910083501389));
#127395=CARTESIAN_POINT('Ctrl Pts',(14.8616506922213,14.3312521590897,6.19841523774386));
#127396=CARTESIAN_POINT('Ctrl Pts',(14.8602601107601,14.3458785675009,6.21213239542386));
#127397=CARTESIAN_POINT('Ctrl Pts',(14.8563343075277,14.3878317057881,6.24909410500529));
#127398=CARTESIAN_POINT('Ctrl Pts',(14.8537656270426,14.4160413212151,6.27128726434364));
#127399=CARTESIAN_POINT('Ctrl Pts',(14.8465672445191,14.4984028839494,6.32896949270947));
#127400=CARTESIAN_POINT('Ctrl Pts',(14.8419697127358,14.55498719631,6.36067191768671));
#127401=CARTESIAN_POINT('Ctrl Pts',(14.8364694708892,14.6290544025969,6.39289588266202));
#127402=CARTESIAN_POINT('Ctrl Pts',(14.8353870985073,14.6439451282188,6.39893752468016));
#127403=CARTESIAN_POINT('Ctrl Pts',(14.8336681639751,14.6680922729971,6.40804055571155));
#127404=CARTESIAN_POINT('Ctrl Pts',(14.8330240428701,14.6772558909764,6.41133783073744));
#127405=CARTESIAN_POINT('Ctrl Pts',(14.8317923816868,14.6949940721784,6.41741930660174));
#127406=CARTESIAN_POINT('Ctrl Pts',(14.831204261519,14.7035607805634,6.42022312419855));
#127407=CARTESIAN_POINT('Ctrl Pts',(14.8298310914207,14.7237813525899,6.42652947532849));
#127408=CARTESIAN_POINT('Ctrl Pts',(14.8290492726973,14.73546475944,6.42993265204433));
#127409=CARTESIAN_POINT('Ctrl Pts',(14.8263170151823,14.7768525511048,6.44114502876785));
#127410=CARTESIAN_POINT('Ctrl Pts',(14.8244035820216,14.8068629438175,6.44775898429116));
#127411=CARTESIAN_POINT('Ctrl Pts',(14.8192180719922,14.8901229161273,6.46198846762755));
#127412=CARTESIAN_POINT('Ctrl Pts',(14.8160166896129,14.9437686689442,6.46660899051327));
#127413=CARTESIAN_POINT('Ctrl Pts',(14.8102680296816,15.0387520554816,6.46685254576769));
#127414=CARTESIAN_POINT('Ctrl Pts',(14.8077459676647,15.0799431242302,6.46432043434005));
#127415=CARTESIAN_POINT('Ctrl Pts',(14.804539681343,15.1296271005955,6.45806095118941));
#127416=CARTESIAN_POINT('Ctrl Pts',(14.8039674307318,15.1383965417581,6.45683350454771));
#127417=CARTESIAN_POINT('Ctrl Pts',(14.8030364083054,15.1524803602225,6.45466455680153));
#127418=CARTESIAN_POINT('Ctrl Pts',(14.8026815762018,15.1578060834347,6.45379867523597));
#127419=CARTESIAN_POINT('Ctrl Pts',(14.8019701441423,15.1683936638962,6.45198619648021));
#127420=CARTESIAN_POINT('Ctrl Pts',(14.8016135968478,15.1736554617176,6.45104044143365));
#127421=CARTESIAN_POINT('Ctrl Pts',(14.8006762223517,15.1873807585009,6.44845576079329));
#127422=CARTESIAN_POINT('Ctrl Pts',(14.8000918421118,15.195830475384,6.44674721614167));
#127423=CARTESIAN_POINT('Ctrl Pts',(14.7970262403958,15.2396615804815,6.43727265424319));
#127424=CARTESIAN_POINT('Ctrl Pts',(14.7944665863109,15.2746059060149,6.42763613005524));
#127425=CARTESIAN_POINT('Ctrl Pts',(14.7858956768326,15.3884708324279,6.38923752049845));
#127426=CARTESIAN_POINT('Ctrl Pts',(14.7798545262504,15.464203214228,6.35215809855692));
#127427=CARTESIAN_POINT('Ctrl Pts',(14.7731435505965,15.5465954303663,6.29753387804318));
#127428=CARTESIAN_POINT('Ctrl Pts',(14.7721437969525,15.5588030513961,6.28902854314845));
#127429=CARTESIAN_POINT('Ctrl Pts',(14.7705225650791,15.5784783068559,6.27463454822229));
#127430=CARTESIAN_POINT('Ctrl Pts',(14.769895019805,15.5860636137766,6.2689117544654));
#127431=CARTESIAN_POINT('Ctrl Pts',(14.7686731848782,15.6007656562799,6.25747570490312));
#127432=CARTESIAN_POINT('Ctrl Pts',(14.7680786266893,15.6078882784428,6.25177168576603));
#127433=CARTESIAN_POINT('Ctrl Pts',(14.76665494423,15.6248578655109,6.23778301235662));
#127434=CARTESIAN_POINT('Ctrl Pts',(14.7658297805056,15.6346224062644,6.22940081676402));
#127435=CARTESIAN_POINT('Ctrl Pts',(14.7626615950873,15.6717823853933,6.19619016999649));
#127436=CARTESIAN_POINT('Ctrl Pts',(14.7603745784783,15.6979135602774,6.16999209656738));
#127437=CARTESIAN_POINT('Ctrl Pts',(14.7556529509188,15.7493805434745,6.11210553044752));
#127438=CARTESIAN_POINT('Ctrl Pts',(14.753229851437,15.7743523385292,6.08019212950624));
#127439=CARTESIAN_POINT('Ctrl Pts',(14.7481999229132,15.8214839937927,6.01147367533789));
#127440=CARTESIAN_POINT('Ctrl Pts',(14.7455958591552,15.8433397127383,5.97457206542411));
#127441=CARTESIAN_POINT('Ctrl Pts',(14.7421881672977,15.8675450821781,5.92671718709921));
#127442=CARTESIAN_POINT('Ctrl Pts',(14.7414951109509,15.8722542247513,5.91700668115971));
#127443=CARTESIAN_POINT('Ctrl Pts',(14.7404116117773,15.8792690490483,5.90190281299664));
#127444=CARTESIAN_POINT('Ctrl Pts',(14.7400275474056,15.8816900022901,5.89656357284522));
#127445=CARTESIAN_POINT('Ctrl Pts',(14.7393041424174,15.8861244866421,5.88654227507385));
#127446=CARTESIAN_POINT('Ctrl Pts',(14.738965483854,15.8881497844291,5.88186580352009));
#127447=CARTESIAN_POINT('Ctrl Pts',(14.7381394003303,15.8929693640861,5.87049149197632));
#127448=CARTESIAN_POINT('Ctrl Pts',(14.7376498625717,15.8957253323618,5.86377788833509));
#127449=CARTESIAN_POINT('Ctrl Pts',(14.7358132560148,15.9057047352811,5.83866670748072));
#127450=CARTESIAN_POINT('Ctrl Pts',(14.7344429502974,15.9124385988233,5.82008107117521));
#127451=CARTESIAN_POINT('Ctrl Pts',(14.7305995272493,15.929506637127,5.76804499072815));
#127452=CARTESIAN_POINT('Ctrl Pts',(14.7280943600802,15.9386008413785,5.73421988092676));
#127453=CARTESIAN_POINT('Ctrl Pts',(14.7208563744918,15.9595146758142,5.63530316622377));
#127454=CARTESIAN_POINT('Ctrl Pts',(14.7161542580187,15.9665213324667,5.56938649679398));
#127455=CARTESIAN_POINT('Ctrl Pts',(14.7105657765703,15.9667983767351,5.4872971117587));
#127456=CARTESIAN_POINT('Ctrl Pts',(14.7094904065259,15.9664567536837,5.47133192676454));
#127457=CARTESIAN_POINT('Ctrl Pts',(14.7077797185688,15.9652712938315,5.44567379571244));
#127458=CARTESIAN_POINT('Ctrl Pts',(14.7071369735811,15.9646763973644,5.43597291943918));
#127459=CARTESIAN_POINT('Ctrl Pts',(14.7059061951079,15.9632474002824,5.41728728704957));
#127460=CARTESIAN_POINT('Ctrl Pts',(14.7053176066802,15.962433603545,5.40830204570714));
#127461=CARTESIAN_POINT('Ctrl Pts',(14.703940672026,15.9602216474156,5.38717591945265));
#127462=CARTESIAN_POINT('Ctrl Pts',(14.7031556100191,15.9587188079405,5.37504739345968));
#127463=CARTESIAN_POINT('Ctrl Pts',(14.7003942497529,15.952574188684,5.33214097749989));
#127464=CARTESIAN_POINT('Ctrl Pts',(14.698456081271,15.9466765411517,5.30156099766003));
#127465=CARTESIAN_POINT('Ctrl Pts',(14.6937404033701,15.9284967959997,5.22688803593776));
#127466=CARTESIAN_POINT('Ctrl Pts',(14.6910033671348,15.9145418097206,5.18328261107043));
#127467=CARTESIAN_POINT('Ctrl Pts',(14.6853251765019,15.8795652913527,5.09587817113486));
#127468=CARTESIAN_POINT('Ctrl Pts',(14.6823887788008,15.8582288404779,5.05234870484421));
#127469=CARTESIAN_POINT('Ctrl Pts',(14.6787150291129,15.8291643817197,5.00283485030576));
#127470=CARTESIAN_POINT('Ctrl Pts',(14.6781329998098,15.8244946211923,4.99512836903688));
#127471=CARTESIAN_POINT('Ctrl Pts',(14.677189944024,15.8168399441178,4.98288536912214));
#127472=CARTESIAN_POINT('Ctrl Pts',(14.6768330415415,15.8139232201728,4.97830658048361));
#127473=CARTESIAN_POINT('Ctrl Pts',(14.6761215872298,15.8080742197859,4.96929303593452));
#127474=CARTESIAN_POINT('Ctrl Pts',(14.6757671397886,15.8051436320107,4.96485744499979));
#127475=CARTESIAN_POINT('Ctrl Pts',(14.674841602851,15.797444688353,4.95341110597143));
#127476=CARTESIAN_POINT('Ctrl Pts',(14.6742671143401,15.7926205064848,4.94643864762816));
#127477=CARTESIAN_POINT('Ctrl Pts',(14.6713956144491,15.7682556047653,4.9121952545743));
#127478=CARTESIAN_POINT('Ctrl Pts',(14.6690311693775,15.7473977718306,4.88589314109405));
#127479=CARTESIAN_POINT('Ctrl Pts',(14.6630790220272,15.6921283389582,4.82319284441154));
#127480=CARTESIAN_POINT('Ctrl Pts',(14.6594734827413,15.6561727673762,4.78827869070979));
#127481=CARTESIAN_POINT('Ctrl Pts',(14.6531348239278,15.5871663563082,4.73096545598608));
#127482=CARTESIAN_POINT('Ctrl Pts',(14.650380596341,15.5551238753468,4.70752500037806));
#127483=CARTESIAN_POINT('Ctrl Pts',(14.6467841020732,15.5103514241787,4.67882425787979));
#127484=CARTESIAN_POINT('Ctrl Pts',(14.6458786938504,15.4988226797119,4.67177047825377));
#127485=CARTESIAN_POINT('Ctrl Pts',(14.64443000349,15.4799660419588,4.66076980395346));
#127486=CARTESIAN_POINT('Ctrl Pts',(14.6438814412111,15.4727288015102,4.65667194354024));
#127487=CARTESIAN_POINT('Ctrl Pts',(14.6427347177708,15.4573998471345,4.6482517515532));
#127488=CARTESIAN_POINT('Ctrl Pts',(14.6421373227796,15.4492976435309,4.643950155745));
#127489=CARTESIAN_POINT('Ctrl Pts',(14.6406931155981,15.4294358553151,4.63376488305315));
#127490=CARTESIAN_POINT('Ctrl Pts',(14.6398505661163,15.4176149092576,4.62800444645703));
#127491=CARTESIAN_POINT('Ctrl Pts',(14.6364709951382,15.3693157286907,4.6056754448396));
#127492=CARTESIAN_POINT('Ctrl Pts',(14.6340009148641,15.3319397893059,4.59113972351818));
#127493=CARTESIAN_POINT('Ctrl Pts',(14.6278618132826,15.2357165728949,4.56044913332094));
#127494=CARTESIAN_POINT('Ctrl Pts',(14.6242567606021,15.1760500560231,4.54746453832502));
#127495=CARTESIAN_POINT('Ctrl Pts',(14.6190133279191,15.0915560248888,4.53729148298161));
#127496=CARTESIAN_POINT('Ctrl Pts',(14.6175009091381,15.067452211537,4.53530305421131));
#127497=CARTESIAN_POINT('Ctrl Pts',(14.6154359475302,15.0353597594244,4.53386416798412));
#127498=CARTESIAN_POINT('Ctrl Pts',(14.6149205339466,15.0274143647318,4.5336060837923));
#127499=CARTESIAN_POINT('Ctrl Pts',(14.6140621467026,15.0143082696865,4.53334211882138));
#127500=CARTESIAN_POINT('Ctrl Pts',(14.6137221313539,15.0091488777585,4.53327952207602));
#127501=CARTESIAN_POINT('Ctrl Pts',(14.613010956915,14.998430177031,4.53323529113415));
#127502=CARTESIAN_POINT('Ctrl Pts',(14.6126394857917,14.9928711456732,4.53326030268536));
#127503=CARTESIAN_POINT('Ctrl Pts',(14.6116180051611,14.9776842480105,4.53345962584562));
#127504=CARTESIAN_POINT('Ctrl Pts',(14.6109632759731,14.968058544759,4.53372984411391));
#127505=CARTESIAN_POINT('Ctrl Pts',(14.6094608041157,14.9461794271081,4.53467130868604));
#127506=CARTESIAN_POINT('Ctrl Pts',(14.6086095314212,14.933931621619,4.5354321806694));
#127507=CARTESIAN_POINT('Ctrl Pts',(14.6057057967256,14.8925534764597,4.53879447288777));
#127508=CARTESIAN_POINT('Ctrl Pts',(14.6036226884099,14.863528698632,4.54248434612449));
#127509=CARTESIAN_POINT('Ctrl Pts',(14.5960022598032,14.7585440238953,4.56070149758644));
#127510=CARTESIAN_POINT('Ctrl Pts',(14.5904708961661,14.684216038275,4.58301183391919));
#127511=CARTESIAN_POINT('Ctrl Pts',(14.5842342283134,14.5999532496313,4.61978339676486));
#127512=CARTESIAN_POINT('Ctrl Pts',(14.5832537069768,14.5867069224777,4.62592475039473));
#127513=CARTESIAN_POINT('Ctrl Pts',(14.5816552061013,14.5651259510178,4.63653062352975));
#127514=CARTESIAN_POINT('Ctrl Pts',(14.5810314904395,14.5567090438686,4.64082135655579));
#127515=CARTESIAN_POINT('Ctrl Pts',(14.579811341566,14.5402577407379,4.64951395562614));
#127516=CARTESIAN_POINT('Ctrl Pts',(14.5792147191394,14.5322203603309,4.65390799865534));
#127517=CARTESIAN_POINT('Ctrl Pts',(14.5777762731377,14.5128697541313,4.66484703435202));
#127518=CARTESIAN_POINT('Ctrl Pts',(14.5769386255146,14.501624274912,4.67150859096992));
#127519=CARTESIAN_POINT('Ctrl Pts',(14.5736219373558,14.457255414414,4.69902208360296));
#127520=CARTESIAN_POINT('Ctrl Pts',(14.5712064497555,14.4252750890677,4.72164977927811));
#127521=CARTESIAN_POINT('Ctrl Pts',(14.5664464018773,14.3642607584039,4.77063712231256));
#127522=CARTESIAN_POINT('Ctrl Pts',(14.5641060511043,14.3352829038458,4.7969453683536));
#127523=CARTESIAN_POINT('Ctrl Pts',(14.5592268717289,14.278871373715,4.854774045929));
#127524=CARTESIAN_POINT('Ctrl Pts',(14.5566899910943,14.2517280401488,4.88645994979635));
#127525=CARTESIAN_POINT('Ctrl Pts',(14.5533592993974,14.2202763431769,4.92837797760429));
#127526=CARTESIAN_POINT('Ctrl Pts',(14.5526700346192,14.2139796722366,4.93706773094576));
#127527=CARTESIAN_POINT('Ctrl Pts',(14.5515911953127,14.2044759999329,4.95065370560499));
#127528=CARTESIAN_POINT('Ctrl Pts',(14.5512079122834,14.2011664297671,4.95547754070249));
#127529=CARTESIAN_POINT('Ctrl Pts',(14.5504848886374,14.1950526914254,4.96456426501141));
#127530=CARTESIAN_POINT('Ctrl Pts',(14.5501458129865,14.1922381766586,4.96881977839053));
#127531=CARTESIAN_POINT('Ctrl Pts',(14.5493172244318,14.1854854581694,4.97920758696076));
#127532=CARTESIAN_POINT('Ctrl Pts',(14.5488255691205,14.1815827254473,4.98536242537818));
#127533=CARTESIAN_POINT('Ctrl Pts',(14.5469711567296,14.1672353732425,5.00856500997365));
#127534=CARTESIAN_POINT('Ctrl Pts',(14.5455846230981,14.1572514370523,5.02589029574184));
#127535=CARTESIAN_POINT('Ctrl Pts',(14.5416753705875,14.1309579236532,5.07497584409133));
#127536=CARTESIAN_POINT('Ctrl Pts',(14.539119511168,14.1158596103938,5.10734847516064));
#127537=CARTESIAN_POINT('Ctrl Pts',(14.5349381316765,14.094136932669,5.16157142395839));
#127538=CARTESIAN_POINT('Ctrl Pts',(14.5333130107176,14.0864333917894,5.18295443030695));
#127539=CARTESIAN_POINT('Ctrl Pts',(14.5283691455784,14.0651672292543,5.24922053192097));
#127540=CARTESIAN_POINT('Ctrl Pts',(14.5250962434043,14.0541074190835,5.29483917715732));
#127541=CARTESIAN_POINT('Ctrl Pts',(14.5209959470131,14.0441465257483,5.35461181805245));
#127542=CARTESIAN_POINT('Ctrl Pts',(14.5200767952742,14.0421804495769,5.36818448974565));
#127543=CARTESIAN_POINT('Ctrl Pts',(14.5186120224877,14.0394824416279,5.39008482047922));
#127544=CARTESIAN_POINT('Ctrl Pts',(14.5180609006384,14.0385686284797,5.39838773804601));
#127545=CARTESIAN_POINT('Ctrl Pts',(14.5169589273949,14.0369471206663,5.4151112500359));
#127546=CARTESIAN_POINT('Ctrl Pts',(14.516408200888,14.0362419895932,5.42353135916073));
#127547=CARTESIAN_POINT('Ctrl Pts',(14.5151899372806,14.0349185707578,5.4422885572769));
#127548=CARTESIAN_POINT('Ctrl Pts',(14.5145241424782,14.0343557906081,5.45262859988518));
#127549=CARTESIAN_POINT('Ctrl Pts',(14.5130663179659,14.0334812575654,5.47544717241359));
#127550=CARTESIAN_POINT('Ctrl Pts',(14.5122765758975,14.0332448196436,5.48792679808038));
#127551=CARTESIAN_POINT('Ctrl Pts',(14.5114930218304,14.0332500860612,5.50040792073653));
#127552=CARTESIAN_POINT('Ctrl Pts',(14.4551338463912,14.0332500192795,5.50019307209264));
#127553=CARTESIAN_POINT('Ctrl Pts',(14.4557159012467,14.0332482657504,5.49141280673769));
#127554=CARTESIAN_POINT('Ctrl Pts',(14.4562942528936,14.0333661289407,5.48263269314337));
#127555=CARTESIAN_POINT('Ctrl Pts',(14.4574635793255,14.0338492876714,5.46477361229857));
#127556=CARTESIAN_POINT('Ctrl Pts',(14.4580542373397,14.034222986886,5.45569574024463));
#127557=CARTESIAN_POINT('Ctrl Pts',(14.4595354630645,14.0354890840162,5.4327989780009));
#127558=CARTESIAN_POINT('Ctrl Pts',(14.4604207967587,14.0365505226987,5.41899123835604));
#127559=CARTESIAN_POINT('Ctrl Pts',(14.4650053873969,14.0436467522466,5.34696613391879));
#127560=CARTESIAN_POINT('Ctrl Pts',(14.4685476779816,14.0546624594865,5.2893607311592));
#127561=CARTESIAN_POINT('Ctrl Pts',(14.4757658684554,14.0877605023073,5.17413416999683));
#127562=CARTESIAN_POINT('Ctrl Pts',(14.479426002587,14.1102705154676,5.11692170777077));
#127563=CARTESIAN_POINT('Ctrl Pts',(14.483965621619,14.1425127685023,5.05343691195598));
#127564=CARTESIAN_POINT('Ctrl Pts',(14.4846011352322,14.147115545359,5.04470774992328));
#127565=CARTESIAN_POINT('Ctrl Pts',(14.4856025939995,14.1544887193919,5.0312287888832));
#127566=CARTESIAN_POINT('Ctrl Pts',(14.4859632321623,14.1571675212422,5.02642932608613));
#127567=CARTESIAN_POINT('Ctrl Pts',(14.4866555699781,14.1623511374431,5.01732542404476));
#127568=CARTESIAN_POINT('Ctrl Pts',(14.4869868289616,14.1648485199009,5.01301708039379));
#127569=CARTESIAN_POINT('Ctrl Pts',(14.4878107610462,14.1711046219397,5.00241406197519));
#127570=CARTESIAN_POINT('Ctrl Pts',(14.4883057356817,14.1749018322251,4.99614256077822));
#127571=CARTESIAN_POINT('Ctrl Pts',(14.4902692504298,14.1901304906588,4.97162461667665));
#127572=CARTESIAN_POINT('Ctrl Pts',(14.4917657964724,14.2020981350885,4.95372018681841));
#127573=CARTESIAN_POINT('Ctrl Pts',(14.4961702948044,14.2385962620791,4.90287711021017));
#127574=CARTESIAN_POINT('Ctrl Pts',(14.4991211079901,14.2646398645396,4.8710829498318));
#127575=CARTESIAN_POINT('Ctrl Pts',(14.5061953170165,14.3320353697439,4.79873554605297));
#127576=CARTESIAN_POINT('Ctrl Pts',(14.510285943358,14.3751670120194,4.76004449787031));
#127577=CARTESIAN_POINT('Ctrl Pts',(14.5153187040557,14.4343689216037,4.71582855177125));
#127578=CARTESIAN_POINT('Ctrl Pts',(14.516400641743,14.4474714974782,4.70654194660089));
#127579=CARTESIAN_POINT('Ctrl Pts',(14.5181056704665,14.4687134886681,4.69226792451271));
#127580=CARTESIAN_POINT('Ctrl Pts',(14.5187365154515,14.4767054256657,4.68706749218021));
#127581=CARTESIAN_POINT('Ctrl Pts',(14.5199338244367,14.4921227089064,4.67735690435418));
#127582=CARTESIAN_POINT('Ctrl Pts',(14.5205009648824,14.4995344255461,4.67282696943287));
#127583=CARTESIAN_POINT('Ctrl Pts',(14.5218103802034,14.5168932448561,4.6625362522747));
#127584=CARTESIAN_POINT('Ctrl Pts',(14.5225499023867,14.526884154408,4.65685168556305));
#127585=CARTESIAN_POINT('Ctrl Pts',(14.5250292573993,14.5609821559958,4.63824780755595));
#127586=CARTESIAN_POINT('Ctrl Pts',(14.5267403140545,14.5855362681686,4.62617305998854));
#127587=CARTESIAN_POINT('Ctrl Pts',(14.5311224474528,14.6505720098178,4.5975502014663));
#127588=CARTESIAN_POINT('Ctrl Pts',(14.5337490469884,14.6917221508466,4.58267748243849));
#127589=CARTESIAN_POINT('Ctrl Pts',(14.5395743864789,14.7847373792455,4.55602862925647));
#127590=CARTESIAN_POINT('Ctrl Pts',(14.5427652566447,14.836846771476,4.54564175129847));
#127591=CARTESIAN_POINT('Ctrl Pts',(14.5468001361465,14.8998548988134,4.53839489916365));
#127592=CARTESIAN_POINT('Ctrl Pts',(14.5474676877465,14.9101898745843,4.53737466675388));
#127593=CARTESIAN_POINT('Ctrl Pts',(14.548512639153,14.9261882144473,4.53605523187129));
#127594=CARTESIAN_POINT('Ctrl Pts',(14.5488841207593,14.9318414667097,4.53563901667661));
#127595=CARTESIAN_POINT('Ctrl Pts',(14.5495835673948,14.9424139890842,4.53495405114045));
#127596=CARTESIAN_POINT('Ctrl Pts',(14.5499108904544,14.9473321502888,4.5346731510154));
#127597=CARTESIAN_POINT('Ctrl Pts',(14.5507065417269,14.9592192347822,4.53408532927657));
#127598=CARTESIAN_POINT('Ctrl Pts',(14.5511768112331,14.9661896320437,4.5338162317592));
#127599=CARTESIAN_POINT('Ctrl Pts',(14.5529151395704,14.9917750737023,4.53310568110659));
#127600=CARTESIAN_POINT('Ctrl Pts',(14.5542039680372,15.0103978073792,4.53312665888173));
#127601=CARTESIAN_POINT('Ctrl Pts',(14.5577476100555,15.0609540829293,4.53464425953279));
#127602=CARTESIAN_POINT('Ctrl Pts',(14.5600301234813,15.0928325337556,4.53718692109876));
#127603=CARTESIAN_POINT('Ctrl Pts',(14.5674990162854,15.1962873302107,4.55062462628029));
#127604=CARTESIAN_POINT('Ctrl Pts',(14.5726644261818,15.2667892039884,4.56797572184593));
#127605=CARTESIAN_POINT('Ctrl Pts',(14.5786123827311,15.3489033941455,4.59827878527939));
#127606=CARTESIAN_POINT('Ctrl Pts',(14.579630627688,15.3629809491717,4.60385291308143));
#127607=CARTESIAN_POINT('Ctrl Pts',(14.5812601175737,15.3855300777399,4.61340003716616));
#127608=CARTESIAN_POINT('Ctrl Pts',(14.5818779547303,15.3940846158589,4.61716917772784));
#127609=CARTESIAN_POINT('Ctrl Pts',(14.5830658599349,15.4105350766351,4.62470404567787));
#127610=CARTESIAN_POINT('Ctrl Pts',(14.5836363872476,15.4184371663903,4.62845401565536));
#127611=CARTESIAN_POINT('Ctrl Pts',(14.5849768638616,15.4369975247548,4.63757254426081));
#127612=CARTESIAN_POINT('Ctrl Pts',(14.5857436224197,15.447609568049,4.64303229492802));
#127613=CARTESIAN_POINT('Ctrl Pts',(14.5884575631631,15.4851102835891,4.66321261214065));
#127614=CARTESIAN_POINT('Ctrl Pts',(14.5903675005709,15.5113978943296,4.67901426358274));
#127615=CARTESIAN_POINT('Ctrl Pts',(14.5953389059958,15.578742943513,4.72398791356286));
#127616=CARTESIAN_POINT('Ctrl Pts',(14.5983422152116,15.6183475668038,4.75516134902374));
#127617=CARTESIAN_POINT('Ctrl Pts',(14.6038990812618,15.6860108712211,4.8175525768507));
#127618=CARTESIAN_POINT('Ctrl Pts',(14.6064373574725,15.7148105584246,4.84778028997057));
#127619=CARTESIAN_POINT('Ctrl Pts',(14.6097623376094,15.7483675553722,4.88790199022174));
#127620=CARTESIAN_POINT('Ctrl Pts',(14.6104434347544,15.7550350304846,4.89614566936446));
#127621=CARTESIAN_POINT('Ctrl Pts',(14.611504992425,15.7650840915549,4.90899701496086));
#127622=CARTESIAN_POINT('Ctrl Pts',(14.6118792284899,15.7685628582689,4.91352807022952));
#127623=CARTESIAN_POINT('Ctrl Pts',(14.6125804643426,15.7749581463652,4.92201248536826));
#127624=CARTESIAN_POINT('Ctrl Pts',(14.612906768711,15.7778849985179,4.92595764914075));
#127625=CARTESIAN_POINT('Ctrl Pts',(14.6136951202583,15.7848408067519,4.93548440557271));
#127626=CARTESIAN_POINT('Ctrl Pts',(14.614159018699,15.7888403838212,4.94108695626274));
#127627=CARTESIAN_POINT('Ctrl Pts',(14.6158444974217,15.8030494123182,4.96144710578652));
#127628=CARTESIAN_POINT('Ctrl Pts',(14.6170853162429,15.8129067507068,4.9764447485323));
#127629=CARTESIAN_POINT('Ctrl Pts',(14.6204480868898,15.8381711372003,5.0173186496646));
#127630=CARTESIAN_POINT('Ctrl Pts',(14.6225948515494,15.8527959785939,5.04365476593296));
#127631=CARTESIAN_POINT('Ctrl Pts',(14.6301976509346,15.8999830525677,5.13884489829768));
#127632=CARTESIAN_POINT('Ctrl Pts',(14.6356427312191,15.9256280953443,5.21083030648119));
#127633=CARTESIAN_POINT('Ctrl Pts',(14.6418039581923,15.9458104016349,5.29934583783434));
#127634=CARTESIAN_POINT('Ctrl Pts',(14.6427865455595,15.9487374722334,5.31367593675688));
#127635=CARTESIAN_POINT('Ctrl Pts',(14.6443737348601,15.9529823288549,5.33716363010445));
#127636=CARTESIAN_POINT('Ctrl Pts',(14.6449843084876,15.9544957307331,5.34628301196179));
#127637=CARTESIAN_POINT('Ctrl Pts',(14.6461678317978,15.95719323404,5.36411768773545));
#127638=CARTESIAN_POINT('Ctrl Pts',(14.6467411093006,15.9583896561407,5.37283017084212));
#127639=CARTESIAN_POINT('Ctrl Pts',(14.6481033879374,15.9609660470993,5.39370082847558));
#127640=CARTESIAN_POINT('Ctrl Pts',(14.6488888923635,15.962234425322,5.40587141970355));
#127641=CARTESIAN_POINT('Ctrl Pts',(14.6517815828048,15.9660854818773,5.45114552820237));
#127642=CARTESIAN_POINT('Ctrl Pts',(14.6538442387805,15.9671935734666,5.48435279840596));
#127643=CARTESIAN_POINT('Ctrl Pts',(14.6598091123436,15.9654237582607,5.58180581490235));
#127644=CARTESIAN_POINT('Ctrl Pts',(14.6636037643855,15.9578535960652,5.64577815765663));
#127645=CARTESIAN_POINT('Ctrl Pts',(14.6693117446593,15.9377319730729,5.73686899247888));
#127646=CARTESIAN_POINT('Ctrl Pts',(14.6711148826084,15.9301979215612,5.76491448124882));
#127647=CARTESIAN_POINT('Ctrl Pts',(14.6735043371278,15.9189299611452,5.80040089062594));
#127648=CARTESIAN_POINT('Ctrl Pts',(14.6740359025913,15.9163457797879,5.80819372108466));
#127649=CARTESIAN_POINT('Ctrl Pts',(14.6748764519703,15.9121460387369,5.82033842157776));
#127650=CARTESIAN_POINT('Ctrl Pts',(14.675181735813,15.9105977838248,5.8247133724245));
#127651=CARTESIAN_POINT('Ctrl Pts',(14.6758259784563,15.9072843803776,5.83386607760869));
#127652=CARTESIAN_POINT('Ctrl Pts',(14.6761653252999,15.905512880837,5.83864128992218));
#127653=CARTESIAN_POINT('Ctrl Pts',(14.6770386651027,15.9008851741584,5.85081965484903));
#127654=CARTESIAN_POINT('Ctrl Pts',(14.6775755743344,15.8979754398581,5.85820193569529));
#127655=CARTESIAN_POINT('Ctrl Pts',(14.6800175767679,15.884437799348,5.89134635985226));
#127656=CARTESIAN_POINT('Ctrl Pts',(14.6819697987547,15.872790597227,5.9166755171201));
#127657=CARTESIAN_POINT('Ctrl Pts',(14.689109918682,15.8268024962347,6.00627028080881));
#127658=CARTESIAN_POINT('Ctrl Pts',(14.6943907107138,15.7863146418972,6.06711833970452));
#127659=CARTESIAN_POINT('Ctrl Pts',(14.701377771157,15.7216688968061,6.14385932824967));
#127660=CARTESIAN_POINT('Ctrl Pts',(14.703261944121,15.7030737018993,6.16411478350293));
#127661=CARTESIAN_POINT('Ctrl Pts',(14.7058247355717,15.6761417083022,6.19105020445264));
#127662=CARTESIAN_POINT('Ctrl Pts',(14.706532875664,15.6685213505722,6.19842480885201));
#127663=CARTESIAN_POINT('Ctrl Pts',(14.7078169050663,15.6543800455728,6.21166650507075));
#127664=CARTESIAN_POINT('Ctrl Pts',(14.7083944155844,15.6478977234032,6.21757299764084));
#127665=CARTESIAN_POINT('Ctrl Pts',(14.7095651813831,15.6345107927995,6.22944143597547));
#127666=CARTESIAN_POINT('Ctrl Pts',(14.710158079161,15.6276003635259,6.23539550424442));
#127667=CARTESIAN_POINT('Ctrl Pts',(14.7116513684583,15.6098708426011,6.25023940366577));
#127668=CARTESIAN_POINT('Ctrl Pts',(14.7125463587244,15.5989407745463,6.25899379929153));
#127669=CARTESIAN_POINT('Ctrl Pts',(14.7174033083303,15.5380465800803,6.30563183241361));
#127670=CARTESIAN_POINT('Ctrl Pts',(14.7211824159237,15.4846770430772,6.33882422675857));
#127671=CARTESIAN_POINT('Ctrl Pts',(14.7283344787804,15.3781693045675,6.3914826904229));
#127672=CARTESIAN_POINT('Ctrl Pts',(14.7316991174617,15.3258115969497,6.41192033966295));
#127673=CARTESIAN_POINT('Ctrl Pts',(14.7359168818552,15.2622411376113,6.43055803270327));
#127674=CARTESIAN_POINT('Ctrl Pts',(14.7365699982163,15.252453310958,6.43326093514765));
#127675=CARTESIAN_POINT('Ctrl Pts',(14.7375969941586,15.2371873302122,6.43721891303761));
#127676=CARTESIAN_POINT('Ctrl Pts',(14.7379652636439,15.2317374444656,6.43858130900884));
#127677=CARTESIAN_POINT('Ctrl Pts',(14.7386623784725,15.221474396713,6.44105209599221));
#127678=CARTESIAN_POINT('Ctrl Pts',(14.7389906395166,15.2166641389722,6.44217121705684));
#127679=CARTESIAN_POINT('Ctrl Pts',(14.7397936848036,15.204947506812,6.44480266017057));
#127680=CARTESIAN_POINT('Ctrl Pts',(14.7402705064242,15.1980328122773,6.44627614641491));
#127681=CARTESIAN_POINT('Ctrl Pts',(14.7420657915134,15.1721325136019,6.45149906326037));
#127682=CARTESIAN_POINT('Ctrl Pts',(14.7434067537731,15.1530529724865,6.45475376161493));
#127683=CARTESIAN_POINT('Ctrl Pts',(14.7471538836816,15.1001484395617,6.46215207725746));
#127684=CARTESIAN_POINT('Ctrl Pts',(14.7495911485891,15.0661824292158,6.46508341685769));
#127685=CARTESIAN_POINT('Ctrl Pts',(14.7569322804306,14.9637293019913,6.46849079877257));
#127686=CARTESIAN_POINT('Ctrl Pts',(14.7618075388576,14.8952648637467,6.46349543267255));
#127687=CARTESIAN_POINT('Ctrl Pts',(14.7675260069024,14.8125533357465,6.44853168723102));
#127688=CARTESIAN_POINT('Ctrl Pts',(14.7685755823343,14.7972809606664,6.44538545153537));
#127689=CARTESIAN_POINT('Ctrl Pts',(14.7702421680797,14.7728953674135,6.43974364925108));
#127690=CARTESIAN_POINT('Ctrl Pts',(14.7708663356886,14.7637315276876,6.43748165849733));
#127691=CARTESIAN_POINT('Ctrl Pts',(14.7720584679983,14.7461760629583,6.43287451330997));
#127692=CARTESIAN_POINT('Ctrl Pts',(14.7726270019202,14.7377801782427,6.43054941933844));
#127693=CARTESIAN_POINT('Ctrl Pts',(14.7739507486897,14.7181851831991,6.42483665532532));
#127694=CARTESIAN_POINT('Ctrl Pts',(14.7747030032042,14.7070137287492,6.42135850441716));
#127695=CARTESIAN_POINT('Ctrl Pts',(14.7772893928943,14.6685210105139,6.40860312307736));
#127696=CARTESIAN_POINT('Ctrl Pts',(14.7790910270293,14.6415526442626,6.39830600372744));
#127697=CARTESIAN_POINT('Ctrl Pts',(14.7838239786133,14.5710000785529,6.36768316142892));
#127698=CARTESIAN_POINT('Ctrl Pts',(14.786699852823,14.5284044492095,6.34528864055014));
#127699=CARTESIAN_POINT('Ctrl Pts',(14.7923937280301,14.4482914393166,6.29522154189329));
#127700=CARTESIAN_POINT('Ctrl Pts',(14.7952041116426,14.4107598617516,6.26782469489093));
#127701=CARTESIAN_POINT('Ctrl Pts',(14.798825981993,14.3672804095238,6.23101513923496));
#127702=CARTESIAN_POINT('Ctrl Pts',(14.7995048468504,14.3593286917441,6.22405625977445));
#127703=CARTESIAN_POINT('Ctrl Pts',(14.8005636588418,14.3472619004382,6.21314170038985));
#127704=CARTESIAN_POINT('Ctrl Pts',(14.8009374319884,14.3430648764696,6.2092773441921));
#127705=CARTESIAN_POINT('Ctrl Pts',(14.8016383620152,14.3353163936808,6.20201525729485));
#127706=CARTESIAN_POINT('Ctrl Pts',(14.8019648323866,14.3317562701737,6.19862724776633));
#127707=CARTESIAN_POINT('Ctrl Pts',(14.8027543665008,14.3232612522442,6.19041858379502));
#127708=CARTESIAN_POINT('Ctrl Pts',(14.8032192960369,14.3183519161801,6.18557205067067));
#127709=CARTESIAN_POINT('Ctrl Pts',(14.8049131101738,14.3007856258145,6.16785526842038));
#127710=CARTESIAN_POINT('Ctrl Pts',(14.8061614693273,14.2884385929593,6.1546844059523));
#127711=CARTESIAN_POINT('Ctrl Pts',(14.809552233321,14.2563097125978,6.11842878111755));
#127712=CARTESIAN_POINT('Ctrl Pts',(14.8117198883546,14.2372360730487,6.09474398093096));
#127713=CARTESIAN_POINT('Ctrl Pts',(14.8193008655827,14.1747571118368,6.00920115099284));
#127714=CARTESIAN_POINT('Ctrl Pts',(14.8247014641308,14.1374981619209,5.94317728032089));
#127715=CARTESIAN_POINT('Ctrl Pts',(14.830829231318,14.1026231417896,5.85991208247549));
#127716=CARTESIAN_POINT('Ctrl Pts',(14.8318177769152,14.0972506323274,5.84621604777781));
#127717=CARTESIAN_POINT('Ctrl Pts',(14.8334120657391,14.0890082139625,5.82370557210395));
#127718=CARTESIAN_POINT('Ctrl Pts',(14.8340238820166,14.0859489460937,5.81496350975598));
#127719=CARTESIAN_POINT('Ctrl Pts',(14.8352081690579,14.0802331754215,5.79784515952652));
#127720=CARTESIAN_POINT('Ctrl Pts',(14.8357809898768,14.0775643267897,5.78947398464046));
#127721=CARTESIAN_POINT('Ctrl Pts',(14.8371395329623,14.0714678942418,5.76941068086777));
#127722=CARTESIAN_POINT('Ctrl Pts',(14.8379218122652,14.0681464402074,5.75768769972735));
#127723=CARTESIAN_POINT('Ctrl Pts',(14.8395761523705,14.0615377959022,5.73256100977512));
#127724=CARTESIAN_POINT('Ctrl Pts',(14.8404461779773,14.0583141926738,5.7191433310388));
#127725=CARTESIAN_POINT('Ctrl Pts',(14.845648774081,14.0406118807541,5.63783476903828));
#127726=CARTESIAN_POINT('Ctrl Pts',(14.8497692954516,14.0331928278937,5.56861699671362));
#127727=CARTESIAN_POINT('Ctrl Pts',(14.8539665691581,14.033250331692,5.49919917142664));
#127728=CARTESIAN_POINT('Origin',(16.125,15.,5.5));
#127729=CARTESIAN_POINT('',(15.3122364200794,14.0332501750868,5.50058183360759));
#127730=CARTESIAN_POINT('',(15.2539186838427,14.0332502815979,5.50073788408625));
#127731=CARTESIAN_POINT('',(16.125,14.03325,5.5));
#127732=CARTESIAN_POINT('Ctrl Pts',(15.3128321466295,14.0332501978693,5.50061853078022));
#127733=CARTESIAN_POINT('Ctrl Pts',(15.3115187040417,14.0332638396951,5.52194039987235));
#127734=CARTESIAN_POINT('Ctrl Pts',(15.3101876143888,14.0339828660901,5.54325476764825));
#127735=CARTESIAN_POINT('Ctrl Pts',(15.3083790219664,14.0358729530645,5.57150927105893));
#127736=CARTESIAN_POINT('Ctrl Pts',(15.3079288180362,14.0364158523844,5.57848644909956));
#127737=CARTESIAN_POINT('Ctrl Pts',(15.3071453680829,14.0374835322328,5.59051753162644));
#127738=CARTESIAN_POINT('Ctrl Pts',(15.3068138862805,14.0379725046415,5.59557441990132));
#127739=CARTESIAN_POINT('Ctrl Pts',(15.306156146715,14.039015099918,5.60553648913005));
#127740=CARTESIAN_POINT('Ctrl Pts',(15.3058300085175,14.0395664581816,5.61044156497212));
#127741=CARTESIAN_POINT('Ctrl Pts',(15.3051079721908,14.0408618432062,5.62122136784803));
#127742=CARTESIAN_POINT('Ctrl Pts',(15.3047112602944,14.0416222809291,5.6270935364513));
#127743=CARTESIAN_POINT('Ctrl Pts',(15.3035651261934,14.0439593190561,5.64392486281022));
#127744=CARTESIAN_POINT('Ctrl Pts',(15.3028091909319,14.0456702614042,5.65486405339201));
#127745=CARTESIAN_POINT('Ctrl Pts',(15.2983855678006,14.0566730876314,5.71808044788869));
#127746=CARTESIAN_POINT('Ctrl Pts',(15.2945699991171,14.07007083561,5.76954720982888));
#127747=CARTESIAN_POINT('Ctrl Pts',(15.2883795028949,14.0986762662122,5.85119564355005));
#127748=CARTESIAN_POINT('Ctrl Pts',(15.2859971059405,14.1113575208729,5.88214870315479));
#127749=CARTESIAN_POINT('Ctrl Pts',(15.2812617651042,14.1401358777695,5.94316777095965));
#127750=CARTESIAN_POINT('Ctrl Pts',(15.2789134700689,14.1562710933651,5.97316589341539));
#127751=CARTESIAN_POINT('Ctrl Pts',(15.2757712375708,14.1804831742435,6.01298687661458));
#127752=CARTESIAN_POINT('Ctrl Pts',(15.2749316322307,14.1872182451739,6.02359259654184));
#127753=CARTESIAN_POINT('Ctrl Pts',(15.2734983980139,14.1991710494237,6.04162799799324));
#127754=CARTESIAN_POINT('Ctrl Pts',(15.2729012825498,14.2042900859759,6.04912078665659));
#127755=CARTESIAN_POINT('Ctrl Pts',(15.2716807686209,14.2150374634005,6.06438589252334));
#127756=CARTESIAN_POINT('Ctrl Pts',(15.2710578969236,14.2206775625385,6.0721487295442));
#127757=CARTESIAN_POINT('Ctrl Pts',(15.2694496980913,14.235637224425,6.09210695476351));
#127758=CARTESIAN_POINT('Ctrl Pts',(15.2684711943613,14.245133475394,6.1041669215372));
#127759=CARTESIAN_POINT('Ctrl Pts',(15.2629625348449,14.3007436687247,6.17143099904223));
#127760=CARTESIAN_POINT('Ctrl Pts',(15.2586755591041,14.3526170486515,6.22157835515635));
#127761=CARTESIAN_POINT('Ctrl Pts',(15.2517457763976,14.4435331535795,6.29170016046074));
#127762=CARTESIAN_POINT('Ctrl Pts',(15.2491403377796,14.4791910352566,6.31559902256754));
#127763=CARTESIAN_POINT('Ctrl Pts',(15.2457139439915,14.5259039493217,6.3425919521112));
#127764=CARTESIAN_POINT('Ctrl Pts',(15.2450027918963,14.5355889408296,6.34796851752898));
#127765=CARTESIAN_POINT('Ctrl Pts',(15.2439010976513,14.5505319641898,6.35593127250696));
#127766=CARTESIAN_POINT('Ctrl Pts',(15.2435174260375,14.5557250091717,6.35863821644771));
#127767=CARTESIAN_POINT('Ctrl Pts',(15.2427943175024,14.56548390062,6.36361293959962));
#127768=CARTESIAN_POINT('Ctrl Pts',(15.2424555554474,14.5700435867575,6.36589204176814));
#127769=CARTESIAN_POINT('Ctrl Pts',(15.2416285914776,14.581148132739,6.37133317894235));
#127770=CARTESIAN_POINT('Ctrl Pts',(15.2411382647219,14.5877109347826,6.3744576115256));
#127771=CARTESIAN_POINT('Ctrl Pts',(15.2393872358782,14.6110937954121,6.38526804429975));
#127772=CARTESIAN_POINT('Ctrl Pts',(15.2381066469615,14.6280975515904,6.39254468642281));
#127773=CARTESIAN_POINT('Ctrl Pts',(15.2325441423059,14.701940794573,6.42166899836418));
#127774=CARTESIAN_POINT('Ctrl Pts',(15.2281351401414,14.7605661354887,6.43860771142775));
#127775=CARTESIAN_POINT('Ctrl Pts',(15.2216090235543,14.8508778384536,6.45568329931842));
#127776=CARTESIAN_POINT('Ctrl Pts',(15.2194300351935,14.8816225354205,6.45997658592658));
#127777=CARTESIAN_POINT('Ctrl Pts',(15.2157619620799,14.9345858496299,6.46478875885003));
#127778=CARTESIAN_POINT('Ctrl Pts',(15.2142546488528,14.9567126562855,6.46603452202677));
#127779=CARTESIAN_POINT('Ctrl Pts',(15.2120405778929,14.9897492895735,6.46675696293682));
#127780=CARTESIAN_POINT('Ctrl Pts',(15.2113166874645,15.0006378908934,6.46681110448699));
#127781=CARTESIAN_POINT('Ctrl Pts',(15.2100691471211,15.0195473747028,6.46658565207274));
#127782=CARTESIAN_POINT('Ctrl Pts',(15.2095429880161,15.02756797352,6.46639015718251));
#127783=CARTESIAN_POINT('Ctrl Pts',(15.2083575996848,15.0457346205461,6.46572100170452));
#127784=CARTESIAN_POINT('Ctrl Pts',(15.2077002665615,15.0558776006124,6.46518724347849));
#127785=CARTESIAN_POINT('Ctrl Pts',(15.2059108829298,15.0836585950152,6.4632858934019));
#127786=CARTESIAN_POINT('Ctrl Pts',(15.2047887247483,15.1012708838623,6.46159385452689));
#127787=CARTESIAN_POINT('Ctrl Pts',(15.1990713239709,15.1917177073616,6.45039167419396));
#127788=CARTESIAN_POINT('Ctrl Pts',(15.1947180110117,15.2633402485568,6.43308762765077));
#127789=CARTESIAN_POINT('Ctrl Pts',(15.1879918923192,15.3676629205402,6.394900222755));
#127790=CARTESIAN_POINT('Ctrl Pts',(15.1856893642871,15.4022212976442,6.37990903033206));
#127791=CARTESIAN_POINT('Ctrl Pts',(15.1826265938316,15.4451842621796,6.35821135318109));
#127792=CARTESIAN_POINT('Ctrl Pts',(15.1819515987372,15.4544761783783,6.35332709802575));
#127793=CARTESIAN_POINT('Ctrl Pts',(15.1808942376215,15.4687222803984,6.34554001992032));
#127794=CARTESIAN_POINT('Ctrl Pts',(15.180517914238,15.4737335205734,6.34274257569455));
#127795=CARTESIAN_POINT('Ctrl Pts',(15.1797994870259,15.4831815477642,6.33735747055257));
#127796=CARTESIAN_POINT('Ctrl Pts',(15.1794579141628,15.4876230909291,6.33477880771696));
#127797=CARTESIAN_POINT('Ctrl Pts',(15.1786917750274,15.4974770424425,6.32895234884509));
#127798=CARTESIAN_POINT('Ctrl Pts',(15.1782661551395,15.5028785969426,6.32568669363078));
#127799=CARTESIAN_POINT('Ctrl Pts',(15.1767365279009,15.5220468193235,6.31384017546189));
#127800=CARTESIAN_POINT('Ctrl Pts',(15.1756169167759,15.5356283090814,6.30496643302873));
#127801=CARTESIAN_POINT('Ctrl Pts',(15.1691365325615,15.6120399606369,6.2522512593837));
#127802=CARTESIAN_POINT('Ctrl Pts',(15.1635541137289,15.6697063774724,6.20140518916088));
#127803=CARTESIAN_POINT('Ctrl Pts',(15.1556708014497,15.7444309020794,6.11780977981688));
#127804=CARTESIAN_POINT('Ctrl Pts',(15.1532173907206,15.7666198071558,6.0900515812407));
#127805=CARTESIAN_POINT('Ctrl Pts',(15.1499635952347,15.7946161493953,6.05077448259291));
#127806=CARTESIAN_POINT('Ctrl Pts',(15.1491130743593,15.8017942561891,6.04027155402949));
#127807=CARTESIAN_POINT('Ctrl Pts',(15.1476672079899,15.8137484842671,6.02201702099355));
#127808=CARTESIAN_POINT('Ctrl Pts',(15.14706821163,15.8186260840331,6.01433423938282));
#127809=CARTESIAN_POINT('Ctrl Pts',(15.1458489345443,15.8283960603813,5.99845423969093));
#127810=CARTESIAN_POINT('Ctrl Pts',(15.1452291127318,15.8332769713166,5.99025112090035));
#127811=CARTESIAN_POINT('Ctrl Pts',(15.143639827844,15.8455615270486,5.96889138662987));
#127812=CARTESIAN_POINT('Ctrl Pts',(15.1426768750275,15.8527800934401,5.95563096839243));
#127813=CARTESIAN_POINT('Ctrl Pts',(15.1370604225208,15.8934553924482,5.87655484565393));
#127814=CARTESIAN_POINT('Ctrl Pts',(15.1326665494928,15.9195942117416,5.80725164799159));
#127815=CARTESIAN_POINT('Ctrl Pts',(15.1256897907898,15.9477537718199,5.69520915942276));
#127816=CARTESIAN_POINT('Ctrl Pts',(15.1231528619947,15.9552888987025,5.65416303838326));
#127817=CARTESIAN_POINT('Ctrl Pts',(15.1198086302791,15.9614283904363,5.60188692141483));
#127818=CARTESIAN_POINT('Ctrl Pts',(15.1191053099038,15.9625208066296,5.59098993250991));
#127819=CARTESIAN_POINT('Ctrl Pts',(15.118013209201,15.9639108358018,5.57426617935566));
#127820=CARTESIAN_POINT('Ctrl Pts',(15.1176311161427,15.9643412369382,5.56845099934459));
#127821=CARTESIAN_POINT('Ctrl Pts',(15.1169090801069,15.9650497320371,5.55753814918427));
#127822=CARTESIAN_POINT('Ctrl Pts',(15.1165697816303,15.9653400933337,5.55244161788744));
#127823=CARTESIAN_POINT('Ctrl Pts',(15.1157388347372,15.9659484926609,5.5400329799026));
#127824=CARTESIAN_POINT('Ctrl Pts',(15.1152450093898,15.966223874153,5.53271921514453));
#127825=CARTESIAN_POINT('Ctrl Pts',(15.1134684198291,15.9669105107585,5.50659754613027));
#127826=CARTESIAN_POINT('Ctrl Pts',(15.112165056105,15.9668557794016,5.48778267660359));
#127827=CARTESIAN_POINT('Ctrl Pts',(15.1070213867429,15.9645020198274,5.41445796172126));
#127828=CARTESIAN_POINT('Ctrl Pts',(15.103081557505,15.9581398280082,5.3601806381725));
#127829=CARTESIAN_POINT('Ctrl Pts',(15.0967378311562,15.9403384593363,5.2729341326345));
#127830=CARTESIAN_POINT('Ctrl Pts',(15.0943046223575,15.9316384624109,5.23952838127793));
#127831=CARTESIAN_POINT('Ctrl Pts',(15.0902749733644,15.913961005331,5.18401679659159));
#127832=CARTESIAN_POINT('Ctrl Pts',(15.0886548438555,15.9059187776485,5.1616489492879));
#127833=CARTESIAN_POINT('Ctrl Pts',(15.0863122829395,15.8928998164517,5.12924401333605));
#127834=CARTESIAN_POINT('Ctrl Pts',(15.0855696324456,15.8885607021878,5.11896197060088));
#127835=CARTESIAN_POINT('Ctrl Pts',(15.0842506818744,15.8804757800673,5.10069345267799));
#127836=CARTESIAN_POINT('Ctrl Pts',(15.0836722360708,15.8767969287001,5.09267890754575));
#127837=CARTESIAN_POINT('Ctrl Pts',(15.082429290043,15.8686056626878,5.07545926848846));
#127838=CARTESIAN_POINT('Ctrl Pts',(15.0817661513036,15.8640554272843,5.06627328713382));
#127839=CARTESIAN_POINT('Ctrl Pts',(15.0799420589107,15.8510462098436,5.04102799096384));
#127840=CARTESIAN_POINT('Ctrl Pts',(15.0787916716643,15.842279575443,5.02513145226642));
#127841=CARTESIAN_POINT('Ctrl Pts',(15.0723122670322,15.7898213633755,4.9360376525949));
#127842=CARTESIAN_POINT('Ctrl Pts',(15.0673232111859,15.7370519080608,4.86863218129446));
#127843=CARTESIAN_POINT('Ctrl Pts',(15.0603111804128,15.6551531066365,4.78849366376793));
#127844=CARTESIAN_POINT('Ctrl Pts',(15.0584879480145,15.6332549899201,4.76893594634241));
#127845=CARTESIAN_POINT('Ctrl Pts',(15.0560773584071,15.6041438666722,4.74522650533729));
#127846=CARTESIAN_POINT('Ctrl Pts',(15.0555460661274,15.597718613909,4.74012811094686));
#127847=CARTESIAN_POINT('Ctrl Pts',(15.0546651201179,15.5870673348336,4.73189507147508));
#127848=CARTESIAN_POINT('Ctrl Pts',(15.0543186587826,15.5828790296137,4.72871193978219));
#127849=CARTESIAN_POINT('Ctrl Pts',(15.0536505535982,15.5748089187273,4.72268189211238));
#127850=CARTESIAN_POINT('Ctrl Pts',(15.0533293378125,15.5709314564826,4.71982950359688));
#127851=CARTESIAN_POINT('Ctrl Pts',(15.0524295618524,15.5600726717527,4.71196572568825));
#127852=CARTESIAN_POINT('Ctrl Pts',(15.0518470585849,15.5530457714742,4.70701842554861));
#127853=CARTESIAN_POINT('Ctrl Pts',(15.0490234461091,15.5189554020508,4.68369055142465));
#127854=CARTESIAN_POINT('Ctrl Pts',(15.0467188459707,15.4910386608113,4.66659946174765));
#127855=CARTESIAN_POINT('Ctrl Pts',(15.0400845651691,15.4091899059507,4.62203195702067));
#127856=CARTESIAN_POINT('Ctrl Pts',(15.0357198800467,15.3534649020903,4.59815310887772));
#127857=CARTESIAN_POINT('Ctrl Pts',(15.0292075009051,15.26496571232,4.56970291212749));
#127858=CARTESIAN_POINT('Ctrl Pts',(15.0269712323874,15.2335756724448,4.5613295048864));
#127859=CARTESIAN_POINT('Ctrl Pts',(15.0239489083797,15.1897113268647,4.55196598554933));
#127860=CARTESIAN_POINT('Ctrl Pts',(15.0231217250932,15.177553012943,4.54961385137285));
#127861=CARTESIAN_POINT('Ctrl Pts',(15.02170280573,15.1564402375478,4.54594872547178));
#127862=CARTESIAN_POINT('Ctrl Pts',(15.0211077682847,15.1475065810969,4.54452671407416));
#127863=CARTESIAN_POINT('Ctrl Pts',(15.0198854750664,15.1289972334731,4.54184629424673));
#127864=CARTESIAN_POINT('Ctrl Pts',(15.0192588271024,15.1194199769279,4.54060556072871));
#127865=CARTESIAN_POINT('Ctrl Pts',(15.0176273001013,15.0942690734407,4.53772973175266));
#127866=CARTESIAN_POINT('Ctrl Pts',(15.0166296378564,15.0786711503579,4.53632909129133));
#127867=CARTESIAN_POINT('Ctrl Pts',(15.011269537487,14.9938627887962,4.53078662344062));
#127868=CARTESIAN_POINT('Ctrl Pts',(15.0071290071239,14.9243940946235,4.53372002828192));
#127869=CARTESIAN_POINT('Ctrl Pts',(15.0009454308747,14.8230145011772,4.54900936861542));
#127870=CARTESIAN_POINT('Ctrl Pts',(14.9989350347673,14.7904755410969,4.55564504470598));
#127871=CARTESIAN_POINT('Ctrl Pts',(14.9960491627224,14.7455579781982,4.56724107661652));
#127872=CARTESIAN_POINT('Ctrl Pts',(14.9952193504079,14.7328411236088,4.57080354413752));
#127873=CARTESIAN_POINT('Ctrl Pts',(14.9937300057537,14.7104633526326,4.57756973114395));
#127874=CARTESIAN_POINT('Ctrl Pts',(14.9930751978536,14.7007724033555,4.58066768950022));
#127875=CARTESIAN_POINT('Ctrl Pts',(14.9920426312248,14.6857570868489,4.58573027222678));
#127876=CARTESIAN_POINT('Ctrl Pts',(14.9916704730272,14.6803977851802,4.58758991458406));
#127877=CARTESIAN_POINT('Ctrl Pts',(14.9909582270133,14.6702481069535,4.59121217865941));
#127878=CARTESIAN_POINT('Ctrl Pts',(14.9906186381051,14.6654548183314,4.59296574939043));
#127879=CARTESIAN_POINT('Ctrl Pts',(14.9897659496777,14.6535285212784,4.59743624132784));
#127880=CARTESIAN_POINT('Ctrl Pts',(14.9892503045753,14.6464134727812,4.60019980945992));
#127881=CARTESIAN_POINT('Ctrl Pts',(14.9872860892301,14.6196474496576,4.6109625204421));
#127882=CARTESIAN_POINT('Ctrl Pts',(14.985811097909,14.6002300986498,4.61952309002513));
#127883=CARTESIAN_POINT('Ctrl Pts',(14.9802232581377,14.5286638553669,4.65393003468471));
#127884=CARTESIAN_POINT('Ctrl Pts',(14.9760134215237,14.4786005077096,4.68382918436755));
#127885=CARTESIAN_POINT('Ctrl Pts',(14.968652902069,14.3947067747054,4.7448190749534));
#127886=CARTESIAN_POINT('Ctrl Pts',(14.9654782581637,14.3598167515312,4.77415943030465));
#127887=CARTESIAN_POINT('Ctrl Pts',(14.9614817512756,14.3173890120216,4.81528728728529));
#127888=CARTESIAN_POINT('Ctrl Pts',(14.9605735723496,14.3078563922139,4.82492480625402));
#127889=CARTESIAN_POINT('Ctrl Pts',(14.9590603694239,14.2921662457343,4.84146948247668));
#127890=CARTESIAN_POINT('Ctrl Pts',(14.9584508006636,14.2858997376889,4.84827007783757));
#127891=CARTESIAN_POINT('Ctrl Pts',(14.9572340344631,14.2735056373434,4.86211393900355));
#127892=CARTESIAN_POINT('Ctrl Pts',(14.956626978591,14.2673805664822,4.86915813286785));
#127893=CARTESIAN_POINT('Ctrl Pts',(14.9551183803638,14.2523152344109,4.88699957353619));
#127894=CARTESIAN_POINT('Ctrl Pts',(14.9542220666886,14.2435058161574,4.89790481424447));
#127895=CARTESIAN_POINT('Ctrl Pts',(14.950008530195,14.2028438979122,4.9505424864222));
#127896=CARTESIAN_POINT('Ctrl Pts',(14.9468130005764,14.1741869395769,4.99463371501952));
#127897=CARTESIAN_POINT('Ctrl Pts',(14.9407566682124,14.1265046941246,5.08298099063761));
#127898=CARTESIAN_POINT('Ctrl Pts',(14.9378978596329,14.1069237497955,5.1267531216575));
#127899=CARTESIAN_POINT('Ctrl Pts',(14.9334956103003,14.0827088315208,5.19384314020128));
#127900=CARTESIAN_POINT('Ctrl Pts',(14.9320265113891,14.0755555474625,5.21617367668182));
#127901=CARTESIAN_POINT('Ctrl Pts',(14.9300236955881,14.0671460194274,5.24613391511602));
#127902=CARTESIAN_POINT('Ctrl Pts',(14.9295252595741,14.0651589059166,5.25355191618772));
#127903=CARTESIAN_POINT('Ctrl Pts',(14.928683711039,14.0619840548635,5.26599507709466));
#127904=CARTESIAN_POINT('Ctrl Pts',(14.9283432209048,14.0607477792286,5.27100768150966));
#127905=CARTESIAN_POINT('Ctrl Pts',(14.9276236281917,14.0582371400365,5.28154983310003));
#127906=CARTESIAN_POINT('Ctrl Pts',(14.9272441229189,14.0569712273344,5.28708102523874));
#127907=CARTESIAN_POINT('Ctrl Pts',(14.926176787709,14.05357027302,5.30256651822618));
#127908=CARTESIAN_POINT('Ctrl Pts',(14.9254835499426,14.051543739425,5.31254357874149));
#127909=CARTESIAN_POINT('Ctrl Pts',(14.9207115794005,14.0387995091024,5.38079479053979));
#127910=CARTESIAN_POINT('Ctrl Pts',(14.9164398917085,14.033302170455,5.43991149677583));
#127911=CARTESIAN_POINT('Ctrl Pts',(14.9122050445523,14.0332503695571,5.49915469624611));
#127912=CARTESIAN_POINT('Ctrl Pts',(14.8539665810176,14.0332503318545,5.49919897528513));
#127913=CARTESIAN_POINT('Ctrl Pts',(14.8558549326386,14.0332762091239,5.46796792693476));
#127914=CARTESIAN_POINT('Ctrl Pts',(14.8577581847734,14.0348154625899,5.43675845838677));
#127915=CARTESIAN_POINT('Ctrl Pts',(14.8605946150658,14.0392314940276,5.3917112377512));
#127916=CARTESIAN_POINT('Ctrl Pts',(14.8614847410138,14.0409049080245,5.37777423204118));
#127917=CARTESIAN_POINT('Ctrl Pts',(14.8627517596201,14.0436733221221,5.35830839272474));
#127918=CARTESIAN_POINT('Ctrl Pts',(14.8631166435777,14.0445142291266,5.35274456016862));
#127919=CARTESIAN_POINT('Ctrl Pts',(14.8637821071157,14.0461252016181,5.34268099238523));
#127920=CARTESIAN_POINT('Ctrl Pts',(14.8640818186184,14.0468786680796,5.33817872286671));
#127921=CARTESIAN_POINT('Ctrl Pts',(14.8647099688217,14.048514859091,5.32880989749035));
#127922=CARTESIAN_POINT('Ctrl Pts',(14.8650387425845,14.0494030701827,5.3239446190901));
#127923=CARTESIAN_POINT('Ctrl Pts',(14.8657702516262,14.0514497993923,5.31320069712283));
#127924=CARTESIAN_POINT('Ctrl Pts',(14.8661738854635,14.0526257151797,5.30732560453291));
#127925=CARTESIAN_POINT('Ctrl Pts',(14.8675880700547,14.0569091543951,5.28691263633314));
#127926=CARTESIAN_POINT('Ctrl Pts',(14.8686117796016,14.0602971917482,5.27243650363474));
#127927=CARTESIAN_POINT('Ctrl Pts',(14.8735956716226,14.0782115819465,5.20313613859358));
#127928=CARTESIAN_POINT('Ctrl Pts',(14.8776924171568,14.0972093275343,5.14958512720541));
#127929=CARTESIAN_POINT('Ctrl Pts',(14.8853234017605,14.1416662074297,5.05235147699662));
#127930=CARTESIAN_POINT('Ctrl Pts',(14.8888576076852,14.1660695181915,5.00838298236998));
#127931=CARTESIAN_POINT('Ctrl Pts',(14.8924482469444,14.1951529194408,4.96443215744462));
#127932=CARTESIAN_POINT('Ctrl Pts',(14.8926172683426,14.1965321741247,4.96236518896761));
#127933=CARTESIAN_POINT('Ctrl Pts',(14.893120764164,14.2006713364915,4.95621369059276));
#127934=CARTESIAN_POINT('Ctrl Pts',(14.8934544166077,14.2034545619316,4.95214488304287));
#127935=CARTESIAN_POINT('Ctrl Pts',(14.89382996039,14.2066328046397,4.9475740209656));
#127936=CARTESIAN_POINT('Ctrl Pts',(14.8938729491642,14.2069972975998,4.94705092189678));
#127937=CARTESIAN_POINT('Ctrl Pts',(14.8947431350746,14.2143891381514,4.93646492411304));
#127938=CARTESIAN_POINT('Ctrl Pts',(14.8955632878081,14.2216072298334,4.92653602848337));
#127939=CARTESIAN_POINT('Ctrl Pts',(14.8969592621612,14.2343223843272,4.90972819327763));
#127940=CARTESIAN_POINT('Ctrl Pts',(14.8975384804261,14.2397277714504,4.90278214696305));
#127941=CARTESIAN_POINT('Ctrl Pts',(14.898717838094,14.2509967323547,4.88870227065746));
#127942=CARTESIAN_POINT('Ctrl Pts',(14.8993175475896,14.2568691797244,4.88157668026877));
#127943=CARTESIAN_POINT('Ctrl Pts',(14.9008533157214,14.2722677981187,4.8634282310708));
#127944=CARTESIAN_POINT('Ctrl Pts',(14.9017833109925,14.2819428466171,4.85253437608647));
#127945=CARTESIAN_POINT('Ctrl Pts',(14.9075433867644,14.3439653721751,4.78579968115972));
#127946=CARTESIAN_POINT('Ctrl Pts',(14.9120878973818,14.4025421757983,4.73612260574871));
#127947=CARTESIAN_POINT('Ctrl Pts',(14.9185202179851,14.4913208750057,4.67735392864183));
#127948=CARTESIAN_POINT('Ctrl Pts',(14.9203403558027,14.5170251371223,4.6620047304029));
#127949=CARTESIAN_POINT('Ctrl Pts',(14.9233214216175,14.5591543194831,4.63943030916546));
#127950=CARTESIAN_POINT('Ctrl Pts',(14.9244522587349,14.5751407195806,4.63142668193206));
#127951=CARTESIAN_POINT('Ctrl Pts',(14.9260507683635,14.5975689097484,4.62096527824274));
#127952=CARTESIAN_POINT('Ctrl Pts',(14.9264982660378,14.6038298230795,4.61812585432861));
#127953=CARTESIAN_POINT('Ctrl Pts',(14.9272721788027,14.6146148636183,4.61337269141147));
#127954=CARTESIAN_POINT('Ctrl Pts',(14.9275966852868,14.6191242007814,4.61142624836499));
#127955=CARTESIAN_POINT('Ctrl Pts',(14.9283035821782,14.6289158871917,4.60728792616736));
#127956=CARTESIAN_POINT('Ctrl Pts',(14.9286866130523,14.6342029060707,4.60510852746667));
#127957=CARTESIAN_POINT('Ctrl Pts',(14.9297887897135,14.6493722954778,4.59901233268742));
#127958=CARTESIAN_POINT('Ctrl Pts',(14.9305139615139,14.6593000403027,4.5952115832427));
#127959=CARTESIAN_POINT('Ctrl Pts',(14.934158868369,14.7090324736193,4.57710648399116));
#127960=CARTESIAN_POINT('Ctrl Pts',(14.9371745209061,14.7496804682625,4.5652625658698));
#127961=CARTESIAN_POINT('Ctrl Pts',(14.9429112311599,14.8279256677443,4.54793448615564));
#127962=CARTESIAN_POINT('Ctrl Pts',(14.9456253764104,14.8653323927021,4.54192736048103));
#127963=CARTESIAN_POINT('Ctrl Pts',(14.951135891985,14.942939007336,4.53410079947701));
#127964=CARTESIAN_POINT('Ctrl Pts',(14.9539216891916,14.9830979306594,4.53256408050875));
#127965=CARTESIAN_POINT('Ctrl Pts',(14.9575056111915,15.036150698145,4.53383984075792));
#127966=CARTESIAN_POINT('Ctrl Pts',(14.9583699522567,15.0490536486216,4.53440894116425));
#127967=CARTESIAN_POINT('Ctrl Pts',(14.9598175113917,15.0708365814087,4.53580749674134));
#127968=CARTESIAN_POINT('Ctrl Pts',(14.9604047868712,15.0797232129623,4.53650157094055));
#127969=CARTESIAN_POINT('Ctrl Pts',(14.9615816840999,15.09762498287,4.53814913865886));
#127970=CARTESIAN_POINT('Ctrl Pts',(14.9621711181229,15.1066388471809,4.53910672698923));
#127971=CARTESIAN_POINT('Ctrl Pts',(14.9636426450116,15.1292510942968,4.54183105936492));
#127972=CARTESIAN_POINT('Ctrl Pts',(14.9645196651774,15.1428280879056,4.54376063091443));
#127973=CARTESIAN_POINT('Ctrl Pts',(14.9686771474817,15.2075664959849,4.55437097514698));
#127974=CARTESIAN_POINT('Ctrl Pts',(14.9718380269747,15.258016882701,4.56687285525153));
#127975=CARTESIAN_POINT('Ctrl Pts',(14.9773168223527,15.3441311709988,4.59573543590412));
#127976=CARTESIAN_POINT('Ctrl Pts',(14.979644635833,15.3802558777713,4.61032254342958));
#127977=CARTESIAN_POINT('Ctrl Pts',(14.9839861422621,15.4445451444208,4.64091511863044));
#127978=CARTESIAN_POINT('Ctrl Pts',(14.9859832988042,15.4729728670161,4.65623257557793));
#127979=CARTESIAN_POINT('Ctrl Pts',(14.98858287211,15.5076312366802,4.67720959325779));
#127980=CARTESIAN_POINT('Ctrl Pts',(14.9891165686507,15.5146288374633,4.68156816124849));
#127981=CARTESIAN_POINT('Ctrl Pts',(14.9899929972897,15.5259113205249,4.68879753698097));
#127982=CARTESIAN_POINT('Ctrl Pts',(14.9903323911074,15.5302306453159,4.69161419281713));
#127983=CARTESIAN_POINT('Ctrl Pts',(14.9910201754643,15.5388786346381,4.69735272189946));
#127984=CARTESIAN_POINT('Ctrl Pts',(14.9913686041748,15.5432065504057,4.7002753746579));
#127985=CARTESIAN_POINT('Ctrl Pts',(14.9922934473557,15.5545605967957,4.70807747736854));
#127986=CARTESIAN_POINT('Ctrl Pts',(14.9928734340796,15.5615458428177,4.71301525328606));
#127987=CARTESIAN_POINT('Ctrl Pts',(14.9959086467107,15.5974523716931,4.73911851733851));
#127988=CARTESIAN_POINT('Ctrl Pts',(14.9984409206017,15.6252434408736,4.7617858653979));
#127989=CARTESIAN_POINT('Ctrl Pts',(15.0051685527126,15.6949028932764,4.82536283210728));
#127990=CARTESIAN_POINT('Ctrl Pts',(15.0093832253419,15.7344342735321,4.8686264048768));
#127991=CARTESIAN_POINT('Ctrl Pts',(15.0149946989902,15.7829243606754,4.93245728888567));
#127992=CARTESIAN_POINT('Ctrl Pts',(15.0164950713777,15.7954513642682,4.95015227267371));
#127993=CARTESIAN_POINT('Ctrl Pts',(15.0191426873818,15.8167800563305,4.98253661041792));
#127994=CARTESIAN_POINT('Ctrl Pts',(15.0202972161193,15.8258062453848,4.99706647843543));
#127995=CARTESIAN_POINT('Ctrl Pts',(15.022087731005,15.839361098514,5.02023612097309));
#127996=CARTESIAN_POINT('Ctrl Pts',(15.0227328918443,15.8441523102461,5.02871736499166));
#127997=CARTESIAN_POINT('Ctrl Pts',(15.0239415550327,15.8529481199525,5.04485206504839));
#127998=CARTESIAN_POINT('Ctrl Pts',(15.0245059636964,15.8569798869569,5.05248953158339));
#127999=CARTESIAN_POINT('Ctrl Pts',(15.0257871429126,15.8659538671048,5.07005531497917));
#128000=CARTESIAN_POINT('Ctrl Pts',(15.0265015513066,15.8708287222622,5.08001680419696));
#128001=CARTESIAN_POINT('Ctrl Pts',(15.0287868868942,15.8859878561271,5.11239301889865));
#128002=CARTESIAN_POINT('Ctrl Pts',(15.0303350964681,15.8955867052198,5.135118845976));
#128003=CARTESIAN_POINT('Ctrl Pts',(15.0366258561397,15.9315041825646,5.23014315551879));
#128004=CARTESIAN_POINT('Ctrl Pts',(15.0411387039992,15.9500153359253,5.30508204924268));
#128005=CARTESIAN_POINT('Ctrl Pts',(15.0475893202087,15.9629298487889,5.40957597345322));
#128006=CARTESIAN_POINT('Ctrl Pts',(15.0493543222572,15.9651682519459,5.43786835121357));
#128007=CARTESIAN_POINT('Ctrl Pts',(15.0516888492181,15.9664381607476,5.47418465962399));
#128008=CARTESIAN_POINT('Ctrl Pts',(15.052205584009,15.9666182087185,5.48215682133561));
#128009=CARTESIAN_POINT('Ctrl Pts',(15.053061313484,15.9667516940837,5.49523078718063));
#128010=CARTESIAN_POINT('Ctrl Pts',(15.0533972665399,15.9667633999231,5.50033182378754));
#128011=CARTESIAN_POINT('Ctrl Pts',(15.0540862309273,15.9667050099805,5.5107222964774));
#128012=CARTESIAN_POINT('Ctrl Pts',(15.0544393745736,15.9666318706065,5.5160114787546));
#128013=CARTESIAN_POINT('Ctrl Pts',(15.0553906227592,15.9663198904836,5.53016822416586));
#128014=CARTESIAN_POINT('Ctrl Pts',(15.0559926520036,15.9660024009317,5.5390333238352));
#128015=CARTESIAN_POINT('Ctrl Pts',(15.0599378396757,15.9631472154489,5.59659696446058));
#128016=CARTESIAN_POINT('Ctrl Pts',(15.063422369787,15.9570500258061,5.64504441845719));
#128017=CARTESIAN_POINT('Ctrl Pts',(15.070197412373,15.9381798347286,5.73775374878803));
#128018=CARTESIAN_POINT('Ctrl Pts',(15.0734786383384,15.9258479260395,5.78198307317516));
#128019=CARTESIAN_POINT('Ctrl Pts',(15.0788652705024,15.8999424193179,5.85451366478185));
#128020=CARTESIAN_POINT('Ctrl Pts',(15.0810082591409,15.8880495797593,5.88333352566741));
#128021=CARTESIAN_POINT('Ctrl Pts',(15.0839142169799,15.8696781507091,5.9223853191918));
#128022=CARTESIAN_POINT('Ctrl Pts',(15.0847151318455,15.8643702865876,5.93314370950165));
#128023=CARTESIAN_POINT('Ctrl Pts',(15.0860888627734,15.8548439365061,5.95157952656161));
#128024=CARTESIAN_POINT('Ctrl Pts',(15.086664795789,15.8507189134806,5.95930334555372));
#128025=CARTESIAN_POINT('Ctrl Pts',(15.0878466013729,15.8419852658515,5.97513506042166));
#128026=CARTESIAN_POINT('Ctrl Pts',(15.0884519249566,15.837363103714,5.98323447305798));
#128027=CARTESIAN_POINT('Ctrl Pts',(15.0900222162392,15.8249885746461,6.00420749910005));
#128028=CARTESIAN_POINT('Ctrl Pts',(15.0909805645968,15.8170518170708,6.01696974465591));
#128029=CARTESIAN_POINT('Ctrl Pts',(15.0965547845518,15.768699680378,6.09082256474307));
#128030=CARTESIAN_POINT('Ctrl Pts',(15.1009149472164,15.721745201398,6.14734487463986));
#128031=CARTESIAN_POINT('Ctrl Pts',(15.1072382475006,15.6460911361247,6.21983729270203));
#128032=CARTESIAN_POINT('Ctrl Pts',(15.1091517538356,15.6222759664719,6.24052134374049));
#128033=CARTESIAN_POINT('Ctrl Pts',(15.1122655312471,15.5829793705503,6.27141527928985));
#128034=CARTESIAN_POINT('Ctrl Pts',(15.1134323329086,15.5681411528647,6.28240782978899));
#128035=CARTESIAN_POINT('Ctrl Pts',(15.11507326176,15.547294198884,6.29694603670392));
#128036=CARTESIAN_POINT('Ctrl Pts',(15.1155257784418,15.541547393456,6.30086224746086));
#128037=CARTESIAN_POINT('Ctrl Pts',(15.1163053944488,15.5316618215477,6.30744380501268));
#128038=CARTESIAN_POINT('Ctrl Pts',(15.1166305044437,15.5275440873005,6.31014012715346));
#128039=CARTESIAN_POINT('Ctrl Pts',(15.1173350462375,15.5186341185695,6.31587770147371));
#128040=CARTESIAN_POINT('Ctrl Pts',(15.1177150697724,15.5138356432399,6.31890823693493));
#128041=CARTESIAN_POINT('Ctrl Pts',(15.1188001964196,15.5001473534116,6.32738557071843));
#128042=CARTESIAN_POINT('Ctrl Pts',(15.1195110558699,15.4911959980626,6.332730885825));
#128043=CARTESIAN_POINT('Ctrl Pts',(15.1237309887301,15.4380533847637,6.36331012224213));
#128044=CARTESIAN_POINT('Ctrl Pts',(15.1273810804493,15.3920148235246,6.38516591382389));
#128045=CARTESIAN_POINT('Ctrl Pts',(15.1342575143636,15.3022907154883,6.41938248701817));
#128046=CARTESIAN_POINT('Ctrl Pts',(15.1374773849574,15.2590283907437,6.43249599343638));
#128047=CARTESIAN_POINT('Ctrl Pts',(15.1425611810656,15.187837164456,6.44873560615895));
#128048=CARTESIAN_POINT('Ctrl Pts',(15.1444708147778,15.1604122611922,6.45375584555286));
#128049=CARTESIAN_POINT('Ctrl Pts',(15.1471220787523,15.1213517888635,6.45917310057196));
#128050=CARTESIAN_POINT('Ctrl Pts',(15.1478932630662,15.1098692356007,6.46055612229073));
#128051=CARTESIAN_POINT('Ctrl Pts',(15.1492330095174,15.0897167969318,6.46261727527569));
#128052=CARTESIAN_POINT('Ctrl Pts',(15.149804264225,15.0810576332602,6.46338506870814));
#128053=CARTESIAN_POINT('Ctrl Pts',(15.1509921116202,15.0629195479231,6.46474704979121));
#128054=CARTESIAN_POINT('Ctrl Pts',(15.1516079489227,15.0534398217715,6.46531856680731));
#128055=CARTESIAN_POINT('Ctrl Pts',(15.1532424665448,15.0280905710061,6.46647225414388));
#128056=CARTESIAN_POINT('Ctrl Pts',(15.154253446412,15.012212181767,6.46680329202504));
#128057=CARTESIAN_POINT('Ctrl Pts',(15.1609027458769,14.9066879660855,6.4664029256953));
#128058=CARTESIAN_POINT('Ctrl Pts',(15.1661386762117,14.8175337566911,6.45359706158965));
#128059=CARTESIAN_POINT('Ctrl Pts',(15.1734339440527,14.7029615484193,6.42046258289272));
#128060=CARTESIAN_POINT('Ctrl Pts',(15.1752738000915,14.6748986871526,6.41092919993062));
#128061=CARTESIAN_POINT('Ctrl Pts',(15.1776939620517,14.6398088291808,6.39718056825162));
#128062=CARTESIAN_POINT('Ctrl Pts',(15.1782165817196,14.6323344928509,6.39414356577471));
#128063=CARTESIAN_POINT('Ctrl Pts',(15.179079474914,14.6201803554466,6.38902689245148));
#128064=CARTESIAN_POINT('Ctrl Pts',(15.1794166047572,14.6154773288351,6.38700286987054));
#128065=CARTESIAN_POINT('Ctrl Pts',(15.1800620274693,14.6065652712186,6.38308322626607));
#128066=CARTESIAN_POINT('Ctrl Pts',(15.180369868567,14.602353321299,6.3811946363177));
#128067=CARTESIAN_POINT('Ctrl Pts',(15.1812209518324,14.5908101304022,6.37591919196636));
#128068=CARTESIAN_POINT('Ctrl Pts',(15.1817676460518,14.583507734283,6.37247060833897));
#128069=CARTESIAN_POINT('Ctrl Pts',(15.1841737987554,14.5518183394844,6.35701668932205));
#128070=CARTESIAN_POINT('Ctrl Pts',(15.1860774848475,14.5279024098573,6.34407820156081));
#128071=CARTESIAN_POINT('Ctrl Pts',(15.1926762531006,14.447954088701,6.29636499799892));
#128072=CARTESIAN_POINT('Ctrl Pts',(15.1974512250076,14.3949414675465,6.25687327661972));
#128073=CARTESIAN_POINT('Ctrl Pts',(15.2044301543389,14.3216413202208,6.18960909714398));
#128074=CARTESIAN_POINT('Ctrl Pts',(15.2067435746684,14.2981170208507,6.1656515019892));
#128075=CARTESIAN_POINT('Ctrl Pts',(15.2098325211374,14.2677512615314,6.13132243708263));
#128076=CARTESIAN_POINT('Ctrl Pts',(15.2106527486208,14.2597941505056,6.12197392083528));
#128077=CARTESIAN_POINT('Ctrl Pts',(15.2120488059361,14.24644116107,6.1056666537016));
#128078=CARTESIAN_POINT('Ctrl Pts',(15.2126280335836,14.2409584965958,6.09878128209072));
#128079=CARTESIAN_POINT('Ctrl Pts',(15.2137350816395,14.2305952992747,6.08539560753445));
#128080=CARTESIAN_POINT('Ctrl Pts',(15.2142633955932,14.2257012441749,6.07890677496729));
#128081=CARTESIAN_POINT('Ctrl Pts',(15.2156629134787,14.2128807085597,6.06145504961809));
#128082=CARTESIAN_POINT('Ctrl Pts',(15.2165285376058,14.2051013532032,6.05038597494936));
#128083=CARTESIAN_POINT('Ctrl Pts',(15.2202744839761,14.1721541455819,6.00134964794791));
#128084=CARTESIAN_POINT('Ctrl Pts',(15.2230656553926,14.1494538634748,5.96179234756547));
#128085=CARTESIAN_POINT('Ctrl Pts',(15.2287015850314,14.10891463461,5.8779374158332));
#128086=CARTESIAN_POINT('Ctrl Pts',(15.2315357052326,14.091395533674,5.83362776174672));
#128087=CARTESIAN_POINT('Ctrl Pts',(15.236310394775,14.0680976172899,5.75903257109432));
#128088=CARTESIAN_POINT('Ctrl Pts',(15.2382062936243,14.0603746270103,5.72944218633089));
#128089=CARTESIAN_POINT('Ctrl Pts',(15.2406904548279,14.0523879097482,5.6915803885933));
#128090=CARTESIAN_POINT('Ctrl Pts',(15.2412172162665,14.0508096788004,5.68360131419087));
#128091=CARTESIAN_POINT('Ctrl Pts',(15.2420851632927,14.048399878698,5.67055534588784));
#128092=CARTESIAN_POINT('Ctrl Pts',(15.2424231328278,14.0475076319733,5.66549985939347));
#128093=CARTESIAN_POINT('Ctrl Pts',(15.2431112989799,14.0457846563646,5.65526168066202));
#128094=CARTESIAN_POINT('Ctrl Pts',(15.2434615711857,14.0449557938717,5.6500788881891));
#128095=CARTESIAN_POINT('Ctrl Pts',(15.2443967277159,14.0428686250736,5.63630993516556));
#128096=CARTESIAN_POINT('Ctrl Pts',(15.2449853205082,14.0416836874877,5.62771334991782));
#128097=CARTESIAN_POINT('Ctrl Pts',(15.2482857692243,14.0357394374377,5.5798316231963));
#128098=CARTESIAN_POINT('Ctrl Pts',(15.2510914423754,14.0332804794478,5.54030229138642));
#128099=CARTESIAN_POINT('Ctrl Pts',(15.2539186841775,14.0332502815961,5.50073787940146));
#128100=CARTESIAN_POINT('Origin',(16.125,15.,5.5));
#128101=CARTESIAN_POINT('',(15.7122357911024,14.0332500106539,5.50014352462477));
#128102=CARTESIAN_POINT('',(15.6551382358657,14.0332501289961,5.49997318520408));
#128103=CARTESIAN_POINT('',(16.125,14.03325,5.5));
#128104=CARTESIAN_POINT('Ctrl Pts',(15.7122357911024,14.0332500106539,5.50014352462477));
#128105=CARTESIAN_POINT('Ctrl Pts',(15.7094099671659,14.0332564146756,5.5432795924672));
#128106=CARTESIAN_POINT('Ctrl Pts',(15.7065841432294,14.0361541789593,5.58634795534859));
#128107=CARTESIAN_POINT('Ctrl Pts',(15.7037583192929,14.0418907006428,5.62896562714666));
#128108=CARTESIAN_POINT('Ctrl Pts',(15.7009265505009,14.0476392905914,5.67167295629949));
#128109=CARTESIAN_POINT('Ctrl Pts',(15.698094781709,14.0562384428576,5.71392724228728));
#128110=CARTESIAN_POINT('Ctrl Pts',(15.695263012917,14.0675847152264,5.75535719927296));
#128111=CARTESIAN_POINT('Ctrl Pts',(15.6924211308671,14.0789715091871,5.79693511743532));
#128112=CARTESIAN_POINT('Ctrl Pts',(15.6895792488172,14.0931248786537,5.83768237429134));
#128113=CARTESIAN_POINT('Ctrl Pts',(15.6867373667672,14.1098920983802,5.87724459701101));
#128114=CARTESIAN_POINT('Ctrl Pts',(15.6853373489891,14.1181522602357,5.89673443303386));
#128115=CARTESIAN_POINT('Ctrl Pts',(15.683937331211,14.1270460641763,5.91593703186562));
#128116=CARTESIAN_POINT('Ctrl Pts',(15.6825373134329,14.1365512304826,5.93481235598685));
#128117=CARTESIAN_POINT('Ctrl Pts',(15.679865827169,14.1546888010333,5.97082987655267));
#128118=CARTESIAN_POINT('Ctrl Pts',(15.6771943409051,14.1751255833383,6.00579345392184));
#128119=CARTESIAN_POINT('Ctrl Pts',(15.6745228546412,14.1977155281612,6.03939335252336));
#128120=CARTESIAN_POINT('Ctrl Pts',(15.6718553725082,14.2202716142683,6.07294289024849));
#128121=CARTESIAN_POINT('Ctrl Pts',(15.6691878903751,14.2449741607053,6.10513230764752));
#128122=CARTESIAN_POINT('Ctrl Pts',(15.6665204082421,14.2716314227655,6.13567663021175));
#128123=CARTESIAN_POINT('Ctrl Pts',(15.6638556317917,14.2982616458102,6.1661899710342));
#128124=CARTESIAN_POINT('Ctrl Pts',(15.6611908553412,14.3268422802672,6.19506107808628));
#128125=CARTESIAN_POINT('Ctrl Pts',(15.6585260788908,14.3571403207815,6.22203669943783));
#128126=CARTESIAN_POINT('Ctrl Pts',(15.6558627144059,14.3874223074955,6.24899802741495));
#128127=CARTESIAN_POINT('Ctrl Pts',(15.653199349921,14.4194194621698,6.2740654698766));
#128128=CARTESIAN_POINT('Ctrl Pts',(15.6505359854361,14.4528630279837,6.29702364855303));
#128129=CARTESIAN_POINT('Ctrl Pts',(15.6478706894586,14.4863308473314,6.3199984766791));
#128130=CARTESIAN_POINT('Ctrl Pts',(15.6452053934811,14.5212466954558,6.34086064546375));
#128131=CARTESIAN_POINT('Ctrl Pts',(15.6425400975035,14.5573117999295,6.35943744392386));
#128132=CARTESIAN_POINT('Ctrl Pts',(15.6398739707978,14.5933881452929,6.37802003246119));
#128133=CARTESIAN_POINT('Ctrl Pts',(15.6372078440922,14.6306139278099,6.39431558677765));
#128134=CARTESIAN_POINT('Ctrl Pts',(15.6345417173865,14.6686683079245,6.40819869650116));
#128135=CARTESIAN_POINT('Ctrl Pts',(15.6318701892867,14.7067997836646,6.42210993247515));
#128136=CARTESIAN_POINT('Ctrl Pts',(15.6291986611868,14.7457626493866,6.43359878644248));
#128137=CARTESIAN_POINT('Ctrl Pts',(15.626527133087,14.785220543638,6.44258970269405));
#128138=CARTESIAN_POINT('Ctrl Pts',(15.6242183374809,14.8193209571353,6.45035985788643));
#128139=CARTESIAN_POINT('Ctrl Pts',(15.6219095418748,14.8537906613752,6.45626514772572));
#128140=CARTESIAN_POINT('Ctrl Pts',(15.6196007462687,14.8884094044249,6.46028803047794));
#128141=CARTESIAN_POINT('Ctrl Pts',(15.6169292600077,14.9284664351057,6.46494287128482));
#128142=CARTESIAN_POINT('Ctrl Pts',(15.6142577737468,14.9689073831686,6.46709775641789));
#128143=CARTESIAN_POINT('Ctrl Pts',(15.6115862874858,15.0093932329593,6.46670436518854));
#128144=CARTESIAN_POINT('Ctrl Pts',(15.6089188053556,15.0498184009337,6.46631156358975));
#128145=CARTESIAN_POINT('Ctrl Pts',(15.6062513232255,15.0902877576254,6.46337804032544));
#128146=CARTESIAN_POINT('Ctrl Pts',(15.6035838410953,15.1304578434037,6.45790725730336));
#128147=CARTESIAN_POINT('Ctrl Pts',(15.6009190646478,15.1705871838286,6.45244202341028));
#128148=CARTESIAN_POINT('Ctrl Pts',(15.5982542882002,15.210417276379,6.44444469806571));
#128149=CARTESIAN_POINT('Ctrl Pts',(15.5955895117527,15.2496084706341,6.43397064937166));
#128150=CARTESIAN_POINT('Ctrl Pts',(15.5929261472706,15.2887788989391,6.42350215048481));
#128151=CARTESIAN_POINT('Ctrl Pts',(15.5902627827886,15.3273105348896,6.41055967751139));
#128152=CARTESIAN_POINT('Ctrl Pts',(15.5875994183065,15.3648757042798,6.39524928535371));
#128153=CARTESIAN_POINT('Ctrl Pts',(15.5849341223318,15.4024681162237,6.37992778998027));
#128154=CARTESIAN_POINT('Ctrl Pts',(15.5822688263571,15.4390921149018,6.36223515721037));
#128155=CARTESIAN_POINT('Ctrl Pts',(15.5796035303823,15.4744391601403,6.34232597361434));
#128156=CARTESIAN_POINT('Ctrl Pts',(15.5769374036794,15.5097972224617,6.32241058465871));
#128157=CARTESIAN_POINT('Ctrl Pts',(15.5742712769765,15.5438770409738,6.30027757895607));
#128158=CARTESIAN_POINT('Ctrl Pts',(15.5716051502736,15.5763974500778,6.27612598335827));
#128159=CARTESIAN_POINT('Ctrl Pts',(15.5689336221764,15.6089837433537,6.2519254582445));
#128160=CARTESIAN_POINT('Ctrl Pts',(15.5662620940793,15.6400038623056,6.22569854672883));
#128161=CARTESIAN_POINT('Ctrl Pts',(15.5635905659821,15.6692097481378,6.1976846533337));
#128162=CARTESIAN_POINT('Ctrl Pts',(15.5612817703563,15.6944501420275,6.1734744065451));
#128163=CARTESIAN_POINT('Ctrl Pts',(15.5589729747304,15.7183359451346,6.14793029980389));
#128164=CARTESIAN_POINT('Ctrl Pts',(15.5566641791045,15.7407313988466,6.12122665530606));
#128165=CARTESIAN_POINT('Ctrl Pts',(15.5539926928445,15.7666449730963,6.09032811297994));
#128166=CARTESIAN_POINT('Ctrl Pts',(15.5513212065844,15.7906815336472,6.05773428587259));
#128167=CARTESIAN_POINT('Ctrl Pts',(15.5486497203244,15.8126143105961,6.02370177077642));
#128168=CARTESIAN_POINT('Ctrl Pts',(15.5459822381952,15.8345142138186,5.98972026498004));
#128169=CARTESIAN_POINT('Ctrl Pts',(15.543314756066,15.854316251522,5.95430482073426));
#128170=CARTESIAN_POINT('Ctrl Pts',(15.5406472739369,15.8718344621854,5.91774421964397));
#128171=CARTESIAN_POINT('Ctrl Pts',(15.5379824974903,15.8893349037631,5.88122070273224));
#128172=CARTESIAN_POINT('Ctrl Pts',(15.5353177210438,15.904555847848,5.84355485155328));
#128173=CARTESIAN_POINT('Ctrl Pts',(15.5326529445972,15.9173567825961,5.80506080693013));
#128174=CARTESIAN_POINT('Ctrl Pts',(15.5299895801162,15.9301509346069,5.76658715886398));
#128175=CARTESIAN_POINT('Ctrl Pts',(15.5273262156352,15.940527431882,5.72728674056244));
#128176=CARTESIAN_POINT('Ctrl Pts',(15.5246628511542,15.9483946844153,5.68749156000431));
#128177=CARTESIAN_POINT('Ctrl Pts',(15.5219975551806,15.9562676423413,5.64766751967154));
#128178=CARTESIAN_POINT('Ctrl Pts',(15.5193322592069,15.9616275970754,5.6073485735361));
#128179=CARTESIAN_POINT('Ctrl Pts',(15.5166669632333,15.9644340161173,5.56687743308424));
#128180=CARTESIAN_POINT('Ctrl Pts',(15.5140008365315,15.9672413098729,5.52639367845503));
#128181=CARTESIAN_POINT('Ctrl Pts',(15.5113347098296,15.9674934680987,5.48575822120119));
#128182=CARTESIAN_POINT('Ctrl Pts',(15.5086685831278,15.9652021295355,5.44531534365053));
#128183=CARTESIAN_POINT('Ctrl Pts',(15.5059970550318,15.9629061488739,5.40479053153749));
#128184=CARTESIAN_POINT('Ctrl Pts',(15.5033255269358,15.9580564395887,5.3644596626397));
#128185=CARTESIAN_POINT('Ctrl Pts',(15.5006539988398,15.9507165702229,5.32466156837791));
#128186=CARTESIAN_POINT('Ctrl Pts',(15.4983452032066,15.9443732873784,5.29026714580888));
#128187=CARTESIAN_POINT('Ctrl Pts',(15.4960364075735,15.9361710558104,5.25627072857965));
#128188=CARTESIAN_POINT('Ctrl Pts',(15.4937276119403,15.9261808322606,5.2228815624086));
#128189=CARTESIAN_POINT('Ctrl Pts',(15.4910561256672,15.9146212361253,5.18424726415616));
#128190=CARTESIAN_POINT('Ctrl Pts',(15.4883846393942,15.9006135505576,5.1462485987931));
#128191=CARTESIAN_POINT('Ctrl Pts',(15.4857131531211,15.884247409928,5.10921606924586));
#128192=CARTESIAN_POINT('Ctrl Pts',(15.4830456709788,15.8679057995266,5.07223904553962));
#128193=CARTESIAN_POINT('Ctrl Pts',(15.4803781888366,15.8492129552526,5.03622582607153));
#128194=CARTESIAN_POINT('Ctrl Pts',(15.4777107066943,15.8283078328668,5.00149052515366));
#128195=CARTESIAN_POINT('Ctrl Pts',(15.4750459302346,15.8074239149815,4.96679045697406));
#128196=CARTESIAN_POINT('Ctrl Pts',(15.472381153775,15.7843324571946,4.93336624305674));
#128197=CARTESIAN_POINT('Ctrl Pts',(15.4697163773154,15.7592185875527,4.90150797932261));
#128198=CARTESIAN_POINT('Ctrl Pts',(15.4670530128213,15.7341180248127,4.86966659609304));
#128199=CARTESIAN_POINT('Ctrl Pts',(15.4643896483272,15.706997533657,4.83938997890157));
#128200=CARTESIAN_POINT('Ctrl Pts',(15.4617262838331,15.6780840657846,4.81093718557081));
#128201=CARTESIAN_POINT('Ctrl Pts',(15.4590609878465,15.6491496296419,4.78246375805457));
#128202=CARTESIAN_POINT('Ctrl Pts',(15.4563956918599,15.6184200302807,4.75581721475183));
#128203=CARTESIAN_POINT('Ctrl Pts',(15.4537303958733,15.5861592338527,4.73121985257867));
#128204=CARTESIAN_POINT('Ctrl Pts',(15.4510642691587,15.5538883822751,4.70661482381985));
#128205=CARTESIAN_POINT('Ctrl Pts',(15.448398142444,15.5200858646421,4.68406058283007));
#128206=CARTESIAN_POINT('Ctrl Pts',(15.4457320157293,15.4850456458025,4.66373671371512));
#128207=CARTESIAN_POINT('Ctrl Pts',(15.4430604876207,15.4499344378296,4.64337166980436));
#128208=CARTESIAN_POINT('Ctrl Pts',(15.4403889595121,15.4135810415084,4.62524629374348));
#128209=CARTESIAN_POINT('Ctrl Pts',(15.4377174314035,15.3763034226429,4.609493797547));
#128210=CARTESIAN_POINT('Ctrl Pts',(15.435408635861,15.3440872539292,4.5958801309403));
#128211=CARTESIAN_POINT('Ctrl Pts',(15.4330998403186,15.3111813702823,4.5840380148832));
#128212=CARTESIAN_POINT('Ctrl Pts',(15.4307910447761,15.2777995621772,4.57402323692537));
#128213=CARTESIAN_POINT('Ctrl Pts',(15.4281195585274,15.2391737767107,4.56243522876013));
#128214=CARTESIAN_POINT('Ctrl Pts',(15.4254480722788,15.1997328148548,4.55324151762621));
#128215=CARTESIAN_POINT('Ctrl Pts',(15.4227765860301,15.1598020183826,4.54654896432965));
#128216=CARTESIAN_POINT('Ctrl Pts',(15.4201091039122,15.1199310717899,4.53986644210044));
#128217=CARTESIAN_POINT('Ctrl Pts',(15.4174416217942,15.0795723137171,4.53567776410846));
#128218=CARTESIAN_POINT('Ctrl Pts',(15.4147741396763,15.0390645168156,4.5340395836133));
#128219=CARTESIAN_POINT('Ctrl Pts',(15.4121093632409,14.9985978078139,4.53240306475864));
#128220=CARTESIAN_POINT('Ctrl Pts',(15.4094445868055,14.9579829410967,4.53331195070426));
#128221=CARTESIAN_POINT('Ctrl Pts',(15.4067798103701,14.9175640157947,4.53677112221025));
#128222=CARTESIAN_POINT('Ctrl Pts',(15.4041164459001,14.87716650697,4.54022846083059));
#128223=CARTESIAN_POINT('Ctrl Pts',(15.4014530814301,14.836965316024,4.54623335958583));
#128224=CARTESIAN_POINT('Ctrl Pts',(15.3987897169601,14.7973016141674,4.55473869915201));
#128225=CARTESIAN_POINT('Ctrl Pts',(15.3961244209971,14.7576091478806,4.56325020685768));
#128226=CARTESIAN_POINT('Ctrl Pts',(15.3934591250342,14.7184555246137,4.57426566442385));
#128227=CARTESIAN_POINT('Ctrl Pts',(15.3907938290712,14.680171563261,4.58768682265733));
#128228=CARTESIAN_POINT('Ctrl Pts',(15.3881277023799,14.6418756694357,4.60111216404211));
#128229=CARTESIAN_POINT('Ctrl Pts',(15.3854615756886,14.6044505216104,4.61694448124139));
#128230=CARTESIAN_POINT('Ctrl Pts',(15.3827954489973,14.5682077573255,4.63503698248647));
#128231=CARTESIAN_POINT('Ctrl Pts',(15.3801239209114,14.5318915676205,4.6531661379308));
#128232=CARTESIAN_POINT('Ctrl Pts',(15.3774523928255,14.4967630587329,4.67356433679313));
#128233=CARTESIAN_POINT('Ctrl Pts',(15.3747808647396,14.4631083325078,4.69603924232742));
#128234=CARTESIAN_POINT('Ctrl Pts',(15.3724720690303,14.4340231479225,4.71546257002381));
#128235=CARTESIAN_POINT('Ctrl Pts',(15.3701632733211,14.4060384251854,4.73643608570972));
#128236=CARTESIAN_POINT('Ctrl Pts',(15.3678544776119,14.37931831527,4.75881189382131));
#128237=CARTESIAN_POINT('Ctrl Pts',(15.3652184319464,14.3488108824808,4.7843592611125));
#128238=CARTESIAN_POINT('Ctrl Pts',(15.362582386281,14.3198040591793,4.81186000691865));
#128239=CARTESIAN_POINT('Ctrl Pts',(15.3599463406155,14.2925623556372,4.84110885433293));
#128240=CARTESIAN_POINT('Ctrl Pts',(15.3573142732769,14.2653617653438,4.87031355931191));
#128241=CARTESIAN_POINT('Ctrl Pts',(15.3546822059383,14.2399214422276,4.90126072057937));
#128242=CARTESIAN_POINT('Ctrl Pts',(15.3520501385997,14.216471745972,4.93370587356051));
#128243=CARTESIAN_POINT('Ctrl Pts',(15.3494206841004,14.1930453281058,4.96611881840993));
#128244=CARTESIAN_POINT('Ctrl Pts',(15.3467912296011,14.1716059838233,5.00002633051279));
#128245=CARTESIAN_POINT('Ctrl Pts',(15.3441617751018,14.1523439514045,5.03515079242886));
#128246=CARTESIAN_POINT('Ctrl Pts',(15.3415013288499,14.1328548893326,5.07068924463591));
#128247=CARTESIAN_POINT('Ctrl Pts',(15.3388408825981,14.1155951837442,5.10747301979994));
#128248=CARTESIAN_POINT('Ctrl Pts',(15.3361804363462,14.100715181879,5.14518684015803));
#128249=CARTESIAN_POINT('Ctrl Pts',(15.3335506383373,14.086006597088,5.1824661986926));
#128250=CARTESIAN_POINT('Ctrl Pts',(15.3309208403284,14.0736233230897,5.22065368630612));
#128251=CARTESIAN_POINT('Ctrl Pts',(15.3282910423195,14.0636614816181,5.25942622442494));
#128252=CARTESIAN_POINT('Ctrl Pts',(15.3256152719462,14.0535254939173,5.29887655804275));
#128253=CARTESIAN_POINT('Ctrl Pts',(15.3229395015728,14.0458966007295,5.33893197443122));
#128254=CARTESIAN_POINT('Ctrl Pts',(15.3202637311995,14.0408216861288,5.37924187522471));
#128255=CARTESIAN_POINT('Ctrl Pts',(15.3175879608261,14.0357467715282,5.4195517760182));
#128256=CARTESIAN_POINT('Ctrl Pts',(15.3149121904528,14.0332258206287,5.46011550819873));
#128257=CARTESIAN_POINT('Ctrl Pts',(15.3122364200794,14.0332501750868,5.50058183360759));
#128258=CARTESIAN_POINT('Ctrl Pts',(15.2539186841775,14.0332502815961,5.50073787940146));
#128259=CARTESIAN_POINT('Ctrl Pts',(15.2595175253243,14.0331904802114,5.42238771578732));
#128260=CARTESIAN_POINT('Ctrl Pts',(15.2651438586834,14.0426560102427,5.34430511256021));
#128261=CARTESIAN_POINT('Ctrl Pts',(15.271565093549,14.0652663824751,5.25275041137276));
#128262=CARTESIAN_POINT('Ctrl Pts',(15.2726381794736,14.0694672655116,5.23738207371249));
#128263=CARTESIAN_POINT('Ctrl Pts',(15.2743325847113,14.0767786539322,5.21301868091487));
#128264=CARTESIAN_POINT('Ctrl Pts',(15.2749614962956,14.0796452960216,5.20395412346234));
#128265=CARTESIAN_POINT('Ctrl Pts',(15.2761570694372,14.085387311679,5.18668753596458));
#128266=CARTESIAN_POINT('Ctrl Pts',(15.276724379512,14.0882404775814,5.1784791590938));
#128267=CARTESIAN_POINT('Ctrl Pts',(15.27803698782,14.0951400850736,5.15946026762035));
#128268=CARTESIAN_POINT('Ctrl Pts',(15.2787794827675,14.0992702753139,5.14868140367013));
#128269=CARTESIAN_POINT('Ctrl Pts',(15.2812841727986,14.1139675115272,5.11228931581595));
#128270=CARTESIAN_POINT('Ctrl Pts',(15.2830167148293,14.1254424768501,5.08705631314722));
#128271=CARTESIAN_POINT('Ctrl Pts',(15.2874793866644,14.1582192186663,5.02249798807187));
#128272=CARTESIAN_POINT('Ctrl Pts',(15.2901626456772,14.1811919509576,4.98409622350412));
#128273=CARTESIAN_POINT('Ctrl Pts',(15.2959559396889,14.2361896734283,4.90514370521323));
#128274=CARTESIAN_POINT('Ctrl Pts',(15.2990594701861,14.2689690534642,4.8652931613692));
#128275=CARTESIAN_POINT('Ctrl Pts',(15.3030003780523,14.3120236313532,4.82073327307412));
#128276=CARTESIAN_POINT('Ctrl Pts',(15.3036719877099,14.3194060763851,4.81333657408827));
#128277=CARTESIAN_POINT('Ctrl Pts',(15.3047218384011,14.3309841852592,4.80210626059355));
#128278=CARTESIAN_POINT('Ctrl Pts',(15.3050940666254,14.3350964201846,4.79818730595112));
#128279=CARTESIAN_POINT('Ctrl Pts',(15.3057938835754,14.3428349785455,4.79094153052705));
#128280=CARTESIAN_POINT('Ctrl Pts',(15.3061208141385,14.3464525298845,4.78760581235585));
#128281=CARTESIAN_POINT('Ctrl Pts',(15.3069139442854,14.3552364194114,4.77962946099534));
#128282=CARTESIAN_POINT('Ctrl Pts',(15.3073820555686,14.3604275142673,4.77501667815));
#128283=CARTESIAN_POINT('Ctrl Pts',(15.3091023901688,14.3795453598865,4.75839377318508));
#128284=CARTESIAN_POINT('Ctrl Pts',(15.3103748567058,14.3937635676673,4.74672644657944));
#128285=CARTESIAN_POINT('Ctrl Pts',(15.3138562153588,14.4330743508532,4.71630241881851));
#128286=CARTESIAN_POINT('Ctrl Pts',(15.3160918018314,14.4587597698188,4.69834832589819));
#128287=CARTESIAN_POINT('Ctrl Pts',(15.3236054598915,14.5476077030973,4.64246266708636));
#128288=CARTESIAN_POINT('Ctrl Pts',(15.3288656385872,14.6142334565252,4.61049629414746));
#128289=CARTESIAN_POINT('Ctrl Pts',(15.3348866777584,14.6980003878017,4.58150887271192));
#128290=CARTESIAN_POINT('Ctrl Pts',(15.3358933898418,14.7122614167875,4.57694189438178));
#128291=CARTESIAN_POINT('Ctrl Pts',(15.3375092098169,14.7355571417003,4.57007404361211));
#128292=CARTESIAN_POINT('Ctrl Pts',(15.3381247066906,14.7445286602044,4.56756945868733));
#128293=CARTESIAN_POINT('Ctrl Pts',(15.3393111473073,14.7620063289039,4.56296140818578));
#128294=CARTESIAN_POINT('Ctrl Pts',(15.3398825085595,14.7705076020362,4.56084316667103));
#128295=CARTESIAN_POINT('Ctrl Pts',(15.3412297070632,14.7907445399543,4.55609198365884));
#128296=CARTESIAN_POINT('Ctrl Pts',(15.3420022598421,14.8025030099882,4.55356186142754));
#128297=CARTESIAN_POINT('Ctrl Pts',(15.3447696829348,14.8451331349749,4.54521807193019));
#128298=CARTESIAN_POINT('Ctrl Pts',(15.3467252102816,14.8762378004628,4.54069010368549));
#128299=CARTESIAN_POINT('Ctrl Pts',(15.3514496561643,14.9529169220548,4.53332034134832));
#128300=CARTESIAN_POINT('Ctrl Pts',(15.3541789790425,14.9985759484482,4.5321753616651));
#128301=CARTESIAN_POINT('Ctrl Pts',(15.3598641700541,15.0927766311417,4.53648149448564));
#128302=CARTESIAN_POINT('Ctrl Pts',(15.3628155112691,15.1411638987668,4.54237428355098));
#128303=CARTESIAN_POINT('Ctrl Pts',(15.3664979756387,15.1975919734861,4.55361656136522));
#128304=CARTESIAN_POINT('Ctrl Pts',(15.3670708445496,15.2062642604029,4.55546877102017));
#128305=CARTESIAN_POINT('Ctrl Pts',(15.3679954241269,15.2200662570228,4.55861571081712));
#128306=CARTESIAN_POINT('Ctrl Pts',(15.3683430831841,15.2252131590899,4.55983375557463));
#128307=CARTESIAN_POINT('Ctrl Pts',(15.3690308380418,15.2353043623555,4.56230951467175));
#128308=CARTESIAN_POINT('Ctrl Pts',(15.3693707721161,15.240249170188,4.56356424595803));
#128309=CARTESIAN_POINT('Ctrl Pts',(15.3702475396231,15.2528993368111,4.56688097626477));
#128310=CARTESIAN_POINT('Ctrl Pts',(15.3707873323813,15.2605894086003,4.56899928191545));
#128311=CARTESIAN_POINT('Ctrl Pts',(15.3732688099982,15.2955360976485,4.57909257136174));
#128312=CARTESIAN_POINT('Ctrl Pts',(15.3752594338012,15.3224572591916,4.5881704660809));
#128313=CARTESIAN_POINT('Ctrl Pts',(15.3827472689139,15.4209004838652,4.62627076379622));
#128314=CARTESIAN_POINT('Ctrl Pts',(15.388341942421,15.4892823035855,4.66264371626222));
#128315=CARTESIAN_POINT('Ctrl Pts',(15.3953810119013,15.5726812983413,4.72074398337533));
#128316=CARTESIAN_POINT('Ctrl Pts',(15.3970502948583,15.5922139612932,4.73548276092965));
#128317=CARTESIAN_POINT('Ctrl Pts',(15.3994338596525,15.6197355960493,4.75793826128105));
#128318=CARTESIAN_POINT('Ctrl Pts',(15.4001700862239,15.628182909002,4.7650754576437));
#128319=CARTESIAN_POINT('Ctrl Pts',(15.4014707398241,15.6430036933045,4.77803993586671));
#128320=CARTESIAN_POINT('Ctrl Pts',(15.4020373695996,15.6494249200041,4.78381052429582));
#128321=CARTESIAN_POINT('Ctrl Pts',(15.4032370690625,15.6629387313244,4.79628625208128));
#128322=CARTESIAN_POINT('Ctrl Pts',(15.4038690925951,15.6700088488294,4.80301438019936));
#128323=CARTESIAN_POINT('Ctrl Pts',(15.4056027911921,15.6892525902552,4.82189075010275));
#128324=CARTESIAN_POINT('Ctrl Pts',(15.4066949683271,15.7012061262668,4.8342588248614));
#128325=CARTESIAN_POINT('Ctrl Pts',(15.4091470682088,15.7275759455093,4.86304183611818));
#128326=CARTESIAN_POINT('Ctrl Pts',(15.410498926853,15.741778737318,4.87963973937127));
#128327=CARTESIAN_POINT('Ctrl Pts',(15.4154846561445,15.7925530256519,4.94321612271183));
#128328=CARTESIAN_POINT('Ctrl Pts',(15.4190123229926,15.8253223624569,4.99305673929817));
#128329=CARTESIAN_POINT('Ctrl Pts',(15.4247358514212,15.8695540187805,5.07611653611215));
#128330=CARTESIAN_POINT('Ctrl Pts',(15.4268684103275,15.8841570916619,5.10748614819478));
#128331=CARTESIAN_POINT('Ctrl Pts',(15.4296291407849,15.900214819738,5.14745067038789));
#128332=CARTESIAN_POINT('Ctrl Pts',(15.4301786956532,15.903278335539,5.15537558380203));
#128333=CARTESIAN_POINT('Ctrl Pts',(15.4310745959043,15.9080512390398,5.16822348659012));
#128334=CARTESIAN_POINT('Ctrl Pts',(15.4314173194299,15.9098260360525,5.17312190559403));
#128335=CARTESIAN_POINT('Ctrl Pts',(15.4321047003577,15.9132822545413,5.182907277898));
#128336=CARTESIAN_POINT('Ctrl Pts',(15.4324493133189,15.9149642504095,5.18779383731844));
#128337=CARTESIAN_POINT('Ctrl Pts',(15.4333527908699,15.9192447024389,5.20056119476978));
#128338=CARTESIAN_POINT('Ctrl Pts',(15.4339149519035,15.9217809555641,5.2084622155463));
#128339=CARTESIAN_POINT('Ctrl Pts',(15.4367482152983,15.9339491700872,5.24811606702138));
#128340=CARTESIAN_POINT('Ctrl Pts',(15.4390859610181,15.9420427515469,5.28031477274497));
#128341=CARTESIAN_POINT('Ctrl Pts',(15.4453039460653,15.958945657235,5.3659832860125));
#128342=CARTESIAN_POINT('Ctrl Pts',(15.449209686754,15.9649460527726,5.4198943911944));
#128343=CARTESIAN_POINT('Ctrl Pts',(15.4556654627283,15.9674068762499,5.51144914686525));
#128344=CARTESIAN_POINT('Ctrl Pts',(15.4582583897597,15.9662381513011,5.54890367014075));
#128345=CARTESIAN_POINT('Ctrl Pts',(15.4616577381952,15.9617497432213,5.59904148996148));
#128346=CARTESIAN_POINT('Ctrl Pts',(15.4625206312506,15.9603433534721,5.61185908856759));
#128347=CARTESIAN_POINT('Ctrl Pts',(15.4639074929291,15.957646952564,5.632597849062));
#128348=CARTESIAN_POINT('Ctrl Pts',(15.464436222963,15.9565140375325,5.64053746051362));
#128349=CARTESIAN_POINT('Ctrl Pts',(15.4655452710826,15.9539157168945,5.65725638997519));
#128350=CARTESIAN_POINT('Ctrl Pts',(15.466124830147,15.9524275986089,5.66603145841488));
#128351=CARTESIAN_POINT('Ctrl Pts',(15.4675315732024,15.9484969641867,5.68741384494798));
#128352=CARTESIAN_POINT('Ctrl Pts',(15.4683546334165,15.9459239946132,5.69999565311109));
#128353=CARTESIAN_POINT('Ctrl Pts',(15.471666645392,15.9344651598364,5.75084587317177));
#128354=CARTESIAN_POINT('Ctrl Pts',(15.4740909316105,15.9235009668209,5.78860914971829));
#128355=CARTESIAN_POINT('Ctrl Pts',(15.4788342431152,15.8972327725345,5.86204532493796));
#128356=CARTESIAN_POINT('Ctrl Pts',(15.4811501695692,15.8820210232896,5.89767125469481));
#128357=CARTESIAN_POINT('Ctrl Pts',(15.4860487463233,15.8457283743711,5.9702679012516));
#128358=CARTESIAN_POINT('Ctrl Pts',(15.4886303141887,15.8242627263851,6.00695028648403));
#128359=CARTESIAN_POINT('Ctrl Pts',(15.4920048188514,15.7944923541623,6.05090895071373));
#128360=CARTESIAN_POINT('Ctrl Pts',(15.4926882691952,15.7883812723433,6.05961926377231));
#128361=CARTESIAN_POINT('Ctrl Pts',(15.4937527482016,15.7787655165545,6.07285474545321));
#128362=CARTESIAN_POINT('Ctrl Pts',(15.4941275003126,15.7753621355024,6.07745289333438));
#128363=CARTESIAN_POINT('Ctrl Pts',(15.494829163135,15.7689614443556,6.08594196020945));
#128364=CARTESIAN_POINT('Ctrl Pts',(15.4951553696684,15.7659749888083,6.0898406530489));
#128365=CARTESIAN_POINT('Ctrl Pts',(15.495942745915,15.7587393314746,6.09913888136806));
#128366=CARTESIAN_POINT('Ctrl Pts',(15.4964057535631,15.754462096117,6.10451609669501));
#128367=CARTESIAN_POINT('Ctrl Pts',(15.4980837101978,15.7388688129166,6.12369624834307));
#128368=CARTESIAN_POINT('Ctrl Pts',(15.4993176807345,15.7272289604491,6.13723000673157));
#128369=CARTESIAN_POINT('Ctrl Pts',(15.502655045806,15.695138258194,6.17251724551104));
#128370=CARTESIAN_POINT('Ctrl Pts',(15.5047828528751,15.6740433257741,6.19365845577138));
#128371=CARTESIAN_POINT('Ctrl Pts',(15.5124052651986,15.595389322123,6.2655044195885));
#128372=CARTESIAN_POINT('Ctrl Pts',(15.5178905971892,15.5328100143352,6.31031044419269));
#128373=CARTESIAN_POINT('Ctrl Pts',(15.5240820642154,15.4528373572988,6.35425725070756));
#128374=CARTESIAN_POINT('Ctrl Pts',(15.525059223476,15.4399331329825,6.36097386694533));
#128375=CARTESIAN_POINT('Ctrl Pts',(15.5266400262731,15.4186016663122,6.37147195617902));
#128376=CARTESIAN_POINT('Ctrl Pts',(15.5272495474524,15.4102635372747,6.3754282182494));
#128377=CARTESIAN_POINT('Ctrl Pts',(15.5284326071863,15.3938632580389,6.38292400139175));
#128378=CARTESIAN_POINT('Ctrl Pts',(15.5290064523207,15.3858069091369,6.38647396776245));
#128379=CARTESIAN_POINT('Ctrl Pts',(15.5303726562686,15.3663914478694,6.39471440624157));
#128380=CARTESIAN_POINT('Ctrl Pts',(15.5311614651041,15.3549890365193,6.39929937583708));
#128381=CARTESIAN_POINT('Ctrl Pts',(15.534086927839,15.3120279578001,6.41562976076759));
#128382=CARTESIAN_POINT('Ctrl Pts',(15.5361776435485,15.2799485835347,6.42594191674715));
#128383=CARTESIAN_POINT('Ctrl Pts',(15.5423065447752,15.1830825156925,6.45158400748197));
#128384=CARTESIAN_POINT('Ctrl Pts',(15.5462283213267,15.1171895063828,6.46192375117493));
#128385=CARTESIAN_POINT('Ctrl Pts',(15.5519423630345,15.0242398087023,6.46681086157044));
#128386=CARTESIAN_POINT('Ctrl Pts',(15.5535977767732,14.9976760462093,6.46711176052837));
#128387=CARTESIAN_POINT('Ctrl Pts',(15.5558182452771,14.9631215654536,6.46607962100183));
#128388=CARTESIAN_POINT('Ctrl Pts',(15.5563377434236,14.9551106019397,6.46574053707156));
#128389=CARTESIAN_POINT('Ctrl Pts',(15.5571638134655,14.9425066079403,6.46504988575111));
#128390=CARTESIAN_POINT('Ctrl Pts',(15.5574668997558,14.9379100917275,6.46476505599464));
#128391=CARTESIAN_POINT('Ctrl Pts',(15.5581116526307,14.9281956485794,6.46409337719542));
#128392=CARTESIAN_POINT('Ctrl Pts',(15.5584537639934,14.9230784772076,6.46369859419588));
#128393=CARTESIAN_POINT('Ctrl Pts',(15.5593430615093,14.9098665445954,6.46257341604216));
#128394=CARTESIAN_POINT('Ctrl Pts',(15.5598933645677,14.9017775582408,6.46178166045271));
#128395=CARTESIAN_POINT('Ctrl Pts',(15.5625286244504,14.8634057878595,6.45753670700769));
#128396=CARTESIAN_POINT('Ctrl Pts',(15.5646699072689,14.83328986756,6.45275490439155));
#128397=CARTESIAN_POINT('Ctrl Pts',(15.5703459190587,14.7550868435611,6.43651656000711));
#128398=CARTESIAN_POINT('Ctrl Pts',(15.5739088101027,14.707561063446,6.42278133980252));
#128399=CARTESIAN_POINT('Ctrl Pts',(15.5805301500298,14.6201060648715,6.39006730536638));
#128400=CARTESIAN_POINT('Ctrl Pts',(15.5835940321438,14.5800147872644,6.37186727593042));
#128401=CARTESIAN_POINT('Ctrl Pts',(15.587479917268,14.5294478088551,6.34461080200532));
#128402=CARTESIAN_POINT('Ctrl Pts',(15.5883821034378,14.5177324230444,6.33797660247071));
#128403=CARTESIAN_POINT('Ctrl Pts',(15.5898144589288,14.4991820497335,6.32695393233695));
#128404=CARTESIAN_POINT('Ctrl Pts',(15.5903500168414,14.4922575025864,6.32272048020689));
#128405=CARTESIAN_POINT('Ctrl Pts',(15.591460417144,14.4779290080856,6.31371066973453));
#128406=CARTESIAN_POINT('Ctrl Pts',(15.5920346500362,14.470535367909,6.3089192706395));
#128407=CARTESIAN_POINT('Ctrl Pts',(15.593403725678,14.4529554477259,6.29718240656121));
#128408=CARTESIAN_POINT('Ctrl Pts',(15.5941949781779,14.4428343610594,6.29014176203187));
#128409=CARTESIAN_POINT('Ctrl Pts',(15.597145384632,14.4052919229046,6.26294552855077));
#128410=CARTESIAN_POINT('Ctrl Pts',(15.5992575048577,14.3788051221356,6.24153951114497));
#128411=CARTESIAN_POINT('Ctrl Pts',(15.6055182180954,14.3026712494375,6.17306157283416));
#128412=CARTESIAN_POINT('Ctrl Pts',(15.6095429016476,14.2568382359838,6.12208441508455));
#128413=CARTESIAN_POINT('Ctrl Pts',(15.6152678327459,14.2023282709744,6.04674681527668));
#128414=CARTESIAN_POINT('Ctrl Pts',(15.6168076195095,14.1886586594488,6.02624831485754));
#128415=CARTESIAN_POINT('Ctrl Pts',(15.6188948470073,14.1716889935412,5.99856588892394));
#128416=CARTESIAN_POINT('Ctrl Pts',(15.6194033044282,14.1676718847976,5.9918302229538));
#128417=CARTESIAN_POINT('Ctrl Pts',(15.6202161738297,14.1614426568302,5.98109049224276));
#128418=CARTESIAN_POINT('Ctrl Pts',(15.6205172921297,14.1591761531177,5.97711815719065));
#128419=CARTESIAN_POINT('Ctrl Pts',(15.6211629005091,14.1544061167868,5.96861851320094));
#128420=CARTESIAN_POINT('Ctrl Pts',(15.6215078898227,14.15191058755,5.96408692232078));
#128421=CARTESIAN_POINT('Ctrl Pts',(15.6224134841664,14.1454951233105,5.95221262582946));
#128422=CARTESIAN_POINT('Ctrl Pts',(15.6229774125683,14.1416335211085,5.94483909431455));
#128423=CARTESIAN_POINT('Ctrl Pts',(15.6258430362792,14.122653464822,5.90743012096101));
#128424=CARTESIAN_POINT('Ctrl Pts',(15.6282131481239,14.109015440328,5.87667270225498));
#128425=CARTESIAN_POINT('Ctrl Pts',(15.6341222070828,14.079387692006,5.79918683639663));
#128426=CARTESIAN_POINT('Ctrl Pts',(15.6376782398824,14.0653197678851,5.75181932782896));
#128427=CARTESIAN_POINT('Ctrl Pts',(15.6440752975221,14.0462744567851,5.6634081089236));
#128428=CARTESIAN_POINT('Ctrl Pts',(15.6469311412012,14.0401895872312,5.62271656071804));
#128429=CARTESIAN_POINT('Ctrl Pts',(15.6505836809088,14.0356195354829,5.56887037062414));
#128430=CARTESIAN_POINT('Ctrl Pts',(15.6514499965795,14.0347845031464,5.55596320297559));
#128431=CARTESIAN_POINT('Ctrl Pts',(15.652814918391,14.0338689125233,5.53541916057281));
#128432=CARTESIAN_POINT('Ctrl Pts',(15.6533186235992,14.0336194235813,5.5277917655005));
#128433=CARTESIAN_POINT('Ctrl Pts',(15.6542613554327,14.0333199090117,5.51343345209547));
#128434=CARTESIAN_POINT('Ctrl Pts',(15.6547009683701,14.0332498134312,5.50670346095259));
#128435=CARTESIAN_POINT('Ctrl Pts',(15.6551384615117,14.0332500003729,5.49997314748094));
#128436=CARTESIAN_POINT('Origin',(16.125,15.,5.5));
#128437=CARTESIAN_POINT('',(16.1125616277506,14.0332502848258,5.49925789884204));
#128438=CARTESIAN_POINT('',(16.0537548202437,14.0332502522516,5.49930162248347));
#128439=CARTESIAN_POINT('',(16.125,14.03325,5.5));
#128440=CARTESIAN_POINT('Ctrl Pts',(16.1125616274111,14.033250284824,5.49925790359377));
#128441=CARTESIAN_POINT('Ctrl Pts',(16.1073559830469,14.0331943674599,5.57210301548347));
#128442=CARTESIAN_POINT('Ctrl Pts',(16.1021282237257,14.0413721963873,5.64473355734449));
#128443=CARTESIAN_POINT('Ctrl Pts',(16.095897439841,14.0616857744272,5.73345544885228));
#128444=CARTESIAN_POINT('Ctrl Pts',(16.094669390181,14.0662345449869,5.75103223120923));
#128445=CARTESIAN_POINT('Ctrl Pts',(16.0927719147452,14.0741224866012,5.77831900578406));
#128446=CARTESIAN_POINT('Ctrl Pts',(16.0920921318069,14.0771256816659,5.78812088588505));
#128447=CARTESIAN_POINT('Ctrl Pts',(16.0908368400081,14.0830012481834,5.80626231593391));
#128448=CARTESIAN_POINT('Ctrl Pts',(16.0902601005158,14.0858329075989,5.8146138150736));
#128449=CARTESIAN_POINT('Ctrl Pts',(16.0889617871747,14.0925057374861,5.83344299829025));
#128450=CARTESIAN_POINT('Ctrl Pts',(16.0882424962458,14.096414885327,5.84389537154835));
#128451=CARTESIAN_POINT('Ctrl Pts',(16.0860092111178,14.109210081522,5.8763817862009));
#128452=CARTESIAN_POINT('Ctrl Pts',(16.0845157678623,14.1187281521941,5.89815825158713));
#128453=CARTESIAN_POINT('Ctrl Pts',(16.0809031029579,14.1440057637913,5.95063138391362));
#128454=CARTESIAN_POINT('Ctrl Pts',(16.078809013189,14.1606243097535,5.98087779207209));
#128455=CARTESIAN_POINT('Ctrl Pts',(16.0734365601449,14.2076013074271,6.05649210963097));
#128456=CARTESIAN_POINT('Ctrl Pts',(16.0701897651757,14.2402434620536,6.10029018998348));
#128457=CARTESIAN_POINT('Ctrl Pts',(16.0656260447405,14.288895528575,6.15520303986655));
#128458=CARTESIAN_POINT('Ctrl Pts',(16.0644371463051,14.3017995191111,6.16893690240557));
#128459=CARTESIAN_POINT('Ctrl Pts',(16.062750268492,14.3202639751207,6.1874722759581));
#128460=CARTESIAN_POINT('Ctrl Pts',(16.0622742452965,14.3254910182834,6.192601486775));
#128461=CARTESIAN_POINT('Ctrl Pts',(16.0614589014763,14.3344601364066,6.20120490522481));
#128462=CARTESIAN_POINT('Ctrl Pts',(16.0611218387834,14.3381723436076,6.20470971418489));
#128463=CARTESIAN_POINT('Ctrl Pts',(16.0603950642301,14.3461822873295,6.21215303019434));
#128464=CARTESIAN_POINT('Ctrl Pts',(16.0600047745553,14.3504879477886,6.21608213887289));
#128465=CARTESIAN_POINT('Ctrl Pts',(16.0588744813706,14.362976643957,6.22727333580981));
#128466=CARTESIAN_POINT('Ctrl Pts',(16.058128059539,14.3712475054409,6.23443552314028));
#128467=CARTESIAN_POINT('Ctrl Pts',(16.0545092689552,14.4115370495578,6.26814505305229));
#128468=CARTESIAN_POINT('Ctrl Pts',(16.0515456005969,14.4451229683162,6.29274609434139));
#128469=CARTESIAN_POINT('Ctrl Pts',(16.043276719109,14.5425596783632,6.35488407467061));
#128470=CARTESIAN_POINT('Ctrl Pts',(16.0379924889092,14.6093055432432,6.38737810176765));
#128471=CARTESIAN_POINT('Ctrl Pts',(16.0319421746931,14.6933319620555,6.41694464235156));
#128472=CARTESIAN_POINT('Ctrl Pts',(16.0309287361999,14.7076662587569,6.42161477257108));
#128473=CARTESIAN_POINT('Ctrl Pts',(16.0292913167586,14.7312421915324,6.42869037841406));
#128474=CARTESIAN_POINT('Ctrl Pts',(16.0286610296978,14.7404201317674,6.43129741836877));
#128475=CARTESIAN_POINT('Ctrl Pts',(16.0274378193656,14.7584269456808,6.43612545573894));
#128476=CARTESIAN_POINT('Ctrl Pts',(16.0268445729351,14.7672515363398,6.43835844503077));
#128477=CARTESIAN_POINT('Ctrl Pts',(16.0254305771287,14.7884945760319,6.4434156971549));
#128478=CARTESIAN_POINT('Ctrl Pts',(16.0246136474746,14.8009400422729,6.44611990737854));
#128479=CARTESIAN_POINT('Ctrl Pts',(16.0215367331926,14.8484118352093,6.45545655901631));
#128480=CARTESIAN_POINT('Ctrl Pts',(16.0193283921805,14.8837437051285,6.46039630739235));
#128481=CARTESIAN_POINT('Ctrl Pts',(16.0124157158759,14.9965974235826,6.46985328539258));
#128482=CARTESIAN_POINT('Ctrl Pts',(16.0078753691624,15.0744140903304,6.46699909607143));
#128483=CARTESIAN_POINT('Ctrl Pts',(16.0020477843197,15.1662616544443,6.45247046237586));
#128484=CARTESIAN_POINT('Ctrl Pts',(16.0010696607862,15.1814181938449,6.44970011013545));
#128485=CARTESIAN_POINT('Ctrl Pts',(15.9996738685021,15.2025621558754,6.44531077170842));
#128486=CARTESIAN_POINT('Ctrl Pts',(15.9992709533124,15.2086108024591,6.44399439109653));
#128487=CARTESIAN_POINT('Ctrl Pts',(15.9985297113356,15.2196286601962,6.44148548914403));
#128488=CARTESIAN_POINT('Ctrl Pts',(15.9981923869776,15.2246017348553,6.44031150915673));
#128489=CARTESIAN_POINT('Ctrl Pts',(15.9974663490607,15.2352135883743,6.43771740832042));
#128490=CARTESIAN_POINT('Ctrl Pts',(15.9970770749847,15.2408489572423,6.43628582474119));
#128491=CARTESIAN_POINT('Ctrl Pts',(15.995952781455,15.2569798491264,6.43203274359874));
#128492=CARTESIAN_POINT('Ctrl Pts',(15.9952114432159,15.2674408200437,6.42908506722868));
#128493=CARTESIAN_POINT('Ctrl Pts',(15.9916446776112,15.3170433086303,6.41420106422892));
#128494=CARTESIAN_POINT('Ctrl Pts',(15.9887306260668,15.3554478431438,6.39996461843803));
#128495=CARTESIAN_POINT('Ctrl Pts',(15.9804320678423,15.4614362444033,6.35283034363875));
#128496=CARTESIAN_POINT('Ctrl Pts',(15.9750660572825,15.5262661104544,6.31442665335761));
#128497=CARTESIAN_POINT('Ctrl Pts',(15.9689536860992,15.5978685415422,6.25985613153497));
#128498=CARTESIAN_POINT('Ctrl Pts',(15.9679509490473,15.6095237368577,6.25053913234669));
#128499=CARTESIAN_POINT('Ctrl Pts',(15.9663261872256,15.6282477851073,6.23484741094146));
#128500=CARTESIAN_POINT('Ctrl Pts',(15.9656980436076,15.6354460790801,6.22863179193351));
#128501=CARTESIAN_POINT('Ctrl Pts',(15.9644759158744,15.6493653068344,6.21624955454216));
#128502=CARTESIAN_POINT('Ctrl Pts',(15.9638816512118,15.6560929831189,6.21009205944995));
#128503=CARTESIAN_POINT('Ctrl Pts',(15.962460125571,15.6720790679656,6.19503963314108));
#128504=CARTESIAN_POINT('Ctrl Pts',(15.9616367936941,15.6812495234686,6.18605355218398));
#128505=CARTESIAN_POINT('Ctrl Pts',(15.9584893577171,15.7159125441216,6.15070680890273));
#128506=CARTESIAN_POINT('Ctrl Pts',(15.9562202487941,15.7400777548757,6.12308542872458));
#128507=CARTESIAN_POINT('Ctrl Pts',(15.9498144328366,15.804643749653,6.04021293969853));
#128508=CARTESIAN_POINT('Ctrl Pts',(15.9457875645173,15.8408253560152,5.98196804449622));
#128509=CARTESIAN_POINT('Ctrl Pts',(15.9402269200436,15.8798947322617,5.90106336349003));
#128510=CARTESIAN_POINT('Ctrl Pts',(15.9388782115468,15.888584078633,5.88142463579809));
#128511=CARTESIAN_POINT('Ctrl Pts',(15.9370031330575,15.8994776365651,5.85440693460589));
#128512=CARTESIAN_POINT('Ctrl Pts',(15.9365056978748,15.9022587194492,5.84726573151318));
#128513=CARTESIAN_POINT('Ctrl Pts',(15.9356686667423,15.9067518716136,5.83530987135058));
#128514=CARTESIAN_POINT('Ctrl Pts',(15.9353317191763,15.908511261121,5.83051316738401));
#128515=CARTESIAN_POINT('Ctrl Pts',(15.9346166376098,15.9121397299699,5.82037278509638));
#128516=CARTESIAN_POINT('Ctrl Pts',(15.9342380639457,15.9140000086389,5.81502633019523));
#128517=CARTESIAN_POINT('Ctrl Pts',(15.93317608188,15.9190535362268,5.8000808184879));
#128518=CARTESIAN_POINT('Ctrl Pts',(15.9324873479841,15.9221431322509,5.79044779964323));
#128519=CARTESIAN_POINT('Ctrl Pts',(15.9281517841875,15.9404672238376,5.73007327912846));
#128520=CARTESIAN_POINT('Ctrl Pts',(15.924349236942,15.9516591132974,5.67820312908497));
#128521=CARTESIAN_POINT('Ctrl Pts',(15.916132519835,15.9665836474667,5.56437766626793));
#128522=CARTESIAN_POINT('Ctrl Pts',(15.9117461075325,15.9687232192829,5.50243460987787));
#128523=CARTESIAN_POINT('Ctrl Pts',(15.9064304147305,15.9639366710472,5.42454243712536));
#128524=CARTESIAN_POINT('Ctrl Pts',(15.9053393085399,15.9625375900903,5.40840747885397));
#128525=CARTESIAN_POINT('Ctrl Pts',(15.9036100489793,15.9596462679916,5.38261209180479));
#128526=CARTESIAN_POINT('Ctrl Pts',(15.9029641722851,15.9584118198074,5.37292649376607));
#128527=CARTESIAN_POINT('Ctrl Pts',(15.9017312762011,15.9557572080952,5.3543469783687));
#128528=CARTESIAN_POINT('Ctrl Pts',(15.9011436460825,15.9543590823371,5.34545099653667));
#128529=CARTESIAN_POINT('Ctrl Pts',(15.8997748191213,15.9507903213054,5.32464353548988));
#128530=CARTESIAN_POINT('Ctrl Pts',(15.8989967908379,15.9485197929731,5.31275057335208));
#128531=CARTESIAN_POINT('Ctrl Pts',(15.8962983639835,15.9398001781217,5.27131858690539));
#128532=CARTESIAN_POINT('Ctrl Pts',(15.8944136832919,15.9321892938038,5.24204081877785));
#128533=CARTESIAN_POINT('Ctrl Pts',(15.8893558698805,15.9077602843337,5.16341248924754));
#128534=CARTESIAN_POINT('Ctrl Pts',(15.8862485699041,15.8883060403032,5.11499035224674));
#128535=CARTESIAN_POINT('Ctrl Pts',(15.8806789894354,15.8471673321851,5.03254271394913));
#128536=CARTESIAN_POINT('Ctrl Pts',(15.8782375274485,15.8270833828993,4.99786332735044));
#128537=CARTESIAN_POINT('Ctrl Pts',(15.8750144861897,15.7990008719898,4.95564993973623));
#128538=CARTESIAN_POINT('Ctrl Pts',(15.8743291145243,15.7929453549398,4.94686617922809));
#128539=CARTESIAN_POINT('Ctrl Pts',(15.8732551152119,15.7833542775733,4.93343517430583));
#128540=CARTESIAN_POINT('Ctrl Pts',(15.8728726930437,15.7799196945114,4.92871645235685));
#128541=CARTESIAN_POINT('Ctrl Pts',(15.8721504365594,15.7734021494417,4.91993041514342));
#128542=CARTESIAN_POINT('Ctrl Pts',(15.8718112531023,15.7703293785615,4.91585596661415));
#128543=CARTESIAN_POINT('Ctrl Pts',(15.8709811507635,15.7627780275539,4.90600618291672));
#128544=CARTESIAN_POINT('Ctrl Pts',(15.870488065974,15.7582660066827,4.90025703066892));
#128545=CARTESIAN_POINT('Ctrl Pts',(15.8686196874381,15.7410549471082,4.87883163906568));
#128546=CARTESIAN_POINT('Ctrl Pts',(15.8672201502287,15.7279321758293,4.86350397432698));
#128547=CARTESIAN_POINT('Ctrl Pts',(15.8632575633959,15.6899121629053,4.82181037763897));
#128548=CARTESIAN_POINT('Ctrl Pts',(15.8606604227985,15.6639970871807,4.79641801618213));
#128549=CARTESIAN_POINT('Ctrl Pts',(15.8534787222765,15.5885074171763,4.73034453724786));
#128550=CARTESIAN_POINT('Ctrl Pts',(15.8489268378337,15.5362136648007,4.693037912234));
#128551=CARTESIAN_POINT('Ctrl Pts',(15.8434657664078,15.4666340831746,4.65317210454957));
#128552=CARTESIAN_POINT('Ctrl Pts',(15.8423808925587,15.4524639338855,4.64551694431356));
#128553=CARTESIAN_POINT('Ctrl Pts',(15.8406589966178,15.4294213407824,4.63380265317274));
#128554=CARTESIAN_POINT('Ctrl Pts',(15.8400143687425,15.4206677263204,4.62951783061913));
#128555=CARTESIAN_POINT('Ctrl Pts',(15.838782346825,15.4036983782576,4.62152724831228));
#128556=CARTESIAN_POINT('Ctrl Pts',(15.8381943639143,15.3954927257299,4.61780259071355));
#128557=CARTESIAN_POINT('Ctrl Pts',(15.8368224349295,15.3761033054182,4.60932638574957));
#128558=CARTESIAN_POINT('Ctrl Pts',(15.8360417020124,15.3648795183189,4.60466981425817));
#128559=CARTESIAN_POINT('Ctrl Pts',(15.8333192262497,15.3251158797495,4.58904450315052));
#128560=CARTESIAN_POINT('Ctrl Pts',(15.8314141134521,15.2961451865936,4.57921851476289));
#128561=CARTESIAN_POINT('Ctrl Pts',(15.8262660012174,15.2155572451679,4.55608374604975));
#128562=CARTESIAN_POINT('Ctrl Pts',(15.8230922472621,15.1632324420339,4.54564256033955));
#128563=CARTESIAN_POINT('Ctrl Pts',(15.8173350719284,15.0686926629639,4.53478396086078));
#128564=CARTESIAN_POINT('Ctrl Pts',(15.8147743925482,15.026809915178,4.5327145625386));
#128565=CARTESIAN_POINT('Ctrl Pts',(15.8115255278422,14.9760738062427,4.53350553199079));
#128566=CARTESIAN_POINT('Ctrl Pts',(15.8109531070492,14.96721997769,4.53376530989647));
#128567=CARTESIAN_POINT('Ctrl Pts',(15.8100218722228,14.9529800087402,4.53437905809718));
#128568=CARTESIAN_POINT('Ctrl Pts',(15.809667000976,14.9475908691475,4.53465655717467));
#128569=CARTESIAN_POINT('Ctrl Pts',(15.8089555572655,14.9368682529702,4.53529873918228));
#128570=CARTESIAN_POINT('Ctrl Pts',(15.8085990383027,14.9315349269467,4.53566257452602));
#128571=CARTESIAN_POINT('Ctrl Pts',(15.8076618416041,14.9176116924178,4.53672848678808));
#128572=CARTESIAN_POINT('Ctrl Pts',(15.8070776133299,14.9090278545961,4.537501221983));
#128573=CARTESIAN_POINT('Ctrl Pts',(15.8040153368434,14.864470739322,4.54211368751897));
#128574=CARTESIAN_POINT('Ctrl Pts',(15.8014590544304,14.8287264076335,4.54785546372532));
#128575=CARTESIAN_POINT('Ctrl Pts',(15.7928856231723,14.7112997070172,4.57354475315133));
#128576=CARTESIAN_POINT('Ctrl Pts',(15.7868381870474,14.6318810072862,4.60213547723658));
#128577=CARTESIAN_POINT('Ctrl Pts',(15.7801230651489,14.5439488588012,4.64744873911932));
#128578=CARTESIAN_POINT('Ctrl Pts',(15.7791246067988,14.5309002559615,4.6545582416056));
#128579=CARTESIAN_POINT('Ctrl Pts',(15.7775049051969,14.5097870996908,4.66670108745569));
#128580=CARTESIAN_POINT('Ctrl Pts',(15.776877617437,14.5016241029278,4.67155733980715));
#128581=CARTESIAN_POINT('Ctrl Pts',(15.7756559013371,14.4857597468186,4.68131457768487));
#128582=CARTESIAN_POINT('Ctrl Pts',(15.7750612097264,14.4780536370423,4.6862058846313));
#128583=CARTESIAN_POINT('Ctrl Pts',(15.7736365671182,14.4596419585907,4.69826148246447));
#128584=CARTESIAN_POINT('Ctrl Pts',(15.7728105906044,14.4490078972017,4.70553213359073));
#128585=CARTESIAN_POINT('Ctrl Pts',(15.7696331587769,14.4083170644561,4.73456313829603));
#128586=CARTESIAN_POINT('Ctrl Pts',(15.7673381622905,14.3793760434723,4.75783518360754));
#128587=CARTESIAN_POINT('Ctrl Pts',(15.7626474974636,14.3222751668091,4.80943309727329));
#128588=CARTESIAN_POINT('Ctrl Pts',(15.760261589418,14.2943883250774,4.83795329979655));
#128589=CARTESIAN_POINT('Ctrl Pts',(15.7552454367953,14.2400622752341,4.90085723786862));
#128590=CARTESIAN_POINT('Ctrl Pts',(15.752617197068,14.214016412403,4.93545910567804));
#128591=CARTESIAN_POINT('Ctrl Pts',(15.7491813586544,14.184464340448,4.98074645913912));
#128592=CARTESIAN_POINT('Ctrl Pts',(15.7484865023856,14.1787037845835,4.98990671889887));
#128593=CARTESIAN_POINT('Ctrl Pts',(15.7474007824598,14.1700581736333,5.0041809125312));
#128594=CARTESIAN_POINT('Ctrl Pts',(15.7470163382586,14.167063739241,5.00922797156989));
#128595=CARTESIAN_POINT('Ctrl Pts',(15.7462926923989,14.1615560709209,5.01870664496249));
#128596=CARTESIAN_POINT('Ctrl Pts',(15.7459541803669,14.1590316310737,5.02313134562218));
#128597=CARTESIAN_POINT('Ctrl Pts',(15.7451291088517,14.1530020924413,5.03389637229565));
#128598=CARTESIAN_POINT('Ctrl Pts',(15.7446404493503,14.1495331288844,5.04025644040136));
#128599=CARTESIAN_POINT('Ctrl Pts',(15.7428114142325,14.1369132693476,5.0640256102066));
#128600=CARTESIAN_POINT('Ctrl Pts',(15.7414480344349,14.128223346219,5.0816727081945));
#128601=CARTESIAN_POINT('Ctrl Pts',(15.7376324537265,14.1057011687235,5.1311640244244));
#128602=CARTESIAN_POINT('Ctrl Pts',(15.7351486685707,14.0930366145623,5.1635069369349));
#128603=CARTESIAN_POINT('Ctrl Pts',(15.7278996638257,14.0612440498586,5.25964275582242));
#128604=CARTESIAN_POINT('Ctrl Pts',(15.7231644495544,14.0469256598392,5.32482494169527));
#128605=CARTESIAN_POINT('Ctrl Pts',(15.7175674127192,14.0376531348269,5.40651769189749));
#128606=CARTESIAN_POINT('Ctrl Pts',(15.7165132149986,14.0362660019894,5.42210738489885));
#128607=CARTESIAN_POINT('Ctrl Pts',(15.714831220477,14.034639859842,5.44729886644916));
#128608=CARTESIAN_POINT('Ctrl Pts',(15.7141963539579,14.0341643724357,5.4568820073503));
#128609=CARTESIAN_POINT('Ctrl Pts',(15.7131667839531,14.0336210085073,5.47253949885804));
#128610=CARTESIAN_POINT('Ctrl Pts',(15.7127695005825,14.033467586689,5.47861002314708));
#128611=CARTESIAN_POINT('Ctrl Pts',(15.712039416012,14.0332899944767,5.48981660510008));
#128612=CARTESIAN_POINT('Ctrl Pts',(15.7117061358681,14.0332495375256,5.49495213410438));
#128613=CARTESIAN_POINT('Ctrl Pts',(15.7113740739618,14.0332500039877,5.50008780779963));
#128614=CARTESIAN_POINT('Ctrl Pts',(15.6551384581207,14.0332500003715,5.49997319964798));
#128615=CARTESIAN_POINT('Ctrl Pts',(15.6556495968289,14.0332502183577,5.4921099366161));
#128616=CARTESIAN_POINT('Ctrl Pts',(15.6561578055333,14.0333463724681,5.48424677980226));
#128617=CARTESIAN_POINT('Ctrl Pts',(15.6573484241237,14.033798881653,5.46572713321696));
#128618=CARTESIAN_POINT('Ctrl Pts',(15.6580283880359,14.0342356103667,5.45507352796589));
#128619=CARTESIAN_POINT('Ctrl Pts',(15.6617082259838,14.037576120969,5.39705588127462));
#128620=CARTESIAN_POINT('Ctrl Pts',(15.6646079478208,14.0437879373676,5.34994525653666));
#128621=CARTESIAN_POINT('Ctrl Pts',(15.6704414463854,14.0634145221551,5.25541265464075));
#128622=CARTESIAN_POINT('Ctrl Pts',(15.6733649236248,14.0770394133501,5.2081803913445));
#128623=CARTESIAN_POINT('Ctrl Pts',(15.6774960081779,14.1005487027816,5.1451423642523));
#128624=CARTESIAN_POINT('Ctrl Pts',(15.6786251467091,14.1073857738489,5.12827920656151));
#128625=CARTESIAN_POINT('Ctrl Pts',(15.6805818802552,14.1198309164871,5.09991070985696));
#128626=CARTESIAN_POINT('Ctrl Pts',(15.6813991922176,14.1251992305403,5.08830516989108));
#128627=CARTESIAN_POINT('Ctrl Pts',(15.6826228397123,14.1334520128632,5.07135449587531));
#128628=CARTESIAN_POINT('Ctrl Pts',(15.6830194641986,14.1361594377544,5.06592413039527));
#128629=CARTESIAN_POINT('Ctrl Pts',(15.6837397968014,14.1411301617844,5.05618489242835));
#128630=CARTESIAN_POINT('Ctrl Pts',(15.6840624216962,14.1433751537788,5.05186707499766));
#128631=CARTESIAN_POINT('Ctrl Pts',(15.6848048829462,14.1485840898269,5.0420308463886));
#128632=CARTESIAN_POINT('Ctrl Pts',(15.6852259411836,14.1515691507101,5.03652412511972));
#128633=CARTESIAN_POINT('Ctrl Pts',(15.6866173536018,14.161541143299,5.01854738052514));
#128634=CARTESIAN_POINT('Ctrl Pts',(15.6875996397597,14.1687508306791,5.00620383994242));
#128635=CARTESIAN_POINT('Ctrl Pts',(15.6941483204363,14.2180765640143,4.92589741317553));
#128636=CARTESIAN_POINT('Ctrl Pts',(15.6999872079677,14.2682113875373,4.86322338049762));
#128637=CARTESIAN_POINT('Ctrl Pts',(15.7081339108804,14.3511848613971,4.78241330925159));
#128638=CARTESIAN_POINT('Ctrl Pts',(15.7106125132494,14.3782515483434,4.75883798787974));
#128639=CARTESIAN_POINT('Ctrl Pts',(15.7138765173973,14.4164526171131,4.72913375534097));
#128640=CARTESIAN_POINT('Ctrl Pts',(15.7147136754323,14.4264850772212,4.72164084558442));
#128641=CARTESIAN_POINT('Ctrl Pts',(15.7161294287509,14.4438469533974,4.70919184046298));
#128642=CARTESIAN_POINT('Ctrl Pts',(15.7167116718776,14.4511037888662,4.70413775406642));
#128643=CARTESIAN_POINT('Ctrl Pts',(15.7178186215378,14.4651194074766,4.69465936131876));
#128644=CARTESIAN_POINT('Ctrl Pts',(15.7183438958634,14.4718662552249,4.69021882792767));
#128645=CARTESIAN_POINT('Ctrl Pts',(15.719721822269,14.4898123269664,4.67872707399137));
#128646=CARTESIAN_POINT('Ctrl Pts',(15.7205692250919,14.5011022717516,4.67182021025378));
#128647=CARTESIAN_POINT('Ctrl Pts',(15.723984186577,14.5475708974944,4.64468726595321));
#128648=CARTESIAN_POINT('Ctrl Pts',(15.7264829027725,14.583866292559,4.62645250553793));
#128649=CARTESIAN_POINT('Ctrl Pts',(15.7319567291149,14.6668035989688,4.5911313558562));
#128650=CARTESIAN_POINT('Ctrl Pts',(15.7349056641051,14.7138282020511,4.57524728398047));
#128651=CARTESIAN_POINT('Ctrl Pts',(15.7399808421712,14.7946213794426,4.55471292055863));
#128652=CARTESIAN_POINT('Ctrl Pts',(15.7420681749885,14.8277912890577,4.54811149338693));
#128653=CARTESIAN_POINT('Ctrl Pts',(15.7447703229556,14.8694819431896,4.54206469782178));
#128654=CARTESIAN_POINT('Ctrl Pts',(15.7453096313878,14.8777437365132,4.54097528646347));
#128655=CARTESIAN_POINT('Ctrl Pts',(15.7461929413554,14.8911575645331,4.53938266114961));
#128656=CARTESIAN_POINT('Ctrl Pts',(15.7465335047767,14.8963015658865,4.53881376447233));
#128657=CARTESIAN_POINT('Ctrl Pts',(15.7472210774897,14.9066249222412,4.5377558932344));
#128658=CARTESIAN_POINT('Ctrl Pts',(15.7475680956959,14.9118041444458,4.53726737142786));
#128659=CARTESIAN_POINT('Ctrl Pts',(15.7484850491741,14.9254153347025,4.53609427002527));
#128660=CARTESIAN_POINT('Ctrl Pts',(15.7490584536928,14.9338525903833,4.53547854511962));
#128661=CARTESIAN_POINT('Ctrl Pts',(15.7519292209816,14.9757796125655,4.53297152893087));
#128662=CARTESIAN_POINT('Ctrl Pts',(15.7542940832517,15.0093412069448,4.53271358788778));
#128663=CARTESIAN_POINT('Ctrl Pts',(15.760983417264,15.103149922085,4.53687512608228));
#128664=CARTESIAN_POINT('Ctrl Pts',(15.7653396320154,15.1630776095258,4.54519314191467));
#128665=CARTESIAN_POINT('Ctrl Pts',(15.7711071588488,15.2432217311859,4.56408794958034));
#128666=CARTESIAN_POINT('Ctrl Pts',(15.7726288027139,15.264427148629,4.56985669030132));
#128667=CARTESIAN_POINT('Ctrl Pts',(15.7753092775567,15.301920988245,4.58144265248999));
#128668=CARTESIAN_POINT('Ctrl Pts',(15.7764756701517,15.3182842604172,4.58698352848051));
#128669=CARTESIAN_POINT('Ctrl Pts',(15.7782801457926,15.3436613847601,4.59634191004306));
#128670=CARTESIAN_POINT('Ctrl Pts',(15.7789276438771,15.3527800360638,4.59986259447048));
#128671=CARTESIAN_POINT('Ctrl Pts',(15.7801383285016,15.3698468925271,4.6067512559654));
#128672=CARTESIAN_POINT('Ctrl Pts',(15.7807024570464,15.37780636179,4.61008854171932));
#128673=CARTESIAN_POINT('Ctrl Pts',(15.7819798221948,15.39583715518,4.61793410787388));
#128674=CARTESIAN_POINT('Ctrl Pts',(15.7826907509582,15.4058782316501,4.62250916332058));
#128675=CARTESIAN_POINT('Ctrl Pts',(15.7848901727664,15.4369312719251,4.63730509228897));
#128676=CARTESIAN_POINT('Ctrl Pts',(15.7863588192133,15.4576532673498,4.64811675903615));
#128677=CARTESIAN_POINT('Ctrl Pts',(15.7922723748994,15.540522683884,4.69525134327923));
#128678=CARTESIAN_POINT('Ctrl Pts',(15.7965164386462,15.5989097446057,4.73770593838504));
#128679=CARTESIAN_POINT('Ctrl Pts',(15.8023028676483,15.6690964596576,4.80182458192056));
#128680=CARTESIAN_POINT('Ctrl Pts',(15.8037226294215,15.6855835680331,4.81800730850678));
#128681=CARTESIAN_POINT('Ctrl Pts',(15.8061199086769,15.7118617024375,4.84571692157959));
#128682=CARTESIAN_POINT('Ctrl Pts',(15.807079980182,15.7219904025015,4.85691117888819));
#128683=CARTESIAN_POINT('Ctrl Pts',(15.8084755192149,15.7360741506229,4.87322878254368));
#128684=CARTESIAN_POINT('Ctrl Pts',(15.8088969642284,15.7402467681037,4.87816237568118));
#128685=CARTESIAN_POINT('Ctrl Pts',(15.8096117892207,15.747182311838,4.8865315098997));
#128686=CARTESIAN_POINT('Ctrl Pts',(15.8099033142593,15.7499717246646,4.8899447511957));
#128687=CARTESIAN_POINT('Ctrl Pts',(15.8105801278236,15.7563564828769,4.89786738072869));
#128688=CARTESIAN_POINT('Ctrl Pts',(15.8109665163487,15.7599348152839,4.90238984881359));
#128689=CARTESIAN_POINT('Ctrl Pts',(15.8120878830152,15.7701349206172,4.91552098218511));
#128690=CARTESIAN_POINT('Ctrl Pts',(15.812829197302,15.7766521450197,4.92420929122086));
#128691=CARTESIAN_POINT('Ctrl Pts',(15.8183939215017,15.8240102643661,4.98961096486209));
#128692=CARTESIAN_POINT('Ctrl Pts',(15.8234709983416,15.8587383718413,5.05049170923649));
#128693=CARTESIAN_POINT('Ctrl Pts',(15.8307644690659,15.8996150391371,5.14452254674572));
#128694=CARTESIAN_POINT('Ctrl Pts',(15.8330623195544,15.9111067314229,5.17510573418608));
#128695=CARTESIAN_POINT('Ctrl Pts',(15.8368919777386,15.9279591086787,5.22793856746538));
#128696=CARTESIAN_POINT('Ctrl Pts',(15.8384448507,15.9341183064918,5.24990269183507));
#128697=CARTESIAN_POINT('Ctrl Pts',(15.840696681109,15.9420387944436,5.28254921162091));
#128698=CARTESIAN_POINT('Ctrl Pts',(15.8414142747615,15.944406667795,5.29307489941878));
#128699=CARTESIAN_POINT('Ctrl Pts',(15.8426946429158,15.9483466975313,5.31206855077032));
#128700=CARTESIAN_POINT('Ctrl Pts',(15.8432593611036,15.9499827970973,5.32052191916797));
#128701=CARTESIAN_POINT('Ctrl Pts',(15.8444682820853,15.9532633789661,5.33877586173613));
#128702=CARTESIAN_POINT('Ctrl Pts',(15.8451112535044,15.9548701352099,5.34858226943635));
#128703=CARTESIAN_POINT('Ctrl Pts',(15.8468804235149,15.9589026517713,5.37581903027254));
#128704=CARTESIAN_POINT('Ctrl Pts',(15.8479966524727,15.9610042059478,5.39329393506057));
#128705=CARTESIAN_POINT('Ctrl Pts',(15.8545268951363,15.9706074357716,5.496950134613));
#128706=CARTESIAN_POINT('Ctrl Pts',(15.8595840556235,15.9669913184988,5.58375782895399));
#128707=CARTESIAN_POINT('Ctrl Pts',(15.8666728770546,15.946747677258,5.69782838226927));
#128708=CARTESIAN_POINT('Ctrl Pts',(15.868496601459,15.9403051845685,5.72647972006876));
#128709=CARTESIAN_POINT('Ctrl Pts',(15.8708983239596,15.9304491184675,5.76255432464798));
#128710=CARTESIAN_POINT('Ctrl Pts',(15.871419710188,15.9282312113452,5.77029084997551));
#128711=CARTESIAN_POINT('Ctrl Pts',(15.8722811003307,15.9244458825671,5.78289847482078));
#128712=CARTESIAN_POINT('Ctrl Pts',(15.8726179820302,15.9229358580818,5.78778661656662));
#128713=CARTESIAN_POINT('Ctrl Pts',(15.8732634045381,15.9199886419105,5.79706531648785));
#128714=CARTESIAN_POINT('Ctrl Pts',(15.8735714989943,15.9185586435891,5.80145798981087));
#128715=CARTESIAN_POINT('Ctrl Pts',(15.8744241590459,15.9145363041837,5.81351944294505));
#128716=CARTESIAN_POINT('Ctrl Pts',(15.8749721973459,15.9118791010769,5.82116598092802));
#128717=CARTESIAN_POINT('Ctrl Pts',(15.8773956789997,15.8998033461968,5.85455747446959));
#128718=CARTESIAN_POINT('Ctrl Pts',(15.8793161102307,15.8893888740733,5.87992660886625));
#128719=CARTESIAN_POINT('Ctrl Pts',(15.8859175388306,15.8503958555049,5.96448942326975));
#128720=CARTESIAN_POINT('Ctrl Pts',(15.8906762551205,15.8168644909113,6.02120727481705));
#128721=CARTESIAN_POINT('Ctrl Pts',(15.897636606641,15.7579411560756,6.1010436350139));
#128722=CARTESIAN_POINT('Ctrl Pts',(15.8999468814423,15.7366542436428,6.12695231414162));
#128723=CARTESIAN_POINT('Ctrl Pts',(15.90303247286,15.7057910856038,6.16076853548565));
#128724=CARTESIAN_POINT('Ctrl Pts',(15.9038523613196,15.6973475798021,6.16967342055236));
#128725=CARTESIAN_POINT('Ctrl Pts',(15.9052480253838,15.6825610211547,6.18468493276363));
#128726=CARTESIAN_POINT('Ctrl Pts',(15.9058271938336,15.6763000639869,6.19086991303629));
#128727=CARTESIAN_POINT('Ctrl Pts',(15.9070065679208,15.6632982184298,6.20336782836127));
#128728=CARTESIAN_POINT('Ctrl Pts',(15.9076063421276,15.6565495669797,6.20967140581826));
#128729=CARTESIAN_POINT('Ctrl Pts',(15.9091425272377,15.6389200761236,6.22567146424163));
#128730=CARTESIAN_POINT('Ctrl Pts',(15.9100728680037,15.6279082204021,6.23522053800172));
#128731=CARTESIAN_POINT('Ctrl Pts',(15.915830814087,15.5577701062863,6.29331597926802));
#128732=CARTESIAN_POINT('Ctrl Pts',(15.9203732033247,15.4932732108086,6.33494926264737));
#128733=CARTESIAN_POINT('Ctrl Pts',(15.9268042514346,15.3976379172647,6.38169507271811));
#128734=CARTESIAN_POINT('Ctrl Pts',(15.9286254623712,15.3701422803926,6.39358636157927));
#128735=CARTESIAN_POINT('Ctrl Pts',(15.9316080605303,15.3254158137158,6.41051079135322));
#128736=CARTESIAN_POINT('Ctrl Pts',(15.9327393183586,15.3085192665266,6.41637390037019));
#128737=CARTESIAN_POINT('Ctrl Pts',(15.934338322435,15.2849154045754,6.42383767467148));
#128738=CARTESIAN_POINT('Ctrl Pts',(15.9347858770212,15.2783380058633,6.42584058283552));
#128739=CARTESIAN_POINT('Ctrl Pts',(15.9355598521304,15.2670262431559,6.42915374076354));
#128740=CARTESIAN_POINT('Ctrl Pts',(15.935884363089,15.2623023036063,6.43049835511877));
#128741=CARTESIAN_POINT('Ctrl Pts',(15.9365912256314,15.2520567199103,6.43333041791334));
#128742=CARTESIAN_POINT('Ctrl Pts',(15.9369742170835,15.2465320688042,6.43480489627575));
#128743=CARTESIAN_POINT('Ctrl Pts',(15.9380761707549,15.2307028056774,6.43887950368638));
#128744=CARTESIAN_POINT('Ctrl Pts',(15.9388011554398,15.2203682864799,6.44135875367847));
#128745=CARTESIAN_POINT('Ctrl Pts',(15.9424423921174,15.1687580899615,6.45284364187224));
#128746=CARTESIAN_POINT('Ctrl Pts',(15.9454543412342,15.126966868417,6.4593065775544));
#128747=CARTESIAN_POINT('Ctrl Pts',(15.951257877836,15.0462047926802,6.4664258556855));
#128748=CARTESIAN_POINT('Ctrl Pts',(15.954042640131,15.007346450168,6.46750199061406));
#128749=CARTESIAN_POINT('Ctrl Pts',(15.958655195215,14.9420423647818,6.46537489174267));
#128750=CARTESIAN_POINT('Ctrl Pts',(15.9605045263738,14.9156022496462,6.46342357262938));
#128751=CARTESIAN_POINT('Ctrl Pts',(15.963681653053,14.8696376880029,6.45812417505072));
#128752=CARTESIAN_POINT('Ctrl Pts',(15.9650219014629,14.8500744705347,6.45525844546418));
#128753=CARTESIAN_POINT('Ctrl Pts',(15.9670294859375,14.820518681379,6.44999848045933));
#128754=CARTESIAN_POINT('Ctrl Pts',(15.9677100502371,14.8104546261503,6.44804178253842));
#128755=CARTESIAN_POINT('Ctrl Pts',(15.9689518730169,14.792015703491,6.44415143309504));
#128756=CARTESIAN_POINT('Ctrl Pts',(15.9695145567794,14.7836319507952,6.44226549940818));
#128757=CARTESIAN_POINT('Ctrl Pts',(15.97075085654,14.7651552245341,6.43784952796542));
#128758=CARTESIAN_POINT('Ctrl Pts',(15.9714227744784,14.7550756222975,6.43526780567692));
#128759=CARTESIAN_POINT('Ctrl Pts',(15.9733680741889,14.7258069711588,6.42726548471068));
#128760=CARTESIAN_POINT('Ctrl Pts',(15.9746278503047,14.7067409635156,6.42141321759786));
#128761=CARTESIAN_POINT('Ctrl Pts',(15.9806347414312,14.6156644581305,6.39034369214941));
#128762=CARTESIAN_POINT('Ctrl Pts',(15.9851298013793,14.546632536636,6.35725360489714));
#128763=CARTESIAN_POINT('Ctrl Pts',(15.9918929929511,14.452719114953,6.29768950848176));
#128764=CARTESIAN_POINT('Ctrl Pts',(15.99404625264,14.4242687532711,6.2774046174881));
#128765=CARTESIAN_POINT('Ctrl Pts',(15.9968232857152,14.3904205001339,6.25039246145946));
#128766=CARTESIAN_POINT('Ctrl Pts',(15.9973663748209,14.3839287480584,6.24507195223129));
#128767=CARTESIAN_POINT('Ctrl Pts',(15.9982543279225,14.373537835885,6.23632712616542));
#128768=CARTESIAN_POINT('Ctrl Pts',(15.9985956860415,14.3695953827067,6.23295463382176));
#128769=CARTESIAN_POINT('Ctrl Pts',(15.999241680192,14.3622368376419,6.22655662785863));
#128770=CARTESIAN_POINT('Ctrl Pts',(15.9995457796194,14.3588146258465,6.22353831869193));
#128771=CARTESIAN_POINT('Ctrl Pts',(16.000373167727,14.3496125276711,6.21530573460485));
#128772=CARTESIAN_POINT('Ctrl Pts',(16.0008996015816,14.3438741803584,6.21004581367135));
#128773=CARTESIAN_POINT('Ctrl Pts',(16.0030642831221,14.3207251506482,6.18830656958076));
#128774=CARTESIAN_POINT('Ctrl Pts',(16.0047368448663,14.3038679605313,6.17125274416622));
#128775=CARTESIAN_POINT('Ctrl Pts',(16.0113023671196,14.2410214078813,6.1027575353815));
#128776=CARTESIAN_POINT('Ctrl Pts',(16.01630831422,14.1999535371934,6.04707578193256));
#128777=CARTESIAN_POINT('Ctrl Pts',(16.0235491174608,14.1479415560903,5.95800439584722));
#128778=CARTESIAN_POINT('Ctrl Pts',(16.0259051241987,14.1322952893734,5.92762203977659));
#128779=CARTESIAN_POINT('Ctrl Pts',(16.0290394146784,14.1132274373277,5.88521717439445));
#128780=CARTESIAN_POINT('Ctrl Pts',(16.0298641707206,14.1083822948082,5.8738659395957));
#128781=CARTESIAN_POINT('Ctrl Pts',(16.0312654862192,14.1004521176434,5.85425530381771));
#128782=CARTESIAN_POINT('Ctrl Pts',(16.0318455100048,14.0972603708278,5.84604101408276));
#128783=CARTESIAN_POINT('Ctrl Pts',(16.0329524808061,14.0913466456947,5.83018246880816));
#128784=CARTESIAN_POINT('Ctrl Pts',(16.033479941589,14.0886077307911,5.82254537533416));
#128785=CARTESIAN_POINT('Ctrl Pts',(16.0348734441661,14.0815859498073,5.8021621692857));
#128786=CARTESIAN_POINT('Ctrl Pts',(16.0357339988198,14.077472213602,5.78935938792309));
#128787=CARTESIAN_POINT('Ctrl Pts',(16.0393555836553,14.0611420155299,5.73464236295716));
#128788=CARTESIAN_POINT('Ctrl Pts',(16.0420355822339,14.0515043265455,5.69201022281936));
#128789=CARTESIAN_POINT('Ctrl Pts',(16.0477147800653,14.0370689530188,5.59938527521914));
#128790=CARTESIAN_POINT('Ctrl Pts',(16.0506938265694,14.03321407643,5.54937935504139));
#128791=CARTESIAN_POINT('Ctrl Pts',(16.053754820006,14.0332502522502,5.49930162637244));
#128792=CARTESIAN_POINT('Origin',(16.125,15.,5.5));
#128793=CARTESIAN_POINT('',(16.5125067421103,14.0332503216444,5.50077380256718));
#128794=CARTESIAN_POINT('',(16.4541432637038,14.0332503253858,5.5007624277622));
#128795=CARTESIAN_POINT('',(16.125,14.03325,5.5));
#128796=CARTESIAN_POINT('Ctrl Pts',(16.5125067496464,14.0332503339973,5.50080360660429));
#128797=CARTESIAN_POINT('Ctrl Pts',(16.5105833290927,14.0332767876738,5.53262773901946));
#128798=CARTESIAN_POINT('Ctrl Pts',(16.5086462365695,14.0348746414668,5.5644291826904));
#128799=CARTESIAN_POINT('Ctrl Pts',(16.5057673491034,14.0394468958017,5.61020150264302));
#128800=CARTESIAN_POINT('Ctrl Pts',(16.5048693988576,14.0411665401289,5.62427786879034));
#128801=CARTESIAN_POINT('Ctrl Pts',(16.5035762620414,14.0440418281855,5.64416854663637));
#128802=CARTESIAN_POINT('Ctrl Pts',(16.5031929469513,14.044942389746,5.65001850948271));
#128803=CARTESIAN_POINT('Ctrl Pts',(16.5024976571657,14.0466608445872,5.66053812421363));
#128804=CARTESIAN_POINT('Ctrl Pts',(16.502186679749,14.0474594861647,5.66521077990356));
#128805=CARTESIAN_POINT('Ctrl Pts',(16.5015377746353,14.0491870160363,5.67488896340818));
#128806=CARTESIAN_POINT('Ctrl Pts',(16.5011995249584,14.0501211071857,5.67989320238334));
#128807=CARTESIAN_POINT('Ctrl Pts',(16.5003764658171,14.05247528727,5.69197550914361));
#128808=CARTESIAN_POINT('Ctrl Pts',(16.4998895827829,14.0539351985892,5.69904537483077));
#128809=CARTESIAN_POINT('Ctrl Pts',(16.4981632417358,14.0593509290644,5.7238651141439));
#128810=CARTESIAN_POINT('Ctrl Pts',(16.4969045717342,14.0637280485396,5.74151812196225));
#128811=CARTESIAN_POINT('Ctrl Pts',(16.490577773891,14.0879326106587,5.82854903437541));
#128812=CARTESIAN_POINT('Ctrl Pts',(16.4853308474073,14.1149860537522,5.89567975587241));
#128813=CARTESIAN_POINT('Ctrl Pts',(16.4776819913718,14.1665691581234,5.99125035059317));
#128814=CARTESIAN_POINT('Ctrl Pts',(16.4751589135872,14.1856813043854,6.02232123930006));
#128815=CARTESIAN_POINT('Ctrl Pts',(16.4718074907172,14.2140212633326,6.06304185307378));
#128816=CARTESIAN_POINT('Ctrl Pts',(16.4709266512986,14.2217577424303,6.07368782440317));
#128817=CARTESIAN_POINT('Ctrl Pts',(16.4694454835682,14.2352536902985,6.09148358160653));
#128818=CARTESIAN_POINT('Ctrl Pts',(16.4688410400938,14.2409018434157,6.09871507734019));
#128819=CARTESIAN_POINT('Ctrl Pts',(16.4676963510626,14.251863695255,6.11234531265085));
#128820=CARTESIAN_POINT('Ctrl Pts',(16.4671554464197,14.2571586528099,6.11875799172183));
#128821=CARTESIAN_POINT('Ctrl Pts',(16.4657444459347,14.2712686335921,6.13540425095298));
#128822=CARTESIAN_POINT('Ctrl Pts',(16.4648797475106,14.2802166869923,6.1455230259763));
#128823=CARTESIAN_POINT('Ctrl Pts',(16.461511913143,14.3162073295224,6.1845432797082));
#128824=CARTESIAN_POINT('Ctrl Pts',(16.4590730686303,14.3448031643363,6.21196173385888));
#128825=CARTESIAN_POINT('Ctrl Pts',(16.4536224152011,14.4132311964921,6.26994730214302));
#128826=CARTESIAN_POINT('Ctrl Pts',(16.4506403796383,14.4539200831638,6.29932035565807));
#128827=CARTESIAN_POINT('Ctrl Pts',(16.445543604979,14.5253700556522,6.34288756493675));
#128828=CARTESIAN_POINT('Ctrl Pts',(16.4434695215582,14.5549270863108,6.35886126532734));
#128829=CARTESIAN_POINT('Ctrl Pts',(16.4407728297959,14.5929123534625,6.37690200949856));
#128830=CARTESIAN_POINT('Ctrl Pts',(16.4402240491711,14.6006202661687,6.38043926690264));
#128831=CARTESIAN_POINT('Ctrl Pts',(16.4393218150596,14.6132346716849,6.3860284502893));
#128832=CARTESIAN_POINT('Ctrl Pts',(16.4389718679392,14.6181135211208,6.3881421894044));
#128833=CARTESIAN_POINT('Ctrl Pts',(16.4382596672256,14.6280082235383,6.39233242108524));
#128834=CARTESIAN_POINT('Ctrl Pts',(16.4378973396688,14.6330245921608,6.39440710977871));
#128835=CARTESIAN_POINT('Ctrl Pts',(16.4369275308173,14.6464121815821,6.39981241746529));
#128836=CARTESIAN_POINT('Ctrl Pts',(16.4363160620137,14.6548127332749,6.40306836327861));
#128837=CARTESIAN_POINT('Ctrl Pts',(16.4323846413182,14.7086425547327,6.4230713203994));
#128838=CARTESIAN_POINT('Ctrl Pts',(16.4289264463184,14.7552266076856,6.43650143293388));
#128839=CARTESIAN_POINT('Ctrl Pts',(16.4221879859515,14.8473778614359,6.45572113315245));
#128840=CARTESIAN_POINT('Ctrl Pts',(16.4189169113154,14.8927495167184,6.46187021627812));
#128841=CARTESIAN_POINT('Ctrl Pts',(16.4135422864062,14.9694444752851,6.46676797918873));
#128842=CARTESIAN_POINT('Ctrl Pts',(16.4114017438431,15.000580521315,6.46725073126526));
#128843=CARTESIAN_POINT('Ctrl Pts',(16.4084827310651,15.0439008706756,6.46582999369363));
#128844=CARTESIAN_POINT('Ctrl Pts',(16.4076668319409,15.0561049215193,6.4651979713166));
#128845=CARTESIAN_POINT('Ctrl Pts',(16.4062608491905,15.0772924543401,6.46369747005433));
#128846=CARTESIAN_POINT('Ctrl Pts',(16.4056676309965,15.0862815971163,6.46293428251287));
#128847=CARTESIAN_POINT('Ctrl Pts',(16.4044433308546,15.1049294714602,6.46108782294924));
#128848=CARTESIAN_POINT('Ctrl Pts',(16.4038129343279,15.114585226447,6.45998449694793));
#128849=CARTESIAN_POINT('Ctrl Pts',(16.4021583210635,15.140055576125,6.45668431419686));
#128850=CARTESIAN_POINT('Ctrl Pts',(16.4011417183137,15.1558355601533,6.45424093648017));
#128851=CARTESIAN_POINT('Ctrl Pts',(16.3959680353904,15.2366295709528,6.43967295207971));
#128852=CARTESIAN_POINT('Ctrl Pts',(16.3920085456699,15.300335843104,6.42129158068097));
#128853=CARTESIAN_POINT('Ctrl Pts',(16.3859133527246,15.3941259789592,6.38345628137011));
#128854=CARTESIAN_POINT('Ctrl Pts',(16.3837980252179,15.4258440445157,6.36861202104873));
#128855=CARTESIAN_POINT('Ctrl Pts',(16.3803960164886,15.4741039117932,6.34274646252821));
#128856=CARTESIAN_POINT('Ctrl Pts',(16.3791500298384,15.4912307212228,6.3328795717899));
#128857=CARTESIAN_POINT('Ctrl Pts',(16.377407529083,15.5142157246497,6.31868211822658));
#128858=CARTESIAN_POINT('Ctrl Pts',(16.3769357001066,15.520346252571,6.31479935688548));
#128859=CARTESIAN_POINT('Ctrl Pts',(16.3761251778817,15.5307064696131,6.30807312470866));
#128860=CARTESIAN_POINT('Ctrl Pts',(16.3757886726384,15.5349583907188,6.30526458435078));
#128861=CARTESIAN_POINT('Ctrl Pts',(16.3750601723402,15.5440539669144,6.29915280820992));
#128862=CARTESIAN_POINT('Ctrl Pts',(16.3746675601561,15.5488898559573,6.29583908644269));
#128863=CARTESIAN_POINT('Ctrl Pts',(16.3735448055558,15.5625412267501,6.28630107701731));
#128864=CARTESIAN_POINT('Ctrl Pts',(16.3728085309313,15.5712827612458,6.27997307590908));
#128865=CARTESIAN_POINT('Ctrl Pts',(16.3691133829193,15.6142033227395,6.24779426345757));
#128866=CARTESIAN_POINT('Ctrl Pts',(16.3660570863485,15.6467406059271,6.21983884390686));
#128867=CARTESIAN_POINT('Ctrl Pts',(16.3600940012295,15.7061948721333,6.16146252113395));
#128868=CARTESIAN_POINT('Ctrl Pts',(16.3571940440591,15.7332683582405,6.13131743001137));
#128869=CARTESIAN_POINT('Ctrl Pts',(16.3517402020986,15.7812996795712,6.0705636992478));
#128870=CARTESIAN_POINT('Ctrl Pts',(16.3491822507258,15.802545971781,6.04027090694735));
#128871=CARTESIAN_POINT('Ctrl Pts',(16.3458183843617,15.8287792606081,5.99789161319542));
#128872=CARTESIAN_POINT('Ctrl Pts',(16.3449576887603,15.8353327290766,5.98681657709178));
#128873=CARTESIAN_POINT('Ctrl Pts',(16.3435000074547,15.8461523719744,5.96766973471541));
#128874=CARTESIAN_POINT('Ctrl Pts',(16.3428992164216,15.8505287572435,5.95966255009034));
#128875=CARTESIAN_POINT('Ctrl Pts',(16.3416808417757,15.8592295487312,5.94319343332397));
#128876=CARTESIAN_POINT('Ctrl Pts',(16.3410636563806,15.8635438790499,5.9347272893724));
#128877=CARTESIAN_POINT('Ctrl Pts',(16.3394908009555,15.8742910998221,5.91284614105817));
#128878=CARTESIAN_POINT('Ctrl Pts',(16.3385413732388,15.8805405562273,5.89934349793339));
#128879=CARTESIAN_POINT('Ctrl Pts',(16.332295108105,15.9199737298078,5.80871233210587));
#128880=CARTESIAN_POINT('Ctrl Pts',(16.3273495203905,15.9432985493906,5.72769122974226));
#128881=CARTESIAN_POINT('Ctrl Pts',(16.3200477566085,15.9612845257851,5.6088568530949));
#128882=CARTESIAN_POINT('Ctrl Pts',(16.3178178811493,15.9646875339598,5.57276785108625));
#128883=CARTESIAN_POINT('Ctrl Pts',(16.3149442696165,15.9663839654178,5.52796267925683));
#128884=CARTESIAN_POINT('Ctrl Pts',(16.3143867042571,15.9665948786398,5.51934446607222));
#128885=CARTESIAN_POINT('Ctrl Pts',(16.3134737168902,15.9667498180917,5.50537903400174));
#128886=CARTESIAN_POINT('Ctrl Pts',(16.3131219619996,15.9667647804515,5.50003286266465));
#128887=CARTESIAN_POINT('Ctrl Pts',(16.312410198331,15.9667057461933,5.48929122597609));
#128888=CARTESIAN_POINT('Ctrl Pts',(16.3120501637509,15.9666309194127,5.48389597062502));
#128889=CARTESIAN_POINT('Ctrl Pts',(16.3110932217846,15.9663140171604,5.4696487643885));
#128890=CARTESIAN_POINT('Ctrl Pts',(16.3104925017385,15.9659954783744,5.46079923998198));
#128891=CARTESIAN_POINT('Ctrl Pts',(16.3070636144001,15.9635049902982,5.41074739728882));
#128892=CARTESIAN_POINT('Ctrl Pts',(16.3041343731744,15.9588187660242,5.3697164409778));
#128893=CARTESIAN_POINT('Ctrl Pts',(16.297345241201,15.9420303529762,5.27623484555285));
#128894=CARTESIAN_POINT('Ctrl Pts',(16.2934868792006,15.9281411983399,5.22423415052124));
#128895=CARTESIAN_POINT('Ctrl Pts',(16.2875848626558,15.8996373303231,5.1447521848488));
#128896=CARTESIAN_POINT('Ctrl Pts',(16.285473783497,15.8879005292606,5.11635782049986));
#128897=CARTESIAN_POINT('Ctrl Pts',(16.2825867308426,15.8696528814523,5.07755774600721));
#128898=CARTESIAN_POINT('Ctrl Pts',(16.2817744334564,15.8642673541312,5.0666461545593));
#128899=CARTESIAN_POINT('Ctrl Pts',(16.2803725654047,15.8545360746065,5.04783310926381));
#128900=CARTESIAN_POINT('Ctrl Pts',(16.2797799131304,15.8502832165091,5.03988560038536));
#128901=CARTESIAN_POINT('Ctrl Pts',(16.2785548882698,15.8412053636816,5.02347724557386));
#128902=CARTESIAN_POINT('Ctrl Pts',(16.277923226749,15.8363623956584,5.01502747122555));
#128903=CARTESIAN_POINT('Ctrl Pts',(16.2762608297667,15.8231924246876,4.99283336980867));
#128904=CARTESIAN_POINT('Ctrl Pts',(16.2752378440435,15.8146488336771,4.9792206967599));
#128905=CARTESIAN_POINT('Ctrl Pts',(16.2701509049664,15.7700356661606,4.91192431939944));
#128906=CARTESIAN_POINT('Ctrl Pts',(16.2662741490846,15.7289829632749,4.86174241477248));
#128907=CARTESIAN_POINT('Ctrl Pts',(16.2602151736066,15.6578375874246,4.79067444988966));
#128908=CARTESIAN_POINT('Ctrl Pts',(16.2580485319236,15.6310612995862,4.76675082340595));
#128909=CARTESIAN_POINT('Ctrl Pts',(16.2545754400448,15.5873452483631,4.73186377613888));
#128910=CARTESIAN_POINT('Ctrl Pts',(16.2533117489838,15.5712869796003,4.71984696064718));
#128911=CARTESIAN_POINT('Ctrl Pts',(16.2515484702936,15.5488956134504,4.70415305503031));
#128912=CARTESIAN_POINT('Ctrl Pts',(16.2510743394036,15.5428762737919,4.70003493957868));
#128913=CARTESIAN_POINT('Ctrl Pts',(16.2502611746449,15.5325686457607,4.69315291275355));
#128914=CARTESIAN_POINT('Ctrl Pts',(16.2499243671422,15.5283040703061,4.69035415593343));
#128915=CARTESIAN_POINT('Ctrl Pts',(16.2491968308511,15.5191064601562,4.68442155726726));
#128916=CARTESIAN_POINT('Ctrl Pts',(16.2488055066962,15.5141670868817,4.68129864069463));
#128917=CARTESIAN_POINT('Ctrl Pts',(16.2476900501384,15.5001011134725,4.67258292767819));
#128918=CARTESIAN_POINT('Ctrl Pts',(16.2469599023281,15.4909097978122,4.66709683449133));
#128919=CARTESIAN_POINT('Ctrl Pts',(16.2433973225832,15.4460542455253,4.64132391580039));
#128920=CARTESIAN_POINT('Ctrl Pts',(16.240475408915,15.4092164110101,4.62317027294435));
#128921=CARTESIAN_POINT('Ctrl Pts',(16.2338672770681,15.3239351901979,4.58769096576293));
#128922=CARTESIAN_POINT('Ctrl Pts',(16.2301866545479,15.2750300868017,4.57177533213881));
#128923=CARTESIAN_POINT('Ctrl Pts',(16.224505195386,15.1959067865099,4.55283236172576));
#128924=CARTESIAN_POINT('Ctrl Pts',(16.2224436336864,15.1664123835201,4.54720766327891));
#128925=CARTESIAN_POINT('Ctrl Pts',(16.2196104692767,15.1247455712622,4.5412560498023));
#128926=CARTESIAN_POINT('Ctrl Pts',(16.2188043644101,15.1127584103614,4.5397724318742));
#128927=CARTESIAN_POINT('Ctrl Pts',(16.2174095527018,15.091794750482,4.5375758247239));
#128928=CARTESIAN_POINT('Ctrl Pts',(16.2168178550086,15.0828304716686,4.53676291006744));
#128929=CARTESIAN_POINT('Ctrl Pts',(16.2155914811344,15.0641091732799,4.53532848462104));
#128930=CARTESIAN_POINT('Ctrl Pts',(16.2149575611769,15.0543514160391,4.53472954383689));
#128931=CARTESIAN_POINT('Ctrl Pts',(16.2132812720016,15.0283499304566,4.53352909284104));
#128932=CARTESIAN_POINT('Ctrl Pts',(16.2122468971076,15.0120969092273,4.53318903332481));
#128933=CARTESIAN_POINT('Ctrl Pts',(16.2076907582181,14.9397485130913,4.53350018663546));
#128934=CARTESIAN_POINT('Ctrl Pts',(16.2043028997232,14.8837801471013,4.53862290095077));
#128935=CARTESIAN_POINT('Ctrl Pts',(16.1984056776056,14.7874136864648,4.55598663306492));
#128936=CARTESIAN_POINT('Ctrl Pts',(16.1958960845821,14.7467867791296,4.56606379037165));
#128937=CARTESIAN_POINT('Ctrl Pts',(16.1923816050153,14.6926719960557,4.58327795169618));
#128938=CARTESIAN_POINT('Ctrl Pts',(16.191445103013,14.6785096318547,4.58814819509471));
#128939=CARTESIAN_POINT('Ctrl Pts',(16.1897854025014,14.6539936673505,4.59722101823879));
#128940=CARTESIAN_POINT('Ctrl Pts',(16.1890686235036,14.6435889703397,4.6012778932845));
#128941=CARTESIAN_POINT('Ctrl Pts',(16.1879600399008,14.6278222529524,4.60774230519148));
#128942=CARTESIAN_POINT('Ctrl Pts',(16.1875752388561,14.6224076891339,4.6100201621208));
#128943=CARTESIAN_POINT('Ctrl Pts',(16.1868513421799,14.6123381537226,4.61436475152856));
#128944=CARTESIAN_POINT('Ctrl Pts',(16.186512942971,14.6076782375176,4.6164191432923));
#128945=CARTESIAN_POINT('Ctrl Pts',(16.1856887333997,14.5964391663997,4.62148048269541));
#128946=CARTESIAN_POINT('Ctrl Pts',(16.1852008343408,14.5898772232002,4.62452459259364));
#128947=CARTESIAN_POINT('Ctrl Pts',(16.1834671880298,14.5668584894024,4.6355186429366));
#128948=CARTESIAN_POINT('Ctrl Pts',(16.1822020298152,14.5505944871386,4.64386089036813));
#128949=CARTESIAN_POINT('Ctrl Pts',(16.1758347889273,14.4709245792262,4.68762144287024));
#128950=CARTESIAN_POINT('Ctrl Pts',(16.1705527963481,14.411413153113,4.72964548942773));
#128951=CARTESIAN_POINT('Ctrl Pts',(16.1628632965646,14.3298252397355,4.80228126590489));
#128952=CARTESIAN_POINT('Ctrl Pts',(16.1603311325907,14.3038857561274,4.82815838849209));
#128953=CARTESIAN_POINT('Ctrl Pts',(16.1569943374277,14.270918967912,4.86501097649619));
#128954=CARTESIAN_POINT('Ctrl Pts',(16.1561360899593,14.2625548258743,4.87474416999497));
#128955=CARTESIAN_POINT('Ctrl Pts',(16.1546812546512,14.2485825220966,4.89167403351593));
#128956=CARTESIAN_POINT('Ctrl Pts',(16.1540808987697,14.2428780848884,4.89878862059772));
#128957=CARTESIAN_POINT('Ctrl Pts',(16.1528623276605,14.2314307233898,4.91348717253875));
#128958=CARTESIAN_POINT('Ctrl Pts',(16.1522445250428,14.2256973545143,4.92107733386379));
#128959=CARTESIAN_POINT('Ctrl Pts',(16.1506678157201,14.2112561108543,4.94079389072775));
#128960=CARTESIAN_POINT('Ctrl Pts',(16.1497152138452,14.2027152243588,4.95303983756325));
#128961=CARTESIAN_POINT('Ctrl Pts',(16.1434818965528,14.148172879607,5.03523680137596));
#128962=CARTESIAN_POINT('Ctrl Pts',(16.1385497351003,14.1111431539906,5.11070798638034));
#128963=CARTESIAN_POINT('Ctrl Pts',(16.1312558261808,14.0726417439136,5.2244394773653));
#128964=CARTESIAN_POINT('Ctrl Pts',(16.129018523802,14.0629382069889,5.25949725084588));
#128965=CARTESIAN_POINT('Ctrl Pts',(16.1261364894884,14.0534029649584,5.30344456693666));
#128966=CARTESIAN_POINT('Ctrl Pts',(16.1255785422586,14.0516867644825,5.31189901630506));
#128967=CARTESIAN_POINT('Ctrl Pts',(16.1246650866699,14.049090417552,5.32562934748641));
#128968=CARTESIAN_POINT('Ctrl Pts',(16.1243132524631,14.048140472526,5.33089176424303));
#128969=CARTESIAN_POINT('Ctrl Pts',(16.1236015033954,14.0463200395838,5.34147809013245));
#128970=CARTESIAN_POINT('Ctrl Pts',(16.123241564777,14.045450362164,5.34680193121465));
#128971=CARTESIAN_POINT('Ctrl Pts',(16.1222851609598,14.0432718646222,5.36087725537264));
#128972=CARTESIAN_POINT('Ctrl Pts',(16.121684890353,14.042038601067,5.3696396999101));
#128973=CARTESIAN_POINT('Ctrl Pts',(16.1183149889578,14.0358443564242,5.41850148246738));
#128974=CARTESIAN_POINT('Ctrl Pts',(16.1154484691767,14.0332812943534,5.45886092356221));
#128975=CARTESIAN_POINT('Ctrl Pts',(16.1125616274111,14.033250284824,5.49925790359377));
#128976=CARTESIAN_POINT('Ctrl Pts',(16.053754820006,14.0332502522502,5.49930162637244));
#128977=CARTESIAN_POINT('Ctrl Pts',(16.0555819563119,14.0332718459438,5.46940975039724));
#128978=CARTESIAN_POINT('Ctrl Pts',(16.057436656885,14.0346798156171,5.43953772406872));
#128979=CARTESIAN_POINT('Ctrl Pts',(16.0598841511539,14.0382394990734,5.40155965248761));
#128980=CARTESIAN_POINT('Ctrl Pts',(16.0604187513643,14.0391154732059,5.39334786253083));
#128981=CARTESIAN_POINT('Ctrl Pts',(16.0612629771265,14.0406489664404,5.38053124940146));
#128982=CARTESIAN_POINT('Ctrl Pts',(16.0615688488107,14.0412347263295,5.37591802802548));
#128983=CARTESIAN_POINT('Ctrl Pts',(16.0622130668265,14.0425305617261,5.36627008813138));
#128984=CARTESIAN_POINT('Ctrl Pts',(16.0625517873068,14.0432471089392,5.36123647498748));
#128985=CARTESIAN_POINT('Ctrl Pts',(16.0634214757567,14.0451769564426,5.34840585914653));
#128986=CARTESIAN_POINT('Ctrl Pts',(16.0639553143812,14.0464460612491,5.34061774197943));
#128987=CARTESIAN_POINT('Ctrl Pts',(16.0663566565632,14.0525344365228,5.30593535241904));
#128988=CARTESIAN_POINT('Ctrl Pts',(16.0682694646484,14.0583968933431,5.27923903652652));
#128989=CARTESIAN_POINT('Ctrl Pts',(16.0750854160738,14.0829892584866,5.18624867227684));
#128990=CARTESIAN_POINT('Ctrl Pts',(16.0800765446964,14.1076639584807,5.12173240742865));
#128991=CARTESIAN_POINT('Ctrl Pts',(16.0870558284045,14.1530248046447,5.03289004412398));
#128992=CARTESIAN_POINT('Ctrl Pts',(16.0891806549669,14.1683738677505,5.00607995663884));
#128993=CARTESIAN_POINT('Ctrl Pts',(16.0920883336116,14.191578068668,4.96970764348981));
#128994=CARTESIAN_POINT('Ctrl Pts',(16.0929079081642,14.1983712564409,4.95949340138138));
#128995=CARTESIAN_POINT('Ctrl Pts',(16.0942974387616,14.210319119209,4.94224954269159));
#128996=CARTESIAN_POINT('Ctrl Pts',(16.0948708566776,14.215377689847,4.93515550387149));
#128997=CARTESIAN_POINT('Ctrl Pts',(16.0960432973002,14.2259818498573,4.92070184048405));
#128998=CARTESIAN_POINT('Ctrl Pts',(16.0966418341509,14.2315381593906,4.91335115833387));
#128999=CARTESIAN_POINT('Ctrl Pts',(16.0981703737362,14.2460893286805,4.89466233865598));
#129000=CARTESIAN_POINT('Ctrl Pts',(16.0990944271931,14.2552353971504,4.88344448320808));
#129001=CARTESIAN_POINT('Ctrl Pts',(16.1011050177788,14.2758737295597,4.85926081712003));
#129002=CARTESIAN_POINT('Ctrl Pts',(16.1021873478148,14.2874696480597,4.84638994532465));
#129003=CARTESIAN_POINT('Ctrl Pts',(16.1055902500676,14.3253562935794,4.80654508529898));
#129004=CARTESIAN_POINT('Ctrl Pts',(16.1078682504463,14.3528806535515,4.78079164693743));
#129005=CARTESIAN_POINT('Ctrl Pts',(16.1139258859375,14.4301931704857,4.71649434272923));
#129006=CARTESIAN_POINT('Ctrl Pts',(16.117670177814,14.4823506215545,4.68109946682399));
#129007=CARTESIAN_POINT('Ctrl Pts',(16.1223188099944,14.5464647938768,4.64617680842324));
#129008=CARTESIAN_POINT('Ctrl Pts',(16.1229705672337,14.5554379546427,4.64147056287598));
#129009=CARTESIAN_POINT('Ctrl Pts',(16.1239958646515,14.5694939218463,4.63437792200988));
#129010=CARTESIAN_POINT('Ctrl Pts',(16.1243638230733,14.574526620658,4.63189317193628));
#129011=CARTESIAN_POINT('Ctrl Pts',(16.1250607111793,14.5840290738574,4.62730408717964));
#129012=CARTESIAN_POINT('Ctrl Pts',(16.1253890620748,14.5884937611469,4.62518997569645));
#129013=CARTESIAN_POINT('Ctrl Pts',(16.126192815156,14.5993953378329,4.62012979386847));
#129014=CARTESIAN_POINT('Ctrl Pts',(16.1266702639879,14.6058486684773,4.61722007520581));
#129015=CARTESIAN_POINT('Ctrl Pts',(16.1284711138808,14.6301269272565,4.60659261258317));
#129016=CARTESIAN_POINT('Ctrl Pts',(16.129817186576,14.6481501389731,4.59934223363141));
#129017=CARTESIAN_POINT('Ctrl Pts',(16.1335846756384,14.6985543858762,4.58080938405562));
#129018=CARTESIAN_POINT('Ctrl Pts',(16.1360375367235,14.7313358084232,4.5706990887894));
#129019=CARTESIAN_POINT('Ctrl Pts',(16.1433672498332,14.8306037706531,4.54577573045922));
#129020=CARTESIAN_POINT('Ctrl Pts',(16.1482149169212,14.8982011135298,4.53621636898596));
#129021=CARTESIAN_POINT('Ctrl Pts',(16.1539109873521,14.9818674666426,4.53329375290289));
#129022=CARTESIAN_POINT('Ctrl Pts',(16.1549631029394,14.9974963037979,4.53312692868293));
#129023=CARTESIAN_POINT('Ctrl Pts',(16.1566326969434,15.0225677401307,4.53346729123608));
#129024=CARTESIAN_POINT('Ctrl Pts',(16.1572573791698,15.0320102538792,4.53373392160617));
#129025=CARTESIAN_POINT('Ctrl Pts',(16.1584498772752,15.0501484063339,4.53451227727555));
#129026=CARTESIAN_POINT('Ctrl Pts',(16.1590182710538,15.0588439629896,4.53500321163347));
#129027=CARTESIAN_POINT('Ctrl Pts',(16.1603407678721,15.0791848369827,4.53642759482995));
#129028=CARTESIAN_POINT('Ctrl Pts',(16.1610919300268,15.0908223665397,4.53745476216955));
#129029=CARTESIAN_POINT('Ctrl Pts',(16.1636690133816,15.1309975136282,4.54173590611325));
#129030=CARTESIAN_POINT('Ctrl Pts',(16.1654627657949,15.1594080479737,4.54605046192239));
#129031=CARTESIAN_POINT('Ctrl Pts',(16.1701640731988,15.2343399312697,4.56087180181358));
#129032=CARTESIAN_POINT('Ctrl Pts',(16.1730172316831,15.2803461713758,4.57356422097476));
#129033=CARTESIAN_POINT('Ctrl Pts',(16.1787162285089,15.3694052072202,4.60537950240581));
#129034=CARTESIAN_POINT('Ctrl Pts',(16.1815549913394,15.4123684772372,4.62435319659485));
#129035=CARTESIAN_POINT('Ctrl Pts',(16.185210668159,15.4631481152362,4.65134698056224));
#129036=CARTESIAN_POINT('Ctrl Pts',(16.1858922141997,15.4724331653336,4.65648058310527));
#129037=CARTESIAN_POINT('Ctrl Pts',(16.1869543414194,15.486586057409,4.6646125304026));
#129038=CARTESIAN_POINT('Ctrl Pts',(16.1873286887992,15.4915152264921,4.66750315688759));
#129039=CARTESIAN_POINT('Ctrl Pts',(16.1880300502723,15.5006339746254,4.67295990331286));
#129040=CARTESIAN_POINT('Ctrl Pts',(16.188356367525,15.5048300567797,4.67551451943533));
#129041=CARTESIAN_POINT('Ctrl Pts',(16.1891446420696,15.5148576292771,4.68172464765833));
#129042=CARTESIAN_POINT('Ctrl Pts',(16.189608448849,15.5206697978628,4.68541060307389));
#129043=CARTESIAN_POINT('Ctrl Pts',(16.1912929689092,15.5414822470832,4.69892315883016));
#129044=CARTESIAN_POINT('Ctrl Pts',(16.1925328904097,15.5562469401256,4.70910406541835));
#129045=CARTESIAN_POINT('Ctrl Pts',(16.1958922765854,15.5949938927054,4.73744355292568));
#129046=CARTESIAN_POINT('Ctrl Pts',(16.1980364977369,15.6184259371827,4.75632047196069));
#129047=CARTESIAN_POINT('Ctrl Pts',(16.2056416428003,15.697989998802,4.82678158290062));
#129048=CARTESIAN_POINT('Ctrl Pts',(16.2110918332478,15.748878039024,4.88388414344253));
#129049=CARTESIAN_POINT('Ctrl Pts',(16.2172569433786,15.8009026229382,4.95835979279725));
#129050=CARTESIAN_POINT('Ctrl Pts',(16.2182388589736,15.8089990149851,4.97052879371185));
#129051=CARTESIAN_POINT('Ctrl Pts',(16.2198252972878,15.8217604464134,4.99068600300294));
#129052=CARTESIAN_POINT('Ctrl Pts',(16.2204357789459,15.8265920278571,4.99856544970122));
#129053=CARTESIAN_POINT('Ctrl Pts',(16.2216193473308,15.8357999017637,5.01407670127965));
#129054=CARTESIAN_POINT('Ctrl Pts',(16.2221927588863,15.8401864708521,5.02170131654289));
#129055=CARTESIAN_POINT('Ctrl Pts',(16.2235557245544,15.8504287389778,5.04007997375903));
#129056=CARTESIAN_POINT('Ctrl Pts',(16.2243417740469,15.8561854728063,5.05088762188908));
#129057=CARTESIAN_POINT('Ctrl Pts',(16.227239467204,15.8768169956357,5.09146042536855));
#129058=CARTESIAN_POINT('Ctrl Pts',(16.2293063746298,15.8903581951927,5.12187933196215));
#129059=CARTESIAN_POINT('Ctrl Pts',(16.2352954848077,15.9254941227428,5.21322716348978));
#129060=CARTESIAN_POINT('Ctrl Pts',(16.2391088623504,15.9425817734535,5.27568512856025));
#129061=CARTESIAN_POINT('Ctrl Pts',(16.2448166196166,15.9580729218002,5.367627419638));
#129062=CARTESIAN_POINT('Ctrl Pts',(16.2465970441174,15.9615741159089,5.39607148352723));
#129063=CARTESIAN_POINT('Ctrl Pts',(16.2489608799098,15.9644455666248,5.43278878124079));
#129064=CARTESIAN_POINT('Ctrl Pts',(16.2494910307638,15.9649801737885,5.44095889178846));
#129065=CARTESIAN_POINT('Ctrl Pts',(16.2503298970423,15.9656549013487,5.45376499970002));
#129066=CARTESIAN_POINT('Ctrl Pts',(16.2506349383385,15.96586554976,5.45839709914998));
#129067=CARTESIAN_POINT('Ctrl Pts',(16.251279245037,15.9662378066673,5.46812445058905));
#129068=CARTESIAN_POINT('Ctrl Pts',(16.2516189049702,15.9663924479576,5.473219742582));
#129069=CARTESIAN_POINT('Ctrl Pts',(16.2524940798626,15.9666852625476,5.48627107258372));
#129070=CARTESIAN_POINT('Ctrl Pts',(16.2530325341783,15.9667655109834,5.49422790787831));
#129071=CARTESIAN_POINT('Ctrl Pts',(16.2554955991826,15.9666839199583,5.53033580943649));
#129072=CARTESIAN_POINT('Ctrl Pts',(16.2574683007548,15.9653907052195,5.55846845862868));
#129073=CARTESIAN_POINT('Ctrl Pts',(16.2647895119291,15.9561536310308,5.66128852147467));
#129074=CARTESIAN_POINT('Ctrl Pts',(16.2702333969029,15.940743235831,5.73504947665471));
#129075=CARTESIAN_POINT('Ctrl Pts',(16.2772266606601,15.9088359282518,5.83057313849593));
#129076=CARTESIAN_POINT('Ctrl Pts',(16.2789785324675,15.8997603374191,5.85453191607225));
#129077=CARTESIAN_POINT('Ctrl Pts',(16.2814650842699,15.8852922571526,5.88857778491875));
#129078=CARTESIAN_POINT('Ctrl Pts',(16.2822239390347,15.8806565489891,5.89897260156269));
#129079=CARTESIAN_POINT('Ctrl Pts',(16.2835517291197,15.8721571675057,5.91716068530542));
#129080=CARTESIAN_POINT('Ctrl Pts',(16.2841231560472,15.8683699337616,5.92498803342029));
#129081=CARTESIAN_POINT('Ctrl Pts',(16.2853107069492,15.8602299270374,5.94124830887897));
#129082=CARTESIAN_POINT('Ctrl Pts',(16.2859260842179,15.8558575379562,5.94967041546211));
#129083=CARTESIAN_POINT('Ctrl Pts',(16.2875577939642,15.8438563384391,5.97197774949159));
#129084=CARTESIAN_POINT('Ctrl Pts',(16.2885664745828,15.8360088712636,5.98574244971829));
#129085=CARTESIAN_POINT('Ctrl Pts',(16.2926839045276,15.8022629910539,6.04169125814592));
#129086=CARTESIAN_POINT('Ctrl Pts',(16.2956914034513,15.7734815322143,6.08205013252692));
#129087=CARTESIAN_POINT('Ctrl Pts',(16.3021599277745,15.7046674943836,6.16437131770244));
#129088=CARTESIAN_POINT('Ctrl Pts',(16.3055992079153,15.663704117734,6.20529508273831));
#129089=CARTESIAN_POINT('Ctrl Pts',(16.3101749489064,15.6076863394042,6.2520326389051));
#129090=CARTESIAN_POINT('Ctrl Pts',(16.3111390442231,15.5958094859388,6.26147670762929));
#129091=CARTESIAN_POINT('Ctrl Pts',(16.3125067639051,15.5789534788129,6.27424423018538));
#129092=CARTESIAN_POINT('Ctrl Pts',(16.3128958436033,15.5741576632889,6.27780732316254));
#129093=CARTESIAN_POINT('Ctrl Pts',(16.3136121387264,15.5653349339167,6.28423618964113));
#129094=CARTESIAN_POINT('Ctrl Pts',(16.3139384238034,15.5613185732635,6.28711590440737));
#129095=CARTESIAN_POINT('Ctrl Pts',(16.3146393646178,15.5526996209826,6.29319613851485));
#129096=CARTESIAN_POINT('Ctrl Pts',(16.3150145322228,15.5480912150758,6.29638746936009));
#129097=CARTESIAN_POINT('Ctrl Pts',(16.3160916029437,15.5348671155656,6.30537604157011));
#129098=CARTESIAN_POINT('Ctrl Pts',(16.3167992844313,15.526185680561,6.31107460096355));
#129099=CARTESIAN_POINT('Ctrl Pts',(16.3201163458357,15.4854549542159,6.33688141864371));
#129100=CARTESIAN_POINT('Ctrl Pts',(16.3228032263679,15.4523368304037,6.35523559072662));
#129101=CARTESIAN_POINT('Ctrl Pts',(16.3307390306942,15.3522597246387,6.40325693894611));
#129102=CARTESIAN_POINT('Ctrl Pts',(16.3359912106291,15.2828951386583,6.42732600845898));
#129103=CARTESIAN_POINT('Ctrl Pts',(16.3422235840022,15.1940225214801,6.44724896933727));
#129104=CARTESIAN_POINT('Ctrl Pts',(16.3434330740238,15.176466966323,6.45067598539669));
#129105=CARTESIAN_POINT('Ctrl Pts',(16.345295180927,15.1489663819463,6.4552562361265));
#129106=CARTESIAN_POINT('Ctrl Pts',(16.3459579893046,15.1390821658714,6.45674532835271));
#129107=CARTESIAN_POINT('Ctrl Pts',(16.347182567944,15.1206490448173,6.45923063267351));
#129108=CARTESIAN_POINT('Ctrl Pts',(16.3477455081437,15.1121065874911,6.46026648364706));
#129109=CARTESIAN_POINT('Ctrl Pts',(16.3490012102111,15.0929047273911,6.46233514805039));
#129110=CARTESIAN_POINT('Ctrl Pts',(16.3496919785407,15.0822396054252,6.46330518915648));
#129111=CARTESIAN_POINT('Ctrl Pts',(16.3518074732707,15.0492888858854,6.4657509581501));
#129112=CARTESIAN_POINT('Ctrl Pts',(16.3532141709048,15.0269658218279,6.46663191895112));
#129113=CARTESIAN_POINT('Ctrl Pts',(16.3565700675411,14.972988426526,6.46689048349058));
#129114=CARTESIAN_POINT('Ctrl Pts',(16.3584985430995,14.941356136694,6.46548843927558));
#129115=CARTESIAN_POINT('Ctrl Pts',(16.3642716971533,14.8462900695013,6.45658448504985));
#129116=CARTESIAN_POINT('Ctrl Pts',(16.3680484538433,14.7834840701583,6.44435164053158));
#129117=CARTESIAN_POINT('Ctrl Pts',(16.3730332238562,14.7072178167024,6.42148448941474));
#129118=CARTESIAN_POINT('Ctrl Pts',(16.3740353051051,14.6922018603671,6.41657804507553));
#129119=CARTESIAN_POINT('Ctrl Pts',(16.3754520638716,14.6715342055773,6.40925979595582));
#129120=CARTESIAN_POINT('Ctrl Pts',(16.3758510071461,14.665774370436,6.40715840873849));
#129121=CARTESIAN_POINT('Ctrl Pts',(16.3765761119717,14.6554224610014,6.4032697054944));
#129122=CARTESIAN_POINT('Ctrl Pts',(16.3769011878553,14.6508232350615,6.40150176212317));
#129123=CARTESIAN_POINT('Ctrl Pts',(16.3775931230447,14.6411260930492,6.39768883801965));
#129124=CARTESIAN_POINT('Ctrl Pts',(16.3779604224687,14.6360318313754,6.39563547252004));
#129125=CARTESIAN_POINT('Ctrl Pts',(16.3789919111365,14.6218656165419,6.38978462049598));
#129126=CARTESIAN_POINT('Ctrl Pts',(16.3796611730217,14.612833968551,6.38589205264213));
#129127=CARTESIAN_POINT('Ctrl Pts',(16.3836687509982,14.5596026171385,6.36198031061316));
#129128=CARTESIAN_POINT('Ctrl Pts',(16.3871400720182,14.5169049940767,6.33879574815456));
#129129=CARTESIAN_POINT('Ctrl Pts',(16.3954742107645,14.4190986987596,6.27573465308383));
#129130=CARTESIAN_POINT('Ctrl Pts',(16.400306105088,14.3660865474963,6.23305330499322));
#129131=CARTESIAN_POINT('Ctrl Pts',(16.4059868914364,14.3069109109654,6.17414900444205));
#129132=CARTESIAN_POINT('Ctrl Pts',(16.4070381380039,14.2961126589939,6.16286652063453));
#129133=CARTESIAN_POINT('Ctrl Pts',(16.4087067033969,14.2792299066624,6.14434866722932));
#129134=CARTESIAN_POINT('Ctrl Pts',(16.4093312101,14.2729703044962,6.13727746300967));
#129135=CARTESIAN_POINT('Ctrl Pts',(16.410523584144,14.2611382889258,6.12351005784185));
#129136=CARTESIAN_POINT('Ctrl Pts',(16.4110920264144,14.2555508324878,6.11682806799188));
#129137=CARTESIAN_POINT('Ctrl Pts',(16.4124149520153,14.2426788650934,6.10100487352368));
#129138=CARTESIAN_POINT('Ctrl Pts',(16.4131664884989,14.2354682233647,6.09180515428526));
#129139=CARTESIAN_POINT('Ctrl Pts',(16.4157377233576,14.2111799663433,6.05963186357591));
#129140=CARTESIAN_POINT('Ctrl Pts',(16.4175255265102,14.1949560879664,6.03603114700165));
#129141=CARTESIAN_POINT('Ctrl Pts',(16.4222100246314,14.1546708132903,5.97146385631119));
#129142=CARTESIAN_POINT('Ctrl Pts',(16.4250527344463,14.1325402281817,5.92938723815914));
#129143=CARTESIAN_POINT('Ctrl Pts',(16.4307339682298,14.0949094875043,5.84293924459934));
#129144=CARTESIAN_POINT('Ctrl Pts',(16.4335655236157,14.0793719926254,5.79872946429754));
#129145=CARTESIAN_POINT('Ctrl Pts',(16.4372258037383,14.0642575755087,5.74312335052918));
#129146=CARTESIAN_POINT('Ctrl Pts',(16.437921091114,14.061592897999,5.73262617341984));
#129147=CARTESIAN_POINT('Ctrl Pts',(16.4390001810718,14.0577819076502,5.71648051314522));
#129148=CARTESIAN_POINT('Ctrl Pts',(16.4393774384625,14.0565087467374,5.71086250755645));
#129149=CARTESIAN_POINT('Ctrl Pts',(16.4400484530062,14.0543498145954,5.70092469376081));
#129150=CARTESIAN_POINT('Ctrl Pts',(16.440341062479,14.0534432703204,5.69660966509531));
#129151=CARTESIAN_POINT('Ctrl Pts',(16.4409560897577,14.051610135042,5.68757754432826));
#129152=CARTESIAN_POINT('Ctrl Pts',(16.4412787784145,14.0506891607529,5.68285950682528));
#129153=CARTESIAN_POINT('Ctrl Pts',(16.442038790653,14.048614225378,5.67179151136174));
#129154=CARTESIAN_POINT('Ctrl Pts',(16.4424774909826,14.0474886042698,5.66543654796761));
#129155=CARTESIAN_POINT('Ctrl Pts',(16.4439142669754,14.0440324656431,5.64471824224573));
#129156=CARTESIAN_POINT('Ctrl Pts',(16.4449233431192,14.0419626826163,5.63031403658809));
#129157=CARTESIAN_POINT('Ctrl Pts',(16.4486344742756,14.0356099088061,5.57769211828947));
#129158=CARTESIAN_POINT('Ctrl Pts',(16.4513896445024,14.0332831717413,5.53927576511434));
#129159=CARTESIAN_POINT('Ctrl Pts',(16.4541432617404,14.0332503521631,5.50082517101239));
#129160=CARTESIAN_POINT('Origin',(16.125,15.,5.5));
#129161=CARTESIAN_POINT('',(16.911384655308,14.033250032487,5.49974937350518));
#129162=CARTESIAN_POINT('',(16.8550925403241,14.0332500296882,5.49976041261023));
#129163=CARTESIAN_POINT('',(16.125,14.03325,5.5));
#129164=CARTESIAN_POINT('Ctrl Pts',(16.9113846553004,14.033250032487,5.49974937361882));
#129165=CARTESIAN_POINT('Ctrl Pts',(16.910722591978,14.0332474586815,5.50967740409213));
#129166=CARTESIAN_POINT('Ctrl Pts',(16.9100652231276,14.0333978184175,5.5196051809349));
#129167=CARTESIAN_POINT('Ctrl Pts',(16.908823664226,14.0339746734881,5.5384819026576));
#129168=CARTESIAN_POINT('Ctrl Pts',(16.9082386691869,14.0343726731809,5.54743061083325));
#129169=CARTESIAN_POINT('Ctrl Pts',(16.9068951742441,14.0355799149497,5.56809866600091));
#129170=CARTESIAN_POINT('Ctrl Pts',(16.9061394777521,14.036478505235,5.5798115085104));
#129171=CARTESIAN_POINT('Ctrl Pts',(16.9036296233975,14.0402011406127,5.61896435540944));
#129172=CARTESIAN_POINT('Ctrl Pts',(16.901904477747,14.0439860138778,5.64630047089543));
#129173=CARTESIAN_POINT('Ctrl Pts',(16.8974906322489,14.0568296250312,5.71672920919216));
#129174=CARTESIAN_POINT('Ctrl Pts',(16.8948465495084,14.0676708796551,5.75943127139042));
#129175=CARTESIAN_POINT('Ctrl Pts',(16.8890682674937,14.0975656420813,5.85059168347836));
#129176=CARTESIAN_POINT('Ctrl Pts',(16.8859409490176,14.1176953015698,5.89854672736554));
#129177=CARTESIAN_POINT('Ctrl Pts',(16.8819682217545,14.1464272611037,5.95401591983493));
#129178=CARTESIAN_POINT('Ctrl Pts',(16.8812902124078,14.1514326801779,5.96330374323185));
#129179=CARTESIAN_POINT('Ctrl Pts',(16.8802253161108,14.1594291590603,5.97757721348987));
#129180=CARTESIAN_POINT('Ctrl Pts',(16.879844470719,14.1623150406497,5.98262121606706));
#129181=CARTESIAN_POINT('Ctrl Pts',(16.879123258347,14.1678242279252,5.99205199962114));
#129182=CARTESIAN_POINT('Ctrl Pts',(16.8787835116746,14.1704371221735,5.9964444710351));
#129183=CARTESIAN_POINT('Ctrl Pts',(16.8779493048055,14.1768974477284,6.0071113500585));
#129184=CARTESIAN_POINT('Ctrl Pts',(16.8774526251604,14.1807818848317,6.0133628391683));
#129185=CARTESIAN_POINT('Ctrl Pts',(16.8755515649647,14.1958065530678,6.03693824574563));
#129186=CARTESIAN_POINT('Ctrl Pts',(16.8741218860787,14.2074273600083,6.05394788509376));
#129187=CARTESIAN_POINT('Ctrl Pts',(16.8700335599523,14.2417646883502,6.10091388255471));
#129188=CARTESIAN_POINT('Ctrl Pts',(16.8673386323229,14.2656976179819,6.12993497786153));
#129189=CARTESIAN_POINT('Ctrl Pts',(16.8602082266237,14.3334494297738,6.20296833316082));
#129190=CARTESIAN_POINT('Ctrl Pts',(16.8558064878986,14.3799265831757,6.24428844486873));
#129191=CARTESIAN_POINT('Ctrl Pts',(16.8504771195553,14.4431241602897,6.29041562587712));
#129192=CARTESIAN_POINT('Ctrl Pts',(16.849386414791,14.4564366207541,6.29962895636266));
#129193=CARTESIAN_POINT('Ctrl Pts',(16.8476576294941,14.478138894016,6.31385615695651));
#129194=CARTESIAN_POINT('Ctrl Pts',(16.8470118332279,14.4863837594538,6.31908438348582));
#129195=CARTESIAN_POINT('Ctrl Pts',(16.8457789939215,14.5023836374572,6.32889360377174));
#129196=CARTESIAN_POINT('Ctrl Pts',(16.8451913415545,14.510126203826,6.33349284546529));
#129197=CARTESIAN_POINT('Ctrl Pts',(16.8438223172555,14.5284283177165,6.34402152846769));
#129198=CARTESIAN_POINT('Ctrl Pts',(16.8430441167207,14.5390373842813,6.34986215334015));
#129199=CARTESIAN_POINT('Ctrl Pts',(16.8403441665956,14.5765263065262,6.36959237410414));
#129200=CARTESIAN_POINT('Ctrl Pts',(16.8384581922771,14.6039470660083,6.38241894544169));
#129201=CARTESIAN_POINT('Ctrl Pts',(16.8333947240324,14.6801690559781,6.41380284982873));
#129202=CARTESIAN_POINT('Ctrl Pts',(16.8302832731761,14.7299403522012,6.42972868612837));
#129203=CARTESIAN_POINT('Ctrl Pts',(16.8247147870982,14.819658492454,6.45061984351347));
#129204=CARTESIAN_POINT('Ctrl Pts',(16.8222788972086,14.8590827936255,6.45725798414191));
#129205=CARTESIAN_POINT('Ctrl Pts',(16.8190621143444,14.9094068158703,6.46255502989904));
#129206=CARTESIAN_POINT('Ctrl Pts',(16.8183769500227,14.9200307357841,6.46349582533969));
#129207=CARTESIAN_POINT('Ctrl Pts',(16.8173032070364,14.936488176329,6.46467915180172));
#129208=CARTESIAN_POINT('Ctrl Pts',(16.8169208292091,14.9423123203824,6.46504494458908));
#129209=CARTESIAN_POINT('Ctrl Pts',(16.8161986025968,14.9532355788995,6.46563176163025));
#129210=CARTESIAN_POINT('Ctrl Pts',(16.8158594038163,14.958333685168,6.46586516840361));
#129211=CARTESIAN_POINT('Ctrl Pts',(16.8150291884122,14.9707377684582,6.46633468153167));
#129212=CARTESIAN_POINT('Ctrl Pts',(16.8145360044032,14.978044920341,6.46652830351683));
#129213=CARTESIAN_POINT('Ctrl Pts',(16.8126667326163,15.0055368568391,6.46694486690711));
#129214=CARTESIAN_POINT('Ctrl Pts',(16.8112663728499,15.0257235704931,6.46661843878813));
#129215=CARTESIAN_POINT('Ctrl Pts',(16.8073003940887,15.0821330983503,6.46393812402135));
#129216=CARTESIAN_POINT('Ctrl Pts',(16.8047006255862,15.1182553128496,6.46017603440518));
#129217=CARTESIAN_POINT('Ctrl Pts',(16.797520420676,15.2172740764911,6.44419026845684));
#129218=CARTESIAN_POINT('Ctrl Pts',(16.7929727018695,15.2793090980343,6.42773493158762));
#129219=CARTESIAN_POINT('Ctrl Pts',(16.7875152258932,15.3543498916327,6.3996116407535));
#129220=CARTESIAN_POINT('Ctrl Pts',(16.7864301411606,15.3692881794249,6.39358337175345));
#129221=CARTESIAN_POINT('Ctrl Pts',(16.7847079960367,15.3930133570444,6.38331254069949));
#129222=CARTESIAN_POINT('Ctrl Pts',(16.7840633258956,15.4018982705841,6.37930559823286));
#129223=CARTESIAN_POINT('Ctrl Pts',(16.7828312746443,15.4188782708008,6.37133675834002));
#129224=CARTESIAN_POINT('Ctrl Pts',(16.7822433039227,15.4269814876039,6.36739470278409));
#129225=CARTESIAN_POINT('Ctrl Pts',(16.7808714812237,15.445877599647,6.35787313357056));
#129226=CARTESIAN_POINT('Ctrl Pts',(16.7800908408755,15.4566229172235,6.35220225272463));
#129227=CARTESIAN_POINT('Ctrl Pts',(16.7773691929045,15.4940131424312,6.33155910860444));
#129228=CARTESIAN_POINT('Ctrl Pts',(16.7754647837142,15.5200535215782,6.31552690515192));
#129229=CARTESIAN_POINT('Ctrl Pts',(16.7703198165967,15.5892428407727,6.26826515838282));
#129230=CARTESIAN_POINT('Ctrl Pts',(16.7671483833251,15.6306385652376,6.23466564678162));
#129231=CARTESIAN_POINT('Ctrl Pts',(16.7613904788051,15.6993397794273,6.16879686047644));
#129232=CARTESIAN_POINT('Ctrl Pts',(16.7588265489346,15.7276954720618,6.13782746089455));
#129233=CARTESIAN_POINT('Ctrl Pts',(16.7555740984933,15.7594917242494,6.09821095266105));
#129234=CARTESIAN_POINT('Ctrl Pts',(16.7550016647922,15.7649406602564,6.09122736417949));
#129235=CARTESIAN_POINT('Ctrl Pts',(16.7540704140971,15.7735534701889,6.07987042712077));
#129236=CARTESIAN_POINT('Ctrl Pts',(16.7537155401315,15.7767781464483,6.07554356157806));
#129237=CARTESIAN_POINT('Ctrl Pts',(16.7530040964841,15.7831248005238,6.0668771352577));
#129238=CARTESIAN_POINT('Ctrl Pts',(16.7526475803723,15.7862473360622,6.06253823203378));
#129239=CARTESIAN_POINT('Ctrl Pts',(16.751710399795,15.7943096013112,6.05113709303652));
#129240=CARTESIAN_POINT('Ctrl Pts',(16.7511261850026,15.7991910527928,6.04403445361888));
#129241=CARTESIAN_POINT('Ctrl Pts',(16.7480641970405,15.8240649718226,6.0067849656158));
#129242=CARTESIAN_POINT('Ctrl Pts',(16.7455082066664,15.8424471174724,5.9756011215326));
#129243=CARTESIAN_POINT('Ctrl Pts',(16.7369345298998,15.8975883232977,5.86878676568718));
#129244=CARTESIAN_POINT('Ctrl Pts',(16.7308865213051,15.9262454603174,5.78938371741908));
#129245=CARTESIAN_POINT('Ctrl Pts',(16.7241710170971,15.9474549918226,5.69275706396799));
#129246=CARTESIAN_POINT('Ctrl Pts',(16.7231726720834,15.9503052055342,5.67817492650931));
#129247=CARTESIAN_POINT('Ctrl Pts',(16.7215531045044,15.954424851388,5.65417185932061));
#129248=CARTESIAN_POINT('Ctrl Pts',(16.7209258393961,15.9558933917605,5.64478809852231));
#129249=CARTESIAN_POINT('Ctrl Pts',(16.7197041340052,15.9585015896906,5.62634700166048));
#129250=CARTESIAN_POINT('Ctrl Pts',(16.7191094309115,15.9596517159774,5.6172921804736));
#129251=CARTESIAN_POINT('Ctrl Pts',(16.7176847048384,15.9621154734428,5.59542174078066));
#129252=CARTESIAN_POINT('Ctrl Pts',(16.7168586575583,15.963301541918,5.58259332227013));
#129253=CARTESIAN_POINT('Ctrl Pts',(16.7136804158573,15.9669085881357,5.53272525118239));
#129254=CARTESIAN_POINT('Ctrl Pts',(16.7113847200973,15.967452350495,5.49558023103665));
#129255=CARTESIAN_POINT('Ctrl Pts',(16.7066924784334,15.9641469321776,5.41866437599519));
#129256=CARTESIAN_POINT('Ctrl Pts',(16.7043057034882,15.9599734353505,5.3789798938508));
#129257=CARTESIAN_POINT('Ctrl Pts',(16.6992901692353,15.946190672637,5.29702625274794));
#129258=CARTESIAN_POINT('Ctrl Pts',(16.6966634366622,15.936167777227,5.25491990815527));
#129259=CARTESIAN_POINT('Ctrl Pts',(16.6932293609409,15.9201576196384,5.20329717744535));
#129260=CARTESIAN_POINT('Ctrl Pts',(16.6925346250582,15.9167797964256,5.19301890619807));
#129261=CARTESIAN_POINT('Ctrl Pts',(16.6914490538474,15.9113049731542,5.17725669058079));
#129262=CARTESIAN_POINT('Ctrl Pts',(16.691064635239,15.909329199215,5.17173120609542));
#129263=CARTESIAN_POINT('Ctrl Pts',(16.6903410072991,15.9055443871085,5.16144294438672));
#129264=CARTESIAN_POINT('Ctrl Pts',(16.6900024871061,15.9037478135518,5.15667595237395));
#129265=CARTESIAN_POINT('Ctrl Pts',(16.6891773534538,15.8993049996095,5.14516401496963));
#129266=CARTESIAN_POINT('Ctrl Pts',(16.6886886391605,15.8966204877207,5.13843430488806));
#129267=CARTESIAN_POINT('Ctrl Pts',(16.6868591227057,15.8863663849603,5.11354528287289));
#129268=CARTESIAN_POINT('Ctrl Pts',(16.6854953014026,15.8783190947426,5.09558923301205));
#129269=CARTESIAN_POINT('Ctrl Pts',(16.6816779497534,15.8545668166931,5.04664890168829));
#129270=CARTESIAN_POINT('Ctrl Pts',(16.6791928053261,15.837731393548,5.01624638270794));
#129271=CARTESIAN_POINT('Ctrl Pts',(16.6719404923326,15.7839566058063,4.93039481894949));
#129272=CARTESIAN_POINT('Ctrl Pts',(16.6672034656906,15.7428760795483,4.87776546378233));
#129273=CARTESIAN_POINT('Ctrl Pts',(16.6615859365329,15.6856637005044,4.81829292537741));
#129274=CARTESIAN_POINT('Ctrl Pts',(16.6605132186048,15.6743390377175,4.8070886361339));
#129275=CARTESIAN_POINT('Ctrl Pts',(16.6588056894579,15.655672637336,4.78951196712998));
#129276=CARTESIAN_POINT('Ctrl Pts',(16.6581634997823,15.6485030753689,4.78296190831898));
#129277=CARTESIAN_POINT('Ctrl Pts',(16.6569331410993,15.6344828706865,4.77053548728371));
#129278=CARTESIAN_POINT('Ctrl Pts',(16.656344426411,15.6276462738187,4.76464488001068));
#129279=CARTESIAN_POINT('Ctrl Pts',(16.6549662139003,15.6113458091015,4.75099290076047));
#129280=CARTESIAN_POINT('Ctrl Pts',(16.6541800195706,15.6018149326939,4.74331371020866));
#129281=CARTESIAN_POINT('Ctrl Pts',(16.6514080857931,15.5674193807995,4.71666171008277));
#129282=CARTESIAN_POINT('Ctrl Pts',(16.6494608937632,15.5417818957345,4.69871585199138));
#129283=CARTESIAN_POINT('Ctrl Pts',(16.6441196988179,15.4681169165145,4.65230649772788));
#129284=CARTESIAN_POINT('Ctrl Pts',(16.6408026374728,15.4184317689345,4.62671160424633));
#129285=CARTESIAN_POINT('Ctrl Pts',(16.6350836845776,15.3311617802197,4.59092217403918));
#129286=CARTESIAN_POINT('Ctrl Pts',(16.6327189763895,15.2946684535178,4.57844670472949));
#129287=CARTESIAN_POINT('Ctrl Pts',(16.6296873015446,15.249037595778,4.56583539152958));
#129288=CARTESIAN_POINT('Ctrl Pts',(16.6291176473684,15.2405112397574,4.56360394578876));
#129289=CARTESIAN_POINT('Ctrl Pts',(16.6281898135247,15.2267263023727,4.56019695364344));
#129290=CARTESIAN_POINT('Ctrl Pts',(16.6278355249798,15.2214861144497,4.55894820555222));
#129291=CARTESIAN_POINT('Ctrl Pts',(16.6271240585719,15.2110169650254,4.55654566888808));
#129292=CARTESIAN_POINT('Ctrl Pts',(16.6267669193632,15.2057883137802,4.55539140341949));
#129293=CARTESIAN_POINT('Ctrl Pts',(16.6258262241626,15.192078412871,4.55248406344509));
#129294=CARTESIAN_POINT('Ctrl Pts',(16.625239071707,15.1835829077889,4.5508014590996));
#129295=CARTESIAN_POINT('Ctrl Pts',(16.6221123506709,15.1386083147418,4.54252020987332));
#129296=CARTESIAN_POINT('Ctrl Pts',(16.6194907027615,15.1017977471797,4.53791034808294));
#129297=CARTESIAN_POINT('Ctrl Pts',(16.6109699957622,14.9826570388743,4.52990433464539));
#129298=CARTESIAN_POINT('Ctrl Pts',(16.6050481110505,14.9001097649352,4.53490254373228));
#129299=CARTESIAN_POINT('Ctrl Pts',(16.5984173802141,14.8042454493938,4.55315412532811));
#129300=CARTESIAN_POINT('Ctrl Pts',(16.5973943424893,14.7893708661188,4.5563515663927));
#129301=CARTESIAN_POINT('Ctrl Pts',(16.5957455680379,14.7652732534682,4.56212982900395));
#129302=CARTESIAN_POINT('Ctrl Pts',(16.5951133555927,14.756002666161,4.56449884273853));
#129303=CARTESIAN_POINT('Ctrl Pts',(16.5938891134411,14.7379984196507,4.56938551773038));
#129304=CARTESIAN_POINT('Ctrl Pts',(16.5932967230474,14.729262114151,4.57188947367142));
#129305=CARTESIAN_POINT('Ctrl Pts',(16.5918891745671,14.7084565118162,4.5781714563502));
#129306=CARTESIAN_POINT('Ctrl Pts',(16.5910777428068,14.6964233240763,4.58206389402215));
#129307=CARTESIAN_POINT('Ctrl Pts',(16.588059211781,14.6515723725843,4.59755055430368));
#129308=CARTESIAN_POINT('Ctrl Pts',(16.5859010752542,14.6193106210243,4.61067847553064));
#129309=CARTESIAN_POINT('Ctrl Pts',(16.5793696922586,14.5226075670663,4.65625822629943));
#129310=CARTESIAN_POINT('Ctrl Pts',(16.5751347381663,14.4610394559672,4.6941936334867));
#129311=CARTESIAN_POINT('Ctrl Pts',(16.5693999989503,14.3882122331714,4.75117644735603));
#129312=CARTESIAN_POINT('Ctrl Pts',(16.5681173765514,14.3725624515576,4.76423986104643));
#129313=CARTESIAN_POINT('Ctrl Pts',(16.5663198529068,14.3517137826407,4.7827920595763));
#129314=CARTESIAN_POINT('Ctrl Pts',(16.5658308832474,14.3461480410818,4.78786247339973));
#129315=CARTESIAN_POINT('Ctrl Pts',(16.5650037989226,14.3369221373835,4.79646664092949));
#129316=CARTESIAN_POINT('Ctrl Pts',(16.5646681892916,14.3332294985236,4.79996533190271));
#129317=CARTESIAN_POINT('Ctrl Pts',(16.5639507345624,14.3254471500835,4.80745637165969));
#129318=CARTESIAN_POINT('Ctrl Pts',(16.5635683839398,14.3213650110284,4.81145604917722));
#129319=CARTESIAN_POINT('Ctrl Pts',(16.5624845850809,14.309969797889,4.8228208453607));
#129320=CARTESIAN_POINT('Ctrl Pts',(16.5617774719141,14.3027397517412,4.83026765593785));
#129321=CARTESIAN_POINT('Ctrl Pts',(16.5585435256585,14.2705308679322,4.86452909227338));
#129322=CARTESIAN_POINT('Ctrl Pts',(16.5559443718893,14.2469709234164,4.89263253700157));
#129323=CARTESIAN_POINT('Ctrl Pts',(16.5476205321475,14.1773065216971,4.9860332539458));
#129324=CARTESIAN_POINT('Ctrl Pts',(16.5418885724131,14.137658548171,5.05575003399312));
#129325=CARTESIAN_POINT('Ctrl Pts',(16.5354367067997,14.1012612721259,5.14348682852336));
#129326=CARTESIAN_POINT('Ctrl Pts',(16.5344228548407,14.0958096300957,5.15754889386116));
#129327=CARTESIAN_POINT('Ctrl Pts',(16.5327849463205,14.087449077433,5.18070794742554));
#129328=CARTESIAN_POINT('Ctrl Pts',(16.5321545763732,14.084342171256,5.18973019376714));
#129329=CARTESIAN_POINT('Ctrl Pts',(16.5309313227458,14.0785336025763,5.20744560154263));
#129330=CARTESIAN_POINT('Ctrl Pts',(16.5303381142771,14.0758201505584,5.21613381187037));
#129331=CARTESIAN_POINT('Ctrl Pts',(16.5289244020121,14.0696066304717,5.23706312416377));
#129332=CARTESIAN_POINT('Ctrl Pts',(16.5281077138256,14.0662248220311,5.24933774989583));
#129333=CARTESIAN_POINT('Ctrl Pts',(16.5260929010747,14.0584149444219,5.28004041956747));
#129334=CARTESIAN_POINT('Ctrl Pts',(16.5249038099647,14.0542843225235,5.29853893911191));
#129335=CARTESIAN_POINT('Ctrl Pts',(16.5199014228883,14.0390423622615,5.37766950115862));
#129336=CARTESIAN_POINT('Ctrl Pts',(16.5162320247279,14.0331991100086,5.4391667218192));
#129337=CARTESIAN_POINT('Ctrl Pts',(16.5125067604658,14.0332503338485,5.50080342759133));
#129338=CARTESIAN_POINT('Ctrl Pts',(16.4541432558754,14.033250352233,5.50082525291021));
#129339=CARTESIAN_POINT('Ctrl Pts',(16.4577492683692,14.0332073689333,5.45047209538164));
#129340=CARTESIAN_POINT('Ctrl Pts',(16.4613404233998,14.0370984091453,5.40018751979066));
#129341=CARTESIAN_POINT('Ctrl Pts',(16.4662074935876,14.047961835396,5.33081651676039));
#129342=CARTESIAN_POINT('Ctrl Pts',(16.467567718699,14.0516370512099,5.31130043020353));
#129343=CARTESIAN_POINT('Ctrl Pts',(16.469589386071,14.0580738138264,5.28209728475257));
#129344=CARTESIAN_POINT('Ctrl Pts',(16.4702640356312,14.0603896333483,5.27231841289181));
#129345=CARTESIAN_POINT('Ctrl Pts',(16.4715763064844,14.0652240576706,5.25323624215563));
#129346=CARTESIAN_POINT('Ctrl Pts',(16.4722142356759,14.0677301369894,5.24393100865256));
#129347=CARTESIAN_POINT('Ctrl Pts',(16.4734168511111,14.0727507660036,5.22634081656036));
#129348=CARTESIAN_POINT('Ctrl Pts',(16.4739823312114,14.0752382786214,5.2180491934416));
#129349=CARTESIAN_POINT('Ctrl Pts',(16.4752640657037,14.0811649915053,5.19921651630696));
#129350=CARTESIAN_POINT('Ctrl Pts',(16.4759779790741,14.0846748682881,5.18869886563752));
#129351=CARTESIAN_POINT('Ctrl Pts',(16.4782442391774,14.0964791419248,5.15525372626674));
#129352=CARTESIAN_POINT('Ctrl Pts',(16.4797745564303,14.1054604406175,5.13257782352961));
#129353=CARTESIAN_POINT('Ctrl Pts',(16.4860452502861,14.1462851837861,5.03990462906871));
#129354=CARTESIAN_POINT('Ctrl Pts',(16.4905558747543,14.1855604851074,4.97349795682848));
#129355=CARTESIAN_POINT('Ctrl Pts',(16.4970038522702,14.2495245613705,4.88992069758252));
#129356=CARTESIAN_POINT('Ctrl Pts',(16.4987685818631,14.2677452146626,4.86816713698991));
#129357=CARTESIAN_POINT('Ctrl Pts',(16.5011027970571,14.2922777440739,4.8413662981037));
#129358=CARTESIAN_POINT('Ctrl Pts',(16.5016195100263,14.2977340629855,4.83555159070076));
#129359=CARTESIAN_POINT('Ctrl Pts',(16.5024752131884,14.3067977113262,4.82612896656773));
#129360=CARTESIAN_POINT('Ctrl Pts',(16.5028111621358,14.3103629289267,4.82248078178033));
#129361=CARTESIAN_POINT('Ctrl Pts',(16.5035001287505,14.3176838336843,4.81510716595803));
#129362=CARTESIAN_POINT('Ctrl Pts',(16.5038532788591,14.3214415166913,4.81138405012056));
#129363=CARTESIAN_POINT('Ctrl Pts',(16.5048045640416,14.3315822756947,4.80150017449722));
#129364=CARTESIAN_POINT('Ctrl Pts',(16.5054066243292,14.338019756029,4.79539627912919));
#129365=CARTESIAN_POINT('Ctrl Pts',(16.5093524567836,14.3803912764152,4.75631362258508));
#129366=CARTESIAN_POINT('Ctrl Pts',(16.5128376484093,14.4186902908159,4.72600870603662));
#129367=CARTESIAN_POINT('Ctrl Pts',(16.5196142636065,14.4971245794882,4.67306242555056));
#129368=CARTESIAN_POINT('Ctrl Pts',(16.5228963967761,14.5369225140144,4.65013573330969));
#129369=CARTESIAN_POINT('Ctrl Pts',(16.5282825965558,14.6062192200502,4.61653415054145));
#129370=CARTESIAN_POINT('Ctrl Pts',(16.5304243453575,14.6348804745803,4.60430848344764));
#129371=CARTESIAN_POINT('Ctrl Pts',(16.5333289622871,14.6753303280665,4.58931948725682));
#129372=CARTESIAN_POINT('Ctrl Pts',(16.5341297289252,14.6866529407139,4.58536180141236));
#129373=CARTESIAN_POINT('Ctrl Pts',(16.5355032886334,14.7063640294383,4.57888104168893));
#129374=CARTESIAN_POINT('Ctrl Pts',(16.536079196528,14.7147183361072,4.57625945243649));
#129375=CARTESIAN_POINT('Ctrl Pts',(16.5372610234662,14.7320421497631,4.57108067199679));
#129376=CARTESIAN_POINT('Ctrl Pts',(16.5378663925751,14.7410153825975,4.56853904791834));
#129377=CARTESIAN_POINT('Ctrl Pts',(16.5394369651613,14.7645430871475,4.5622412329812));
#129378=CARTESIAN_POINT('Ctrl Pts',(16.5403955446741,14.7791511530601,4.55869383939881));
#129379=CARTESIAN_POINT('Ctrl Pts',(16.5459681657394,14.8653699496281,4.5398744242856));
#129380=CARTESIAN_POINT('Ctrl Pts',(16.5503267443039,14.938445219751,4.53243687462884));
#129381=CARTESIAN_POINT('Ctrl Pts',(16.5566491452149,15.0432028731231,4.53370092938054));
#129382=CARTESIAN_POINT('Ctrl Pts',(16.5585634799895,15.0747019441898,4.53562468080008));
#129383=CARTESIAN_POINT('Ctrl Pts',(16.5616784295267,15.1244061029229,4.54111012605176));
#129384=CARTESIAN_POINT('Ctrl Pts',(16.5628455441274,15.1427005859471,4.54366161135976));
#129385=CARTESIAN_POINT('Ctrl Pts',(16.5644868413208,15.1677674237073,4.54789284924952));
#129386=CARTESIAN_POINT('Ctrl Pts',(16.5649394006561,15.1746125074586,4.54912440328838));
#129387=CARTESIAN_POINT('Ctrl Pts',(16.5657190650942,15.1862783014608,4.55135349786119));
#129388=CARTESIAN_POINT('Ctrl Pts',(16.5660441801748,15.1911057060802,4.55231418727267));
#129389=CARTESIAN_POINT('Ctrl Pts',(16.5667487021835,15.2014830338668,4.55446186980962));
#129390=CARTESIAN_POINT('Ctrl Pts',(16.5671287004404,15.2070299042807,4.55566087479577));
#129391=CARTESIAN_POINT('Ctrl Pts',(16.568213684381,15.2227346182274,4.55920059952101));
#129392=CARTESIAN_POINT('Ctrl Pts',(16.5689244241698,15.2328652924451,4.56165680231362));
#129393=CARTESIAN_POINT('Ctrl Pts',(16.5732292155071,15.2934037810622,4.57737517335253));
#129394=CARTESIAN_POINT('Ctrl Pts',(16.5769711597976,15.3427078305578,4.59453169463096));
#129395=CARTESIAN_POINT('Ctrl Pts',(16.5838758107612,15.4309279975056,4.63347207096091));
#129396=CARTESIAN_POINT('Ctrl Pts',(16.5870341162533,15.4701960469196,4.65413600602973));
#129397=CARTESIAN_POINT('Ctrl Pts',(16.5920375085859,15.5313702352451,4.69190876932637));
#129398=CARTESIAN_POINT('Ctrl Pts',(16.5939263652396,15.5542014486246,4.70739242595949));
#129399=CARTESIAN_POINT('Ctrl Pts',(16.5965547092106,15.5855928009859,4.73070199922148));
#129400=CARTESIAN_POINT('Ctrl Pts',(16.597323051384,15.5947209651479,4.73773670201446));
#129401=CARTESIAN_POINT('Ctrl Pts',(16.5986595797358,15.610506368952,4.75035808568265));
#129402=CARTESIAN_POINT('Ctrl Pts',(16.5992304183465,15.6172179687675,4.75587432952845));
#129403=CARTESIAN_POINT('Ctrl Pts',(16.60041901472,15.6311230113808,4.76762042777011));
#129404=CARTESIAN_POINT('Ctrl Pts',(16.6010359956504,15.6383006916517,4.77386755285905));
#129405=CARTESIAN_POINT('Ctrl Pts',(16.6026774925372,15.6572764877867,4.7908820496721));
#129406=CARTESIAN_POINT('Ctrl Pts',(16.6036941867412,15.6689022290665,4.80183776799269));
#129407=CARTESIAN_POINT('Ctrl Pts',(16.6086619625971,15.7249339115653,4.85732528196518));
#129408=CARTESIAN_POINT('Ctrl Pts',(16.6124368613394,15.7651934791043,4.90582840789248));
#129409=CARTESIAN_POINT('Ctrl Pts',(16.6184807699982,15.8214823708443,4.98894437616548));
#129410=CARTESIAN_POINT('Ctrl Pts',(16.620740226256,15.8406803762178,5.02118134671776));
#129411=CARTESIAN_POINT('Ctrl Pts',(16.6243356693383,15.8673882376748,5.07261027315677));
#129412=CARTESIAN_POINT('Ctrl Pts',(16.6256243779527,15.8762398014624,5.09106477887754));
#129413=CARTESIAN_POINT('Ctrl Pts',(16.6274083620437,15.8874074814116,5.11637848808386));
#129414=CARTESIAN_POINT('Ctrl Pts',(16.6278767966389,15.8902425342599,5.12300434328766));
#129415=CARTESIAN_POINT('Ctrl Pts',(16.6286748033118,15.8949031256783,5.13424248769473));
#129416=CARTESIAN_POINT('Ctrl Pts',(16.6290021405767,15.8967677814178,5.13883839157188));
#129417=CARTESIAN_POINT('Ctrl Pts',(16.6297005939926,15.9006454065563,5.14861095413516));
#129418=CARTESIAN_POINT('Ctrl Pts',(16.6300721736769,15.9026492319637,5.15379085765597));
#129419=CARTESIAN_POINT('Ctrl Pts',(16.6311283539098,15.9081823120758,5.16846853409687));
#129420=CARTESIAN_POINT('Ctrl Pts',(16.6318184044622,15.9116069314338,5.1780046461681));
#129421=CARTESIAN_POINT('Ctrl Pts',(16.6373711950775,15.9377111408106,5.25445041226836));
#129422=CARTESIAN_POINT('Ctrl Pts',(16.6425040130643,15.9531427938087,5.32360587469783));
#129423=CARTESIAN_POINT('Ctrl Pts',(16.6498830525655,15.9645314738898,5.42667248032859));
#129424=CARTESIAN_POINT('Ctrl Pts',(16.6522104045477,15.9664746773638,5.45968972349377));
#129425=CARTESIAN_POINT('Ctrl Pts',(16.656081946325,15.9668953071581,5.51573187300437));
#129426=CARTESIAN_POINT('Ctrl Pts',(16.6576478452531,15.9662478696983,5.5387198678485));
#129427=CARTESIAN_POINT('Ctrl Pts',(16.6599144857269,15.9640912692188,5.57246123581872));
#129428=CARTESIAN_POINT('Ctrl Pts',(16.6606342214679,15.9632199882089,5.58324587890658));
#129429=CARTESIAN_POINT('Ctrl Pts',(16.6619168971444,15.9613303452022,5.60258505868069));
#129430=CARTESIAN_POINT('Ctrl Pts',(16.662481810538,15.9603783508253,5.61114476189332));
#129431=CARTESIAN_POINT('Ctrl Pts',(16.6636895443819,15.9580846168396,5.62952884858735));
#129432=CARTESIAN_POINT('Ctrl Pts',(16.6643311561,15.9567058547271,5.63934767635601));
#129433=CARTESIAN_POINT('Ctrl Pts',(16.6660922396773,15.952478037983,5.66642428671286));
#129434=CARTESIAN_POINT('Ctrl Pts',(16.6672018960184,15.9493112665748,5.68362906504903));
#129435=CARTESIAN_POINT('Ctrl Pts',(16.6737376463509,15.9276825066201,5.7855217632913));
#129436=CARTESIAN_POINT('Ctrl Pts',(16.6788044644982,15.8983684825073,5.86749295277333));
#129437=CARTESIAN_POINT('Ctrl Pts',(16.6859044763998,15.8450205182713,5.97054059516908));
#129438=CARTESIAN_POINT('Ctrl Pts',(16.6877291085472,15.8303377741881,5.99599090598995));
#129439=CARTESIAN_POINT('Ctrl Pts',(16.6901318688781,15.8101855391817,6.02751279173809));
#129440=CARTESIAN_POINT('Ctrl Pts',(16.6906533250202,15.8057655100517,6.03423991427185));
#129441=CARTESIAN_POINT('Ctrl Pts',(16.691514800342,15.7983995220895,6.04515130221034));
#129442=CARTESIAN_POINT('Ctrl Pts',(16.6918516960913,15.7955033100058,6.04936892968048));
#129443=CARTESIAN_POINT('Ctrl Pts',(16.6924971185142,15.7899287159527,6.05735045108545));
#129444=CARTESIAN_POINT('Ctrl Pts',(16.6928051985276,15.7872565774454,6.06111850861464));
#129445=CARTESIAN_POINT('Ctrl Pts',(16.6936577687543,15.7798283365891,6.07143577102364));
#129446=CARTESIAN_POINT('Ctrl Pts',(16.6942057304948,15.775016947922,6.07794445658906));
#129447=CARTESIAN_POINT('Ctrl Pts',(16.6966282195673,15.753561397556,6.10621906632008));
#129448=CARTESIAN_POINT('Ctrl Pts',(16.6985476910468,15.7360791119222,6.12733054324082));
#129449=CARTESIAN_POINT('Ctrl Pts',(16.70514896621,15.673694523376,6.1964630963521));
#129450=CARTESIAN_POINT('Ctrl Pts',(16.7099086123336,15.6247975800173,6.24064446529119));
#129451=CARTESIAN_POINT('Ctrl Pts',(16.7168700271584,15.5447763909791,6.29934166706548));
#129452=CARTESIAN_POINT('Ctrl Pts',(16.7191804824277,15.5167425028217,6.31774447987447));
#129453=CARTESIAN_POINT('Ctrl Pts',(16.7222662663603,15.4772128518769,6.34084720070379));
#129454=CARTESIAN_POINT('Ctrl Pts',(16.7230861742912,15.4665018983319,6.34683653855195));
#129455=CARTESIAN_POINT('Ctrl Pts',(16.7244818609436,15.4479181233561,6.35676855704967));
#129456=CARTESIAN_POINT('Ctrl Pts',(16.7250610327956,15.4401003698626,6.36081047772485));
#129457=CARTESIAN_POINT('Ctrl Pts',(16.7262404048705,15.4239687150931,6.3688736131134));
#129458=CARTESIAN_POINT('Ctrl Pts',(16.7268401737788,15.4156501884027,6.37288358755015));
#129459=CARTESIAN_POINT('Ctrl Pts',(16.7283763261889,15.3940588710247,6.38291309378859));
#129460=CARTESIAN_POINT('Ctrl Pts',(16.7293066400723,15.3807048661396,6.38875292684243));
#129461=CARTESIAN_POINT('Ctrl Pts',(16.735064754792,15.2964549908939,6.42334859678867));
#129462=CARTESIAN_POINT('Ctrl Pts',(16.7396073113771,15.2224884595989,6.44390575556967));
#129463=CARTESIAN_POINT('Ctrl Pts',(16.7460384618295,15.117273962186,6.46007752162148));
#129464=CARTESIAN_POINT('Ctrl Pts',(16.747859590196,15.0874868486499,6.46324859714241));
#129465=CARTESIAN_POINT('Ctrl Pts',(16.7508420704627,15.0397522827032,6.46609786774926));
#129466=CARTESIAN_POINT('Ctrl Pts',(16.7519732958886,15.0218770042431,6.46666780273942));
#129467=CARTESIAN_POINT('Ctrl Pts',(16.7535722616981,14.9971220061422,6.46677016558036));
#129468=CARTESIAN_POINT('Ctrl Pts',(16.7540198116915,14.9902466301316,6.46672524592449));
#129469=CARTESIAN_POINT('Ctrl Pts',(16.7547937816012,14.978461471832,6.46652251925225));
#129470=CARTESIAN_POINT('Ctrl Pts',(16.755118292027,14.9735514166529,6.46640062070721));
#129471=CARTESIAN_POINT('Ctrl Pts',(16.7558251568151,14.9629271825906,6.46605582950888));
#129472=CARTESIAN_POINT('Ctrl Pts',(16.7562081510912,14.9572139922257,6.46581965865952));
#129473=CARTESIAN_POINT('Ctrl Pts',(16.7573101208438,14.94088906367,6.46499969341926));
#129474=CARTESIAN_POINT('Ctrl Pts',(16.7580351190431,14.9302847408845,6.46429159052797));
#129475=CARTESIAN_POINT('Ctrl Pts',(16.7619433771386,14.8737309851228,6.45957753629581));
#129476=CARTESIAN_POINT('Ctrl Pts',(16.7652411643744,14.8281040344634,6.45246206643116));
#129477=CARTESIAN_POINT('Ctrl Pts',(16.7719939355626,14.7362112822387,6.43131216820889));
#129478=CARTESIAN_POINT('Ctrl Pts',(16.775439147838,14.6901288540215,6.41701005926373));
#129479=CARTESIAN_POINT('Ctrl Pts',(16.7808134647503,14.618425303569,6.38873001568306));
#129480=CARTESIAN_POINT('Ctrl Pts',(16.7827957364795,14.5920351733759,6.37692945754169));
#129481=CARTESIAN_POINT('Ctrl Pts',(16.7855268129005,14.5557508971591,6.35871141400187));
#129482=CARTESIAN_POINT('Ctrl Pts',(16.7863076776659,14.545386713048,6.35326979170319));
#129483=CARTESIAN_POINT('Ctrl Pts',(16.7876584290128,14.5274848150553,6.34345175481248));
#129484=CARTESIAN_POINT('Ctrl Pts',(16.7882311453952,14.5199028969711,6.33915924747966));
#129485=CARTESIAN_POINT('Ctrl Pts',(16.789416683242,14.5042321558482,6.33000532742448));
#129486=CARTESIAN_POINT('Ctrl Pts',(16.7900288199479,14.4961543773629,6.32512677667975));
#129487=CARTESIAN_POINT('Ctrl Pts',(16.7916407548668,14.4749327864901,6.31188219004696));
#129488=CARTESIAN_POINT('Ctrl Pts',(16.792633239925,14.4619172714429,6.30331518643864));
#129489=CARTESIAN_POINT('Ctrl Pts',(16.7979392777867,14.3927704155012,6.25536671072528));
#129490=CARTESIAN_POINT('Ctrl Pts',(16.8020357742926,14.3407424019931,6.21041331131239));
#129491=CARTESIAN_POINT('Ctrl Pts',(16.8082183176407,14.2706765056683,6.1354913980108));
#129492=CARTESIAN_POINT('Ctrl Pts',(16.8102760115387,14.2487761335198,6.10944605594021));
#129493=CARTESIAN_POINT('Ctrl Pts',(16.813592405134,14.2166513186919,6.06687219596239));
#129494=CARTESIAN_POINT('Ctrl Pts',(16.8148121208184,14.2054740671771,6.05109679229484));
#129495=CARTESIAN_POINT('Ctrl Pts',(16.8165152777005,14.1908670148169,6.02911182208111));
#129496=CARTESIAN_POINT('Ctrl Pts',(16.8169749074968,14.1870208319777,6.02318292522592));
#129497=CARTESIAN_POINT('Ctrl Pts',(16.817762690725,14.1805981417413,6.01304048949698));
#129498=CARTESIAN_POINT('Ctrl Pts',(16.8180887402015,14.1779883166802,6.00884844567653));
#129499=CARTESIAN_POINT('Ctrl Pts',(16.8187903230788,14.1724778450051,5.99984418787184));
#129500=CARTESIAN_POINT('Ctrl Pts',(16.8191663831388,14.1695869901407,5.99502662392762));
#129501=CARTESIAN_POINT('Ctrl Pts',(16.8202292218785,14.1615874275188,5.98142821056715));
#129502=CARTESIAN_POINT('Ctrl Pts',(16.8209214125889,14.1565750524341,5.97259189779269));
#129503=CARTESIAN_POINT('Ctrl Pts',(16.825476207258,14.1248085285235,5.91447526346422));
#129504=CARTESIAN_POINT('Ctrl Pts',(16.8295118649565,14.1022478816308,5.86302902330676));
#129505=CARTESIAN_POINT('Ctrl Pts',(16.8380189995739,14.0641375266948,5.75042456357647));
#129506=CARTESIAN_POINT('Ctrl Pts',(16.8424598712464,14.0498443458301,5.68909703755364));
#129507=CARTESIAN_POINT('Ctrl Pts',(16.8476617311138,14.0397718628649,5.6129703879532));
#129508=CARTESIAN_POINT('Ctrl Pts',(16.8485982476018,14.0382408361698,5.59909454462267));
#129509=CARTESIAN_POINT('Ctrl Pts',(16.8501309220511,14.036207816555,5.57611319701687));
#129510=CARTESIAN_POINT('Ctrl Pts',(16.8507322783809,14.0355332103842,5.56702546427246));
#129511=CARTESIAN_POINT('Ctrl Pts',(16.8519049668469,14.034461402571,5.54917079393646));
#129512=CARTESIAN_POINT('Ctrl Pts',(16.8524765293193,14.0340548834672,5.54040532443724));
#129513=CARTESIAN_POINT('Ctrl Pts',(16.8537324010243,14.0334200021052,5.5210142334101));
#129514=CARTESIAN_POINT('Ctrl Pts',(16.8544149537548,14.0332473959202,5.51038783667619));
#129515=CARTESIAN_POINT('Ctrl Pts',(16.8550925403141,14.0332500296882,5.49976041276753));
#129516=CARTESIAN_POINT('Origin',(16.125,15.,5.5));
#129517=CARTESIAN_POINT('',(17.3122359168897,14.0332501543841,5.49945364696662));
#129518=CARTESIAN_POINT('',(17.2535750170786,14.0332500522588,5.49945804013099));
#129519=CARTESIAN_POINT('',(16.125,14.03325,5.5));
#129520=CARTESIAN_POINT('Ctrl Pts',(17.3128750435716,14.0332501300013,5.49949864428434));
#129521=CARTESIAN_POINT('Ctrl Pts',(17.3076106834502,14.0332113526949,5.57427181392873));
#129522=CARTESIAN_POINT('Ctrl Pts',(17.3021747516393,14.0418471203054,5.64880226167124));
#129523=CARTESIAN_POINT('Ctrl Pts',(17.2947357824472,14.0662164561492,5.752284734281));
#129524=CARTESIAN_POINT('Ctrl Pts',(17.292566487215,14.0749393927244,5.78259958989893));
#129525=CARTESIAN_POINT('Ctrl Pts',(17.2896163549051,14.0890942041165,5.82404740441688));
#129526=CARTESIAN_POINT('Ctrl Pts',(17.2887969957306,14.0932801184978,5.83558183642833));
#129527=CARTESIAN_POINT('Ctrl Pts',(17.2873870493272,14.1009255159992,5.85546046865153));
#129528=CARTESIAN_POINT('Ctrl Pts',(17.2867932766066,14.1042843680011,5.86384143294114));
#129529=CARTESIAN_POINT('Ctrl Pts',(17.2855696212882,14.1114939264757,5.88112541471665));
#129530=CARTESIAN_POINT('Ctrl Pts',(17.2849403999434,14.1153622147692,5.89002003078127));
#129531=CARTESIAN_POINT('Ctrl Pts',(17.2832930384043,14.1259106864368,5.91331010174951));
#129532=CARTESIAN_POINT('Ctrl Pts',(17.2822823863766,14.1328127302932,5.92760221236292));
#129533=CARTESIAN_POINT('Ctrl Pts',(17.2770426837281,14.1707931681929,6.00154239473592));
#129534=CARTESIAN_POINT('Ctrl Pts',(17.2730195250341,14.2076813252928,6.05799718054965));
#129535=CARTESIAN_POINT('Ctrl Pts',(17.2668946188679,14.271808630087,6.13680625079424));
#129536=CARTESIAN_POINT('Ctrl Pts',(17.264817290618,14.2948858242393,6.16226776039735));
#129537=CARTESIAN_POINT('Ctrl Pts',(17.2614681373421,14.3331437458408,6.2002072822624));
#129538=CARTESIAN_POINT('Ctrl Pts',(17.2602355043746,14.3474336337868,6.21354364003395));
#129539=CARTESIAN_POINT('Ctrl Pts',(17.2585086883526,14.3675485593439,6.23120653248025));
#129540=CARTESIAN_POINT('Ctrl Pts',(17.2580386158929,14.3730335603861,6.23591500458463));
#129541=CARTESIAN_POINT('Ctrl Pts',(17.2572301017247,14.3824714092226,6.24383461351135));
#129542=CARTESIAN_POINT('Ctrl Pts',(17.256893818727,14.3863977191633,6.2470767915406));
#129543=CARTESIAN_POINT('Ctrl Pts',(17.2561645479275,14.3949106209618,6.25399399429277));
#129544=CARTESIAN_POINT('Ctrl Pts',(17.2557709260442,14.3995051728477,6.25765827276294));
#129545=CARTESIAN_POINT('Ctrl Pts',(17.2546424361792,14.412684643902,6.26797407318739));
#129546=CARTESIAN_POINT('Ctrl Pts',(17.2539013435198,14.4213483563214,6.27452292179586));
#129547=CARTESIAN_POINT('Ctrl Pts',(17.2501645016946,14.4651609191952,6.30649516958091));
#129548=CARTESIAN_POINT('Ctrl Pts',(17.2470692405103,14.5018802939441,6.32967670803815));
#129549=CARTESIAN_POINT('Ctrl Pts',(17.2411030261171,14.5751993051432,6.36933819492763));
#129550=CARTESIAN_POINT('Ctrl Pts',(17.238238922729,14.6115185882246,6.38616422425089));
#129551=CARTESIAN_POINT('Ctrl Pts',(17.2328290006973,14.6831020515089,6.41407801536702));
#129552=CARTESIAN_POINT('Ctrl Pts',(17.2302799768547,14.7181672845786,6.42549111755068));
#129553=CARTESIAN_POINT('Ctrl Pts',(17.2269254773766,14.7662332839478,6.43814920446232));
#129554=CARTESIAN_POINT('Ctrl Pts',(17.2260656255764,14.7787287429741,6.44117472596737));
#129555=CARTESIAN_POINT('Ctrl Pts',(17.2246089260312,14.8001885322323,6.44591974111596));
#129556=CARTESIAN_POINT('Ctrl Pts',(17.2240082858064,14.8091233887306,6.44776310755111));
#129557=CARTESIAN_POINT('Ctrl Pts',(17.2227898466543,14.8274182022474,6.45126832472021));
#129558=CARTESIAN_POINT('Ctrl Pts',(17.2221724508821,14.8367792711836,6.45291915010783));
#129559=CARTESIAN_POINT('Ctrl Pts',(17.2205982784343,14.860867425825,6.45680171060259));
#129560=CARTESIAN_POINT('Ctrl Pts',(17.2196477654434,14.8756247882248,6.45883170082973));
#129561=CARTESIAN_POINT('Ctrl Pts',(17.2134058935599,14.9737615870231,6.47002715409928));
#129562=CARTESIAN_POINT('Ctrl Pts',(17.2084648675997,15.0579785886101,6.46864859581226));
#129563=CARTESIAN_POINT('Ctrl Pts',(17.2011657626691,15.1768430759656,6.4511295454358));
#129564=CARTESIAN_POINT('Ctrl Pts',(17.1989333516914,15.2123931904438,6.44382702920944));
#129565=CARTESIAN_POINT('Ctrl Pts',(17.1960568648701,15.2557806244191,6.43233909494369));
#129566=CARTESIAN_POINT('Ctrl Pts',(17.1954991694994,15.2640859761082,6.43002069908999));
#129567=CARTESIAN_POINT('Ctrl Pts',(17.1945860234339,15.2774889558539,6.42608532474093));
#129568=CARTESIAN_POINT('Ctrl Pts',(17.1942342422719,15.2826063337724,6.42453653602264));
#129569=CARTESIAN_POINT('Ctrl Pts',(17.1935224857099,15.2928613489043,6.4213397324722));
#129570=CARTESIAN_POINT('Ctrl Pts',(17.1931624852142,15.2979985474341,6.41969099952346));
#129571=CARTESIAN_POINT('Ctrl Pts',(17.1922057324492,15.3115280410132,6.41522358844941));
#129572=CARTESIAN_POINT('Ctrl Pts',(17.1916051700539,15.3198956787063,6.41233254820179));
#129573=CARTESIAN_POINT('Ctrl Pts',(17.1882035275343,15.3666586414219,6.39545343426489));
#129574=CARTESIAN_POINT('Ctrl Pts',(17.1853033238585,15.4041733134573,6.37915794720899));
#129575=CARTESIAN_POINT('Ctrl Pts',(17.1785224898527,15.4886232866842,6.33592505357763));
#129576=CARTESIAN_POINT('Ctrl Pts',(17.1746423695747,15.5345623865423,6.30732108265115));
#129577=CARTESIAN_POINT('Ctrl Pts',(17.1687135845517,15.6025548972457,6.25662474166392));
#129578=CARTESIAN_POINT('Ctrl Pts',(17.1665966495201,15.6263451525073,6.23705189223996));
#129579=CARTESIAN_POINT('Ctrl Pts',(17.1637032393467,15.658186280762,6.20819818247666));
#129580=CARTESIAN_POINT('Ctrl Pts',(17.1628902218705,15.6670547550369,6.19985128583535));
#129581=CARTESIAN_POINT('Ctrl Pts',(17.1614875324569,15.6822100559904,6.18503741976923));
#129582=CARTESIAN_POINT('Ctrl Pts',(17.1608947683197,15.6885683233384,6.17864607875259));
#129583=CARTESIAN_POINT('Ctrl Pts',(17.1596698938386,15.7016045052249,6.16517023077048));
#129584=CARTESIAN_POINT('Ctrl Pts',(17.1590384893874,15.7082666993586,6.15807188922337));
#129585=CARTESIAN_POINT('Ctrl Pts',(17.1573776708703,15.7256248830882,6.13900830488633));
#129586=CARTESIAN_POINT('Ctrl Pts',(17.1563559789697,15.7361323448849,6.12687502850902));
#129587=CARTESIAN_POINT('Ctrl Pts',(17.1512494606944,15.7876478712169,6.06430597951119));
#129588=CARTESIAN_POINT('Ctrl Pts',(17.1473541269949,15.8237974445655,6.01008739774125));
#129589=CARTESIAN_POINT('Ctrl Pts',(17.1412872704953,15.8709397613192,5.92112050145835));
#129590=CARTESIAN_POINT('Ctrl Pts',(17.1391323573883,15.8858860921251,5.88869534450003));
#129591=CARTESIAN_POINT('Ctrl Pts',(17.1356754834809,15.9063556902626,5.83693385263708));
#129592=CARTESIAN_POINT('Ctrl Pts',(17.1344158063256,15.9131272896578,5.81812496121841));
#129593=CARTESIAN_POINT('Ctrl Pts',(17.132657236626,15.9215646913578,5.7921936920799));
#129594=CARTESIAN_POINT('Ctrl Pts',(17.1321836248819,15.9237402850596,5.78524114725821));
#129595=CARTESIAN_POINT('Ctrl Pts',(17.1313710570111,15.9273049834889,5.77338076043736));
#129596=CARTESIAN_POINT('Ctrl Pts',(17.1310343185989,15.9287341835196,5.76848535864741));
#129597=CARTESIAN_POINT('Ctrl Pts',(17.1303065686542,15.9317190609568,5.75795223002339));
#129598=CARTESIAN_POINT('Ctrl Pts',(17.1299149568862,15.9332623469274,5.7523116110255));
#129599=CARTESIAN_POINT('Ctrl Pts',(17.1287978733808,15.9374902848146,5.73628905782922));
#129600=CARTESIAN_POINT('Ctrl Pts',(17.1280663602916,15.9400534183356,5.72587629572563));
#129601=CARTESIAN_POINT('Ctrl Pts',(17.1244682549607,15.9516954195802,5.67494445831862));
#129602=CARTESIAN_POINT('Ctrl Pts',(17.1215100353092,15.9583298238891,5.63391454531794));
#129603=CARTESIAN_POINT('Ctrl Pts',(17.115635500724,15.9661932762804,5.55218743701533));
#129604=CARTESIAN_POINT('Ctrl Pts',(17.1127255665204,15.9675325326763,5.51157898045148));
#129605=CARTESIAN_POINT('Ctrl Pts',(17.1071807503692,15.9651736725518,5.43296475202831));
#129606=CARTESIAN_POINT('Ctrl Pts',(17.1045445952136,15.9617868950551,5.39502131441314));
#129607=CARTESIAN_POINT('Ctrl Pts',(17.1010989475308,15.9542573127376,5.34454329609833));
#129608=CARTESIAN_POINT('Ctrl Pts',(17.1002310685472,15.9520856128918,5.33175369613272));
#129609=CARTESIAN_POINT('Ctrl Pts',(17.0987650248699,15.9479455349259,5.31003051203689));
#129610=CARTESIAN_POINT('Ctrl Pts',(17.0981629449963,15.9461066260117,5.30107437242908));
#129611=CARTESIAN_POINT('Ctrl Pts',(17.0970185088022,15.9423456152242,5.28399067956057));
#129612=CARTESIAN_POINT('Ctrl Pts',(17.0964755492781,15.9404447164484,5.27585935788927));
#129613=CARTESIAN_POINT('Ctrl Pts',(17.0950495759109,15.935144879374,5.25444430357452));
#129614=CARTESIAN_POINT('Ctrl Pts',(17.0941721933513,15.9315682237453,5.2412062221827));
#129615=CARTESIAN_POINT('Ctrl Pts',(17.0905003492009,15.91527749382,5.18563355136984));
#129616=CARTESIAN_POINT('Ctrl Pts',(17.0877885121062,15.8999491875991,5.14411906482836));
#129617=CARTESIAN_POINT('Ctrl Pts',(17.0821444258943,15.861761526449,5.05912480948116));
#129618=CARTESIAN_POINT('Ctrl Pts',(17.0792283585936,15.8383265517629,5.01604527397734));
#129619=CARTESIAN_POINT('Ctrl Pts',(17.0743944948884,15.7953849086198,4.9496600774261));
#129620=CARTESIAN_POINT('Ctrl Pts',(17.0725268748431,15.7778707715684,4.92517141896538));
#129621=CARTESIAN_POINT('Ctrl Pts',(17.0700655254145,15.7541339990509,4.89505731972667));
#129622=CARTESIAN_POINT('Ctrl Pts',(17.0695308173356,15.7489401261655,4.88863888619985));
#129623=CARTESIAN_POINT('Ctrl Pts',(17.0686457272327,15.7402966441488,4.87823297799517));
#129624=CARTESIAN_POINT('Ctrl Pts',(17.0682985983077,15.7368953493077,4.87420563027202));
#129625=CARTESIAN_POINT('Ctrl Pts',(17.0676305838473,15.7303326208582,4.86656263840618));
#129626=CARTESIAN_POINT('Ctrl Pts',(17.0673101426296,15.7271768718056,4.86294237086507));
#129627=CARTESIAN_POINT('Ctrl Pts',(17.0664151386439,15.7183380351217,4.85295372399721));
#129628=CARTESIAN_POINT('Ctrl Pts',(17.0658366980359,15.7125975323553,4.84663703752501));
#129629=CARTESIAN_POINT('Ctrl Pts',(17.0631093057454,15.68536797257,4.81746014045381));
#129630=CARTESIAN_POINT('Ctrl Pts',(17.0609020262016,15.662859529037,4.79558052407562));
#129631=CARTESIAN_POINT('Ctrl Pts',(17.0542895561488,15.5931180161702,4.73409399612881));
#129632=CARTESIAN_POINT('Ctrl Pts',(17.0498407625908,15.5431131286031,4.69785903847948));
#129633=CARTESIAN_POINT('Ctrl Pts',(17.0432294507842,15.4617877911234,4.65004200277396));
#129634=CARTESIAN_POINT('Ctrl Pts',(17.0409745388417,15.4327503914839,4.63489650243903));
#129635=CARTESIAN_POINT('Ctrl Pts',(17.0379321855195,15.3917147310829,4.61607737208906));
#129636=CARTESIAN_POINT('Ctrl Pts',(17.0371028766634,15.380332729201,4.61112054711191));
#129637=CARTESIAN_POINT('Ctrl Pts',(17.0356815125061,15.3604923986584,4.60293105101111));
#129638=CARTESIAN_POINT('Ctrl Pts',(17.0350861242755,15.3520785333719,4.59959554403789));
#129639=CARTESIAN_POINT('Ctrl Pts',(17.0338641645262,15.3346031637319,4.59295021016647));
#129640=CARTESIAN_POINT('Ctrl Pts',(17.0332381866449,15.3255364459781,4.58965686050631));
#129641=CARTESIAN_POINT('Ctrl Pts',(17.0316107951971,15.301678406688,4.58139282308706));
#129642=CARTESIAN_POINT('Ctrl Pts',(17.0306165280843,15.2868130629751,4.57664345139428));
#129643=CARTESIAN_POINT('Ctrl Pts',(17.0252282402437,15.2048354727992,4.55262317490542));
#129644=CARTESIAN_POINT('Ctrl Pts',(17.0210600363142,15.1359024171776,4.54030632174868));
#129645=CARTESIAN_POINT('Ctrl Pts',(17.0148619787201,15.0333907916218,4.53326595077989));
#129646=CARTESIAN_POINT('Ctrl Pts',(17.0128668623069,15.0004505509173,4.53268970821658));
#129647=CARTESIAN_POINT('Ctrl Pts',(17.0100005204936,14.9544088050621,4.53423614589188));
#129648=CARTESIAN_POINT('Ctrl Pts',(17.0091743169722,14.9412812215649,4.5349453634108));
#129649=CARTESIAN_POINT('Ctrl Pts',(17.0076907795106,14.9180612685299,4.53667533108472));
#129650=CARTESIAN_POINT('Ctrl Pts',(17.0070381170956,14.9079626660079,4.53758767493448));
#129651=CARTESIAN_POINT('Ctrl Pts',(17.0060081867569,14.8922467127321,4.5392571143912));
#129652=CARTESIAN_POINT('Ctrl Pts',(17.0056364732037,14.8866182064168,4.53990509419112));
#129653=CARTESIAN_POINT('Ctrl Pts',(17.0049244580443,14.87592746963,4.54123117809075));
#129654=CARTESIAN_POINT('Ctrl Pts',(17.0045846462763,14.8708643861681,4.54189998691578));
#129655=CARTESIAN_POINT('Ctrl Pts',(17.0037304878003,14.8582299611661,4.54367089424771));
#129656=CARTESIAN_POINT('Ctrl Pts',(17.0032135765452,14.8506660527944,4.54482280928426));
#129657=CARTESIAN_POINT('Ctrl Pts',(17.0012376811162,14.8220326331237,4.54953182639755));
#129658=CARTESIAN_POINT('Ctrl Pts',(16.9997518880061,14.8010706912037,4.55369713058502));
#129659=CARTESIAN_POINT('Ctrl Pts',(16.99324707997,14.7110706753485,4.57470319094223));
#129660=CARTESIAN_POINT('Ctrl Pts',(16.9880862093617,14.6438658312652,4.5984325584684));
#129661=CARTESIAN_POINT('Ctrl Pts',(16.9806629179709,14.5486802568075,4.64436282493202));
#129662=CARTESIAN_POINT('Ctrl Pts',(16.9782724990335,14.5183237146337,4.66107633665176));
#129663=CARTESIAN_POINT('Ctrl Pts',(16.9750854505441,14.478208719315,4.68605967825578));
#129664=CARTESIAN_POINT('Ctrl Pts',(16.9742413867559,14.4676223504203,4.69294420798522));
#129665=CARTESIAN_POINT('Ctrl Pts',(16.9728029987107,14.4496564267965,4.70513520800126));
#129666=CARTESIAN_POINT('Ctrl Pts',(16.9722051209408,14.4422114618579,4.71034181939273));
#129667=CARTESIAN_POINT('Ctrl Pts',(16.9709851476126,14.4270733780262,4.72124952347356));
#129668=CARTESIAN_POINT('Ctrl Pts',(16.9703635507454,14.4193893316038,4.72696152667446));
#129669=CARTESIAN_POINT('Ctrl Pts',(16.9687632474545,14.3996950927668,4.74206075417177));
#129670=CARTESIAN_POINT('Ctrl Pts',(16.9677912330976,14.3878195447154,4.7516197411115));
#129671=CARTESIAN_POINT('Ctrl Pts',(16.9616381637684,14.3133669924242,4.81450753277526));
#129672=CARTESIAN_POINT('Ctrl Pts',(16.9567892777506,14.2575852392825,4.87535155868957));
#129673=CARTESIAN_POINT('Ctrl Pts',(16.9495429910546,14.1887513448055,4.97287445489697));
#129674=CARTESIAN_POINT('Ctrl Pts',(16.94725878971,14.1690980507912,5.00443256765029));
#129675=CARTESIAN_POINT('Ctrl Pts',(16.9443235885123,14.1471620137522,5.04464519534949));
#129676=CARTESIAN_POINT('Ctrl Pts',(16.9437633048511,14.1431155309344,5.05230632890165));
#129677=CARTESIAN_POINT('Ctrl Pts',(16.9428469831884,14.136735442915,5.06478907783135));
#129678=CARTESIAN_POINT('Ctrl Pts',(16.9424946624713,14.1343378904047,5.06957770599404));
#129679=CARTESIAN_POINT('Ctrl Pts',(16.9417829951092,14.1296090252159,5.07922200078097));
#129680=CARTESIAN_POINT('Ctrl Pts',(16.9414236371304,14.1272782657519,5.08407771788205));
#129681=CARTESIAN_POINT('Ctrl Pts',(16.9404704892153,14.1212425002425,5.09692627131019));
#129682=CARTESIAN_POINT('Ctrl Pts',(16.9398729376423,14.1176060557816,5.10495052449272));
#129683=CARTESIAN_POINT('Ctrl Pts',(16.9366430152249,14.098707023119,5.14821674510514));
#129684=CARTESIAN_POINT('Ctrl Pts',(16.9339231324468,14.0854463455459,5.18429201661173));
#129685=CARTESIAN_POINT('Ctrl Pts',(16.9271907373145,14.0582424424118,5.27456406461322));
#129686=CARTESIAN_POINT('Ctrl Pts',(16.9231709938523,14.046786314049,5.32937400048957));
#129687=CARTESIAN_POINT('Ctrl Pts',(16.9177667114474,14.0375857271319,5.40608111272542));
#129688=CARTESIAN_POINT('Ctrl Pts',(16.9162886353816,14.0357451571529,5.42737289805189));
#129689=CARTESIAN_POINT('Ctrl Pts',(16.9136686245222,14.0337084919509,5.46570695274326));
#129690=CARTESIAN_POINT('Ctrl Pts',(16.9125198714081,14.0332544456984,5.48272613773083));
#129691=CARTESIAN_POINT('Ctrl Pts',(16.9113846553004,14.033250032487,5.49974937361882));
#129692=CARTESIAN_POINT('Ctrl Pts',(16.8550925403141,14.0332500296882,5.49976041276753));
#129693=CARTESIAN_POINT('Ctrl Pts',(16.8569805886081,14.0332573685012,5.47014782776616));
#129694=CARTESIAN_POINT('Ctrl Pts',(16.8588280516786,14.0346252816896,5.44054947718285));
#129695=CARTESIAN_POINT('Ctrl Pts',(16.8637501480891,14.0419916165554,5.36082074904889));
#129696=CARTESIAN_POINT('Ctrl Pts',(16.8667628118452,14.0505586046603,5.3110233457765));
#129697=CARTESIAN_POINT('Ctrl Pts',(16.8723921692601,14.0735129401352,5.22060420950517));
#129698=CARTESIAN_POINT('Ctrl Pts',(16.8749953183793,14.0867991173928,5.17983806412932));
#129699=CARTESIAN_POINT('Ctrl Pts',(16.8783947714423,14.1067118030943,5.13019538297171));
#129700=CARTESIAN_POINT('Ctrl Pts',(16.8790796408903,14.1108446832636,5.1203658889598));
#129701=CARTESIAN_POINT('Ctrl Pts',(16.8801458722479,14.11744523418,5.10536671543337));
#129702=CARTESIAN_POINT('Ctrl Pts',(16.8805209256628,14.1197978251529,5.10014693777188));
#129703=CARTESIAN_POINT('Ctrl Pts',(16.8812228141034,14.1242538791875,5.09049004290508));
#129704=CARTESIAN_POINT('Ctrl Pts',(16.8815489394985,14.1263449934759,5.08604758909313));
#129705=CARTESIAN_POINT('Ctrl Pts',(16.8823356528223,14.1314396533196,5.07543483463591));
#129706=CARTESIAN_POINT('Ctrl Pts',(16.8827980701513,14.1344751799524,5.06928032931161));
#129707=CARTESIAN_POINT('Ctrl Pts',(16.8844711952187,14.1456131576357,5.04729141749724));
#129708=CARTESIAN_POINT('Ctrl Pts',(16.8857007876877,14.1540862865985,5.03164987789483));
#129709=CARTESIAN_POINT('Ctrl Pts',(16.889022006378,14.1778402634125,4.99054907604134));
#129710=CARTESIAN_POINT('Ctrl Pts',(16.8911377941257,14.1938704809174,4.96554523949328));
#129711=CARTESIAN_POINT('Ctrl Pts',(16.8987730088496,14.2555397068338,4.87845514331493));
#129712=CARTESIAN_POINT('Ctrl Pts',(16.9042842671423,14.3074177316254,4.82112367767922));
#129713=CARTESIAN_POINT('Ctrl Pts',(16.9104951272084,14.3764956421193,4.76104265722603));
#129714=CARTESIAN_POINT('Ctrl Pts',(16.9114687486816,14.3876448496,4.75177754202202));
#129715=CARTESIAN_POINT('Ctrl Pts',(16.9130453599745,14.4062191116181,4.73703552244383));
#129716=CARTESIAN_POINT('Ctrl Pts',(16.9136541672156,14.4135213064361,4.73140824278354));
#129717=CARTESIAN_POINT('Ctrl Pts',(16.9148368582036,14.4279566474442,4.72060949418074));
#129718=CARTESIAN_POINT('Ctrl Pts',(16.9154110348513,14.435082178889,4.7154294030732));
#129719=CARTESIAN_POINT('Ctrl Pts',(16.9167796953597,14.4523423689923,4.7032387368818));
#129720=CARTESIAN_POINT('Ctrl Pts',(16.9175705947952,14.462542348759,4.69632302128274));
#129721=CARTESIAN_POINT('Ctrl Pts',(16.9205173765212,14.5013543797885,4.6710774603318));
#129722=CARTESIAN_POINT('Ctrl Pts',(16.92262638522,14.5307952347298,4.65406426684295));
#129723=CARTESIAN_POINT('Ctrl Pts',(16.9288675434884,14.6217415775555,4.60772062321625));
#129724=CARTESIAN_POINT('Ctrl Pts',(16.9328769183196,14.6855020724685,4.58330366859324));
#129725=CARTESIAN_POINT('Ctrl Pts',(16.938600237111,14.775375818592,4.55937759750302));
#129726=CARTESIAN_POINT('Ctrl Pts',(16.940157356991,14.7996931065315,4.55390092408));
#129727=CARTESIAN_POINT('Ctrl Pts',(16.9422644203817,14.8319285034046,4.5479393786893));
#129728=CARTESIAN_POINT('Ctrl Pts',(16.9427744219838,14.8396813554126,4.5466032424631));
#129729=CARTESIAN_POINT('Ctrl Pts',(16.9435891334133,14.851969906475,4.54463953860423));
#129730=CARTESIAN_POINT('Ctrl Pts',(16.9438905229242,14.8564954254587,4.54394929278589));
#129731=CARTESIAN_POINT('Ctrl Pts',(16.9445359851929,14.8661392116224,4.54254840694741));
#129732=CARTESIAN_POINT('Ctrl Pts',(16.9448805494108,14.8712585760792,4.5418466165919));
#129733=CARTESIAN_POINT('Ctrl Pts',(16.9457837526175,14.8846098799488,4.54012527556997));
#129734=CARTESIAN_POINT('Ctrl Pts',(16.9463456845636,14.8928495801515,4.53917059645901));
#129735=CARTESIAN_POINT('Ctrl Pts',(16.9491748155504,14.9340511344386,4.53493339244573));
#129736=CARTESIAN_POINT('Ctrl Pts',(16.9515084332927,14.9671514448371,4.53324079484158));
#129737=CARTESIAN_POINT('Ctrl Pts',(16.9577024681769,15.054138598902,4.53326507157288));
#129738=CARTESIAN_POINT('Ctrl Pts',(16.9615882129949,15.1079153544375,4.53778266070494));
#129739=CARTESIAN_POINT('Ctrl Pts',(16.9680464825794,15.1982324962835,4.55304040153624));
#129740=CARTESIAN_POINT('Ctrl Pts',(16.9706598635109,15.2350324653195,4.56149643402058));
#129741=CARTESIAN_POINT('Ctrl Pts',(16.9740803609126,15.2836457980712,4.57570704711354));
#129742=CARTESIAN_POINT('Ctrl Pts',(16.9749449031465,15.2959701717125,4.5795793972008));
#129743=CARTESIAN_POINT('Ctrl Pts',(16.9763336690487,15.3158185339383,4.58625572938594));
#129744=CARTESIAN_POINT('Ctrl Pts',(16.9768626799689,15.3233913550519,4.58890836003187));
#129745=CARTESIAN_POINT('Ctrl Pts',(16.9779717440913,15.3392884347996,4.59470002315309));
#129746=CARTESIAN_POINT('Ctrl Pts',(16.9785510449438,15.3476041934152,4.59786030825321));
#129747=CARTESIAN_POINT('Ctrl Pts',(16.9799560227229,15.3677919797368,4.60585298370008));
#129748=CARTESIAN_POINT('Ctrl Pts',(16.9807776011295,15.3796139929807,4.61080763171321));
#129749=CARTESIAN_POINT('Ctrl Pts',(16.9840709228368,15.4270052987942,4.63178700740235));
#129750=CARTESIAN_POINT('Ctrl Pts',(16.9864789946547,15.461689886295,4.64972342345273));
#129751=CARTESIAN_POINT('Ctrl Pts',(16.9911994745563,15.5283350591226,4.68947163753116));
#129752=CARTESIAN_POINT('Ctrl Pts',(16.9935085441428,15.56025869538,4.71120065477955));
#129753=CARTESIAN_POINT('Ctrl Pts',(16.9984234901247,15.6247292664395,4.76097601471548));
#129754=CARTESIAN_POINT('Ctrl Pts',(17.0010285414683,15.6568765219826,4.78939773572276));
#129755=CARTESIAN_POINT('Ctrl Pts',(17.0044302026669,15.6945317017549,4.82743400426612));
#129756=CARTESIAN_POINT('Ctrl Pts',(17.0051152062007,15.7019085964831,4.83513640228213));
#129757=CARTESIAN_POINT('Ctrl Pts',(17.0061816031185,15.713047791645,4.84715913427062));
#129758=CARTESIAN_POINT('Ctrl Pts',(17.0065566849855,15.7169018677013,4.85139375793849));
#129759=CARTESIAN_POINT('Ctrl Pts',(17.0072585948304,15.7239905936182,4.85932278607112));
#129760=CARTESIAN_POINT('Ctrl Pts',(17.0075847126636,15.7272350577276,4.8630079759129));
#129761=CARTESIAN_POINT('Ctrl Pts',(17.008371363781,15.734946043608,4.87190211154157));
#129762=CARTESIAN_POINT('Ctrl Pts',(17.0088337256631,15.7393853666401,4.87713410956155));
#129763=CARTESIAN_POINT('Ctrl Pts',(17.0105063972969,15.7551275584549,4.89609263799861));
#129764=CARTESIAN_POINT('Ctrl Pts',(17.0117355789586,15.7661062963535,4.91008239176833));
#129765=CARTESIAN_POINT('Ctrl Pts',(17.0150552848717,15.79435967144,4.9482041347071));
#129766=CARTESIAN_POINT('Ctrl Pts',(17.017169947176,15.8109193513682,4.97284197203264));
#129767=CARTESIAN_POINT('Ctrl Pts',(17.0248063663458,15.8663189015304,5.06406909866737));
#129768=CARTESIAN_POINT('Ctrl Pts',(17.0303200594861,15.8983072586581,5.13449707694267));
#129769=CARTESIAN_POINT('Ctrl Pts',(17.0365327385846,15.9259692603401,5.22179786480939));
#129770=CARTESIAN_POINT('Ctrl Pts',(17.0375060265478,15.9300349488594,5.23570748953081));
#129771=CARTESIAN_POINT('Ctrl Pts',(17.0390822427881,15.9361729904792,5.25860685255865));
#129772=CARTESIAN_POINT('Ctrl Pts',(17.0396909828186,15.9384319932439,5.2675437167275));
#129773=CARTESIAN_POINT('Ctrl Pts',(17.0408736396669,15.9425994079716,5.28508251958931));
#129774=CARTESIAN_POINT('Ctrl Pts',(17.0414478480907,15.9445187181497,5.29368091031825));
#129775=CARTESIAN_POINT('Ctrl Pts',(17.0428167427146,15.948840701846,5.31436920294445));
#129776=CARTESIAN_POINT('Ctrl Pts',(17.0436078412074,15.9511302568103,5.32648133621391));
#129777=CARTESIAN_POINT('Ctrl Pts',(17.0465566649586,15.9588639238478,5.37216415515685));
#129778=CARTESIAN_POINT('Ctrl Pts',(17.0486674264615,15.9627674321898,5.40597210521097));
#129779=CARTESIAN_POINT('Ctrl Pts',(17.054919583033,15.9691224912061,5.50803105509186));
#129780=CARTESIAN_POINT('Ctrl Pts',(17.0589375661397,15.9661395241976,5.57639694824305));
#129781=CARTESIAN_POINT('Ctrl Pts',(17.0646617781144,15.952299510654,5.66835712668768));
#129782=CARTESIAN_POINT('Ctrl Pts',(17.066209142905,15.9476763059727,5.69268598518938));
#129783=CARTESIAN_POINT('Ctrl Pts',(17.0683050445963,15.9403638423426,5.7244617613827));
#129784=CARTESIAN_POINT('Ctrl Pts',(17.068814180564,15.9385094738968,5.73209307664392));
#129785=CARTESIAN_POINT('Ctrl Pts',(17.0696278592342,15.9354279575539,5.74413322881435));
#129786=CARTESIAN_POINT('Ctrl Pts',(17.0699290965608,15.9342620750389,5.74855757929147));
#129787=CARTESIAN_POINT('Ctrl Pts',(17.0705746396514,15.9317118231857,5.75796390667448));
#129788=CARTESIAN_POINT('Ctrl Pts',(17.0709194412268,15.9303188111271,5.76294334937198));
#129789=CARTESIAN_POINT('Ctrl Pts',(17.0718239802219,15.9265828187025,5.77589656159812));
#129790=CARTESIAN_POINT('Ctrl Pts',(17.0723870275845,15.9241768881022,5.78385154717093));
#129791=CARTESIAN_POINT('Ctrl Pts',(17.0752364134043,15.9115875727676,5.82361921480091));
#129792=CARTESIAN_POINT('Ctrl Pts',(17.0775902755841,15.8998635936921,5.8549174300905));
#129793=CARTESIAN_POINT('Ctrl Pts',(17.0839033999428,15.864512540436,5.9362061688339));
#129794=CARTESIAN_POINT('Ctrl Pts',(17.0878888324592,15.8381760337433,5.98489102557268));
#129795=CARTESIAN_POINT('Ctrl Pts',(17.0923404979088,15.8034426860291,6.03772580694495));
#129796=CARTESIAN_POINT('Ctrl Pts',(17.0929001330538,15.798978371731,6.04433699068287));
#129797=CARTESIAN_POINT('Ctrl Pts',(17.0955457325953,15.7774028353802,6.07545071491485));
#129798=CARTESIAN_POINT('Ctrl Pts',(17.0976003791149,15.759242097443,6.09920817909452));
#129799=CARTESIAN_POINT('Ctrl Pts',(17.1004313352177,15.7322004709816,6.13137567991266));
#129800=CARTESIAN_POINT('Ctrl Pts',(17.1012417902442,15.7242184665974,6.14051574064338));
#129801=CARTESIAN_POINT('Ctrl Pts',(17.1026265289631,15.7101689767015,6.15600505699528));
#129802=CARTESIAN_POINT('Ctrl Pts',(17.1032040678017,15.7041833272325,6.1624261924069));
#129803=CARTESIAN_POINT('Ctrl Pts',(17.10438452871,15.6916930222926,6.17546457898329));
#129804=CARTESIAN_POINT('Ctrl Pts',(17.1049869621035,15.685178879644,6.18207151176312));
#129805=CARTESIAN_POINT('Ctrl Pts',(17.106539523719,15.668035486275,6.19896560579679));
#129806=CARTESIAN_POINT('Ctrl Pts',(17.1074833201627,15.6572632483098,6.20910463825069));
#129807=CARTESIAN_POINT('Ctrl Pts',(17.109544581392,15.6330015702537,6.23091208992195));
#129808=CARTESIAN_POINT('Ctrl Pts',(17.1106574651702,15.6194133045659,6.24246258027983));
#129809=CARTESIAN_POINT('Ctrl Pts',(17.1142102854606,15.5746067486109,6.27846287129403));
#129810=CARTESIAN_POINT('Ctrl Pts',(17.1166030389666,15.5422012277256,6.301370983305));
#129811=CARTESIAN_POINT('Ctrl Pts',(17.1226151839751,15.4572745987172,6.3538911921325));
#129812=CARTESIAN_POINT('Ctrl Pts',(17.1262112402832,15.4032300651862,6.38070081854876));
#129813=CARTESIAN_POINT('Ctrl Pts',(17.1306838806059,15.3377283540409,6.40589453769879));
#129814=CARTESIAN_POINT('Ctrl Pts',(17.1313270108584,15.3283500470545,6.40933579206176));
#129815=CARTESIAN_POINT('Ctrl Pts',(17.1323380250233,15.3137051481468,6.41445347857233));
#129816=CARTESIAN_POINT('Ctrl Pts',(17.1327004490219,15.3084743815264,6.41623121359989));
#129817=CARTESIAN_POINT('Ctrl Pts',(17.1333939607351,15.2985085135548,6.41952321471357));
#129818=CARTESIAN_POINT('Ctrl Pts',(17.1337245759304,15.2937765165227,6.42104594287271));
#129819=CARTESIAN_POINT('Ctrl Pts',(17.1345440398682,15.282090371369,6.42470726102692));
#129820=CARTESIAN_POINT('Ctrl Pts',(17.1350351327719,15.2751235088988,6.42680394003697));
#129821=CARTESIAN_POINT('Ctrl Pts',(17.1369613969367,15.2479127128858,6.43465920116543));
#129822=CARTESIAN_POINT('Ctrl Pts',(17.1384233045867,15.2275078076048,6.43983434383364));
#129823=CARTESIAN_POINT('Ctrl Pts',(17.142674254307,15.1684627538008,6.45277407304656));
#129824=CARTESIAN_POINT('Ctrl Pts',(17.1455033208931,15.1294952536638,6.45884768982404));
#129825=CARTESIAN_POINT('Ctrl Pts',(17.1526266015848,15.0304146237354,6.46813965270383));
#129826=CARTESIAN_POINT('Ctrl Pts',(17.1568864661465,14.9701604162608,6.46815859511631));
#129827=CARTESIAN_POINT('Ctrl Pts',(17.162073669323,14.8943261133081,6.46109082360551));
#129828=CARTESIAN_POINT('Ctrl Pts',(17.1631538058722,14.8784034487245,6.45920637590301));
#129829=CARTESIAN_POINT('Ctrl Pts',(17.1648565480208,14.8531043456944,6.45557207273387));
#129830=CARTESIAN_POINT('Ctrl Pts',(17.1654868782415,14.8436947717267,6.45407809215954));
#129831=CARTESIAN_POINT('Ctrl Pts',(17.1666835173301,14.8257534473216,6.45095694212353));
#129832=CARTESIAN_POINT('Ctrl Pts',(17.1672504980261,14.8172185860916,6.4493534271853));
#129833=CARTESIAN_POINT('Ctrl Pts',(17.1685599681171,14.7974363666491,6.44536010222345));
#129834=CARTESIAN_POINT('Ctrl Pts',(17.1692996979501,14.786207598781,6.44288417926362));
#129835=CARTESIAN_POINT('Ctrl Pts',(17.1717818011826,14.7483876693906,6.43383456042668));
#129836=CARTESIAN_POINT('Ctrl Pts',(17.1734952829874,14.7220314533522,6.42633117010752));
#129837=CARTESIAN_POINT('Ctrl Pts',(17.1778861455186,14.6544382398202,6.40394251541647));
#129838=CARTESIAN_POINT('Ctrl Pts',(17.1805187632866,14.6138318129792,6.38735528813823));
#129839=CARTESIAN_POINT('Ctrl Pts',(17.1863435116237,14.5269524741419,6.34476881263823));
#129840=CARTESIAN_POINT('Ctrl Pts',(17.1895279123647,14.4814151126276,6.31760426058058));
#129841=CARTESIAN_POINT('Ctrl Pts',(17.1935559668098,14.4298787200643,6.28081703817897));
#129842=CARTESIAN_POINT('Ctrl Pts',(17.194223835475,14.4215201473601,6.27464479639575));
#129843=CARTESIAN_POINT('Ctrl Pts',(17.1952690618377,14.4087584399973,6.26489940848967));
#129844=CARTESIAN_POINT('Ctrl Pts',(17.1956404890185,14.4042842788252,6.2614200306366));
#129845=CARTESIAN_POINT('Ctrl Pts',(17.1963397375666,14.3959806083238,6.25484461031386));
#129846=CARTESIAN_POINT('Ctrl Pts',(17.1966669155138,14.3921437666636,6.25175834317565));
#129847=CARTESIAN_POINT('Ctrl Pts',(17.1974619511648,14.3829342474817,6.24423382258601));
#129848=CARTESIAN_POINT('Ctrl Pts',(17.1979317448755,14.3775857492722,6.2397665977753));
#129849=CARTESIAN_POINT('Ctrl Pts',(17.1996662916528,14.3581616088595,6.22318321552687));
#129850=CARTESIAN_POINT('Ctrl Pts',(17.2009517063024,14.344388431949,6.21072065884791));
#129851=CARTESIAN_POINT('Ctrl Pts',(17.2044823381726,14.3080082914622,6.17584468015182));
#129852=CARTESIAN_POINT('Ctrl Pts',(17.2067550478549,14.2861356708602,6.15269906940836));
#129853=CARTESIAN_POINT('Ctrl Pts',(17.214233822534,14.21822033755,6.07332586059523));
#129854=CARTESIAN_POINT('Ctrl Pts',(17.219419526279,14.1773577328399,6.01297674458097));
#129855=CARTESIAN_POINT('Ctrl Pts',(17.2253832805294,14.1366301730942,5.93523126106986));
#129856=CARTESIAN_POINT('Ctrl Pts',(17.2263991898725,14.1299352931855,5.92168846039345));
#129857=CARTESIAN_POINT('Ctrl Pts',(17.2280259072467,14.1196182694233,5.89952573834837));
#129858=CARTESIAN_POINT('Ctrl Pts',(17.2286432664246,14.1157991604781,5.89100088589861));
#129859=CARTESIAN_POINT('Ctrl Pts',(17.2298308590498,14.1086432600245,5.87438652095032));
#129860=CARTESIAN_POINT('Ctrl Pts',(17.2304015434043,14.1052915802733,5.86630445928171));
#129861=CARTESIAN_POINT('Ctrl Pts',(17.2317433350006,14.0976221251964,5.84707717181626));
#129862=CARTESIAN_POINT('Ctrl Pts',(17.2325112330752,14.0934003435546,5.83589503574992));
#129863=CARTESIAN_POINT('Ctrl Pts',(17.2352356753645,14.0790436680399,5.79562428986589));
#129864=CARTESIAN_POINT('Ctrl Pts',(17.2371545689029,14.0700923216056,5.76613204447125));
#129865=CARTESIAN_POINT('Ctrl Pts',(17.2439463334806,14.043049831694,5.65883260937626));
#129866=CARTESIAN_POINT('Ctrl Pts',(17.2486080869679,14.033205421626,5.57929423180456));
#129867=CARTESIAN_POINT('Ctrl Pts',(17.2535748249259,14.0332501517357,5.49945835346593));
#129868=CARTESIAN_POINT('Origin',(16.125,15.,5.5));
#129869=CARTESIAN_POINT('',(17.7122358268452,14.0332503676593,5.5008431306014));
#129870=CARTESIAN_POINT('',(17.654370605628,14.0332503772168,5.50085402224954));
#129871=CARTESIAN_POINT('',(16.125,14.03325,5.5));
#129872=CARTESIAN_POINT('Ctrl Pts',(17.7122358268452,14.0332503676593,5.50084313060139));
#129873=CARTESIAN_POINT('Ctrl Pts',(17.7087976196952,14.0332959166321,5.55307045170094));
#129874=CARTESIAN_POINT('Ctrl Pts',(17.7053594125452,14.0375775866098,5.60511395562003));
#129875=CARTESIAN_POINT('Ctrl Pts',(17.7019212053952,14.0459839817697,5.65639373216326));
#129876=CARTESIAN_POINT('Ctrl Pts',(17.7001166244923,14.0503961708862,5.68330848785335));
#129877=CARTESIAN_POINT('Ctrl Pts',(17.6983120435895,14.0559438391561,5.71001327697186));
#129878=CARTESIAN_POINT('Ctrl Pts',(17.6965074626866,14.0626057458369,5.7364266794632));
#129879=CARTESIAN_POINT('Ctrl Pts',(17.6938358502455,14.0724684417909,5.77553070333594));
#129880=CARTESIAN_POINT('Ctrl Pts',(17.6911642378045,14.0848048701166,5.81410643268523));
#129881=CARTESIAN_POINT('Ctrl Pts',(17.6884926253634,14.0995398785608,5.85181974389983));
#129882=CARTESIAN_POINT('Ctrl Pts',(17.6858250159401,14.1142528087655,5.88947654727291));
#129883=CARTESIAN_POINT('Ctrl Pts',(17.6831574065167,14.1313570047041,5.92627294634419));
#129884=CARTESIAN_POINT('Ctrl Pts',(17.6804897970933,14.1507273254122,5.961889041544));
#129885=CARTESIAN_POINT('Ctrl Pts',(17.6778248925357,14.1700780052703,5.99746902322807));
#129886=CARTESIAN_POINT('Ctrl Pts',(17.6751599879781,14.1916899873374,6.03187055612003));
#129887=CARTESIAN_POINT('Ctrl Pts',(17.6724950834204,14.2153909552819,6.06479572364407));
#129888=CARTESIAN_POINT('Ctrl Pts',(17.6698315903055,14.2390793702223,6.09770345264968));
#129889=CARTESIAN_POINT('Ctrl Pts',(17.6671680971905,14.264854239059,6.1291358905146));
#129890=CARTESIAN_POINT('Ctrl Pts',(17.6645046040756,14.2925001081522,6.15882430551352));
#129891=CARTESIAN_POINT('Ctrl Pts',(17.6618391798863,14.3201660209349,6.18853424507983));
#129892=CARTESIAN_POINT('Ctrl Pts',(17.659173755697,14.3497052514647,6.21649720022547));
#129893=CARTESIAN_POINT('Ctrl Pts',(17.6565083315077,14.3808637634722,6.24247955063976));
#129894=CARTESIAN_POINT('Ctrl Pts',(17.6538420766206,14.4120319862438,6.26846999863179));
#129895=CARTESIAN_POINT('Ctrl Pts',(17.6511758217336,14.4448200291885,6.2924782572714));
#129896=CARTESIAN_POINT('Ctrl Pts',(17.6485095668466,14.4789420220101,6.31431206921736));
#129897=CARTESIAN_POINT('Ctrl Pts',(17.645837912486,14.5131331158004,6.3361900971493));
#129898=CARTESIAN_POINT('Ctrl Pts',(17.6431662581255,14.5486630462699,6.3558845898121));
#129899=CARTESIAN_POINT('Ctrl Pts',(17.640494603765,14.5852199411891,6.37324857017508));
#129900=CARTESIAN_POINT('Ctrl Pts',(17.6381867010175,14.6167995345197,6.38824840644879));
#129901=CARTESIAN_POINT('Ctrl Pts',(17.6358787982699,14.6491448829356,6.40150982190342));
#129902=CARTESIAN_POINT('Ctrl Pts',(17.6335708955224,14.6820450946975,6.41296782018541));
#129903=CARTESIAN_POINT('Ctrl Pts',(17.6308993644067,14.7201289955596,6.42623111690236));
#129904=CARTESIAN_POINT('Ctrl Pts',(17.6282278332909,14.7591318060258,6.43713787356378));
#129905=CARTESIAN_POINT('Ctrl Pts',(17.6255563021752,14.7987331433189,6.44556713928822));
#129906=CARTESIAN_POINT('Ctrl Pts',(17.6228887738615,14.8382751452319,6.45398377529558));
#129907=CARTESIAN_POINT('Ctrl Pts',(17.6202212455479,14.8784133342073,6.45993013643737));
#129908=CARTESIAN_POINT('Ctrl Pts',(17.6175537172342,14.9188117202061,6.46333484610706));
#129909=CARTESIAN_POINT('Ctrl Pts',(17.6148888933841,14.9591691484524,6.46673610392459));
#129910=CARTESIAN_POINT('Ctrl Pts',(17.6122240695341,14.9997856714742,6.4676007574624));
#129911=CARTESIAN_POINT('Ctrl Pts',(17.609559245684,15.040317720132,6.46590892114286));
#129912=CARTESIAN_POINT('Ctrl Pts',(17.606895832688,15.0808283096587,6.46421798054259));
#129913=CARTESIAN_POINT('Ctrl Pts',(17.6042324196919,15.1212539297447,6.45997325441683));
#129914=CARTESIAN_POINT('Ctrl Pts',(17.6015690066959,15.1612516684648,6.4532069355168));
#129915=CARTESIAN_POINT('Ctrl Pts',(17.5989036609282,15.2012784325346,6.44643570646987));
#129916=CARTESIAN_POINT('Ctrl Pts',(17.5962383151606,15.2408761153243,6.43713931740122));
#129917=CARTESIAN_POINT('Ctrl Pts',(17.593572969393,15.2797099169859,6.42540149386077));
#129918=CARTESIAN_POINT('Ctrl Pts',(17.5909067921151,15.3185558336613,6.41366000846162));
#129919=CARTESIAN_POINT('Ctrl Pts',(17.5882406148373,15.3566368413702,6.39947576590505));
#129920=CARTESIAN_POINT('Ctrl Pts',(17.5855744375595,15.393635185694,6.38298182488861));
#129921=CARTESIAN_POINT('Ctrl Pts',(17.5829028583062,15.4307084928317,6.3664544652895));
#129922=CARTESIAN_POINT('Ctrl Pts',(17.5802312790529,15.4666942304483,6.34760832401572));
#129923=CARTESIAN_POINT('Ctrl Pts',(17.5775596997995,15.5012981683483,6.32662307547673));
#129924=CARTESIAN_POINT('Ctrl Pts',(17.5752512426524,15.5311987253555,6.30849015019922));
#129925=CARTESIAN_POINT('Ctrl Pts',(17.5729427855053,15.5600678254938,6.28876097242699));
#129926=CARTESIAN_POINT('Ctrl Pts',(17.5706343283582,15.5877350985541,6.26757606556457));
#129927=CARTESIAN_POINT('Ctrl Pts',(17.5679629006329,15.619752639113,6.24306014694741));
#129928=CARTESIAN_POINT('Ctrl Pts',(17.5652914729076,15.65030732673,6.21648107266194));
#129929=CARTESIAN_POINT('Ctrl Pts',(17.5626200451824,15.6791219749082,6.1880399012389));
#129930=CARTESIAN_POINT('Ctrl Pts',(17.5599526226303,15.7078934223451,6.15964137061709));
#129931=CARTESIAN_POINT('Ctrl Pts',(17.5572852000783,15.734929573689,6.12938666818248));
#129932=CARTESIAN_POINT('Ctrl Pts',(17.5546177775262,15.7599860639873,6.09751715041915));
#129933=CARTESIAN_POINT('Ctrl Pts',(17.5519530615594,15.78501712992,6.06567997007675));
#129934=CARTESIAN_POINT('Ctrl Pts',(17.5492883455926,15.8080721472486,6.03223167286745));
#129935=CARTESIAN_POINT('Ctrl Pts',(17.5466236296258,15.8289455889551,5.99744826168351));
#129936=CARTESIAN_POINT('Ctrl Pts',(17.5439603263891,15.8498079643637,5.96268329132948));
#129937=CARTESIAN_POINT('Ctrl Pts',(17.5412970231525,15.8684907536195,5.92658510943038));
#129938=CARTESIAN_POINT('Ctrl Pts',(17.5386337199158,15.8848322879557,5.88945780861491));
#129939=CARTESIAN_POINT('Ctrl Pts',(17.5359684857979,15.9011856698206,5.85230359069643));
#129940=CARTESIAN_POINT('Ctrl Pts',(17.5333032516801,15.9151941608265,5.81411929606249));
#129941=CARTESIAN_POINT('Ctrl Pts',(17.5306380175622,15.9267435947425,5.77523057988494));
#129942=CARTESIAN_POINT('Ctrl Pts',(17.5279719531495,15.9382966266297,5.73632974878616));
#129943=CARTESIAN_POINT('Ctrl Pts',(17.5253058887367,15.9473889337335,5.69672462802192));
#129944=CARTESIAN_POINT('Ctrl Pts',(17.522639824324,15.9539569277647,5.65675376381363));
#129945=CARTESIAN_POINT('Ctrl Pts',(17.5199683583395,15.9605382288602,5.61670191675729));
#129946=CARTESIAN_POINT('Ctrl Pts',(17.5172968923551,15.9645849334581,5.57628342960348));
#129947=CARTESIAN_POINT('Ctrl Pts',(17.5146254263706,15.966085324279,5.53584283349242));
#129948=CARTESIAN_POINT('Ctrl Pts',(17.5123162046451,15.9673822657713,5.5008858833844));
#129949=CARTESIAN_POINT('Ctrl Pts',(17.5100069829195,15.9667774868603,5.4659126948984));
#129950=CARTESIAN_POINT('Ctrl Pts',(17.507697761194,15.9642947089741,5.43114307046806));
#129951=CARTESIAN_POINT('Ctrl Pts',(17.5050262537061,15.9614224167033,5.39091856063004));
#129952=CARTESIAN_POINT('Ctrl Pts',(17.5023547462182,15.956022332195,5.35078154256967));
#129953=CARTESIAN_POINT('Ctrl Pts',(17.4996832387303,15.9481099992535,5.31107411025631));
#129954=CARTESIAN_POINT('Ctrl Pts',(17.4970157351346,15.9402095248333,5.27142618901659));
#129955=CARTESIAN_POINT('Ctrl Pts',(17.4943482315389,15.9298043571631,5.23220714982284));
#129956=CARTESIAN_POINT('Ctrl Pts',(17.4916807279432,15.9169617461634,5.19375382684363));
#129957=CARTESIAN_POINT('Ctrl Pts',(17.4890159298416,15.9041321606786,5.15533950483774));
#129958=CARTESIAN_POINT('Ctrl Pts',(17.4863511317399,15.8888702055026,5.11768991576088));
#129959=CARTESIAN_POINT('Ctrl Pts',(17.4836863336383,15.8712934238896,5.08112850182088));
#129960=CARTESIAN_POINT('Ctrl Pts',(17.4810229473632,15.8537259545644,5.04458645834481));
#129961=CARTESIAN_POINT('Ctrl Pts',(17.4783595610881,15.8338463402288,5.00913197494729));
#129962=CARTESIAN_POINT('Ctrl Pts',(17.475696174813,15.811819701173,4.97506730404046));
#129963=CARTESIAN_POINT('Ctrl Pts',(17.4730308570369,15.7897770882886,4.94097792926422));
#129964=CARTESIAN_POINT('Ctrl Pts',(17.4703655392608,15.7655846503951,4.90828087799683));
#129965=CARTESIAN_POINT('Ctrl Pts',(17.4677002214847,15.7394516367196,4.87725058052796));
#129966=CARTESIAN_POINT('Ctrl Pts',(17.4650340729418,15.7133104775087,4.84621061106385));
#129967=CARTESIAN_POINT('Ctrl Pts',(17.4623679243989,15.6852279349662,4.81683886146808));
#129968=CARTESIAN_POINT('Ctrl Pts',(17.459701775856,15.6554518354536,4.78937460367608));
#129969=CARTESIAN_POINT('Ctrl Pts',(17.4570302261723,15.6256154148804,4.76185470820196));
#129970=CARTESIAN_POINT('Ctrl Pts',(17.4543586764885,15.5940790345019,4.73625040050669));
#129971=CARTESIAN_POINT('Ctrl Pts',(17.4516871268047,15.561124040503,4.7127609170845));
#129972=CARTESIAN_POINT('Ctrl Pts',(17.4493784825464,15.5326456789959,4.69246226369885));
#129973=CARTESIAN_POINT('Ctrl Pts',(17.4470698382881,15.5031086477845,4.67374233222166));
#129974=CARTESIAN_POINT('Ctrl Pts',(17.4447611940298,15.4727094250297,4.65670209179192));
#129975=CARTESIAN_POINT('Ctrl Pts',(17.4420897043288,15.4375324114138,4.63698366759239));
#129976=CARTESIAN_POINT('Ctrl Pts',(17.4394182146278,15.4010385654625,4.61942467951124));
#129977=CARTESIAN_POINT('Ctrl Pts',(17.4367467249268,15.3635221663353,4.60420024721878));
#129978=CARTESIAN_POINT('Ctrl Pts',(17.4340792392166,15.3260619962548,4.58899863308942));
#129979=CARTESIAN_POINT('Ctrl Pts',(17.4314117535064,15.2875828395704,4.57612487716833));
#129980=CARTESIAN_POINT('Ctrl Pts',(17.4287442677963,15.2484030134787,4.56570801919597));
#129981=CARTESIAN_POINT('Ctrl Pts',(17.4260794876373,15.2092629263167,4.55530172673215));
#129982=CARTESIAN_POINT('Ctrl Pts',(17.4234147074784,15.1694241382623,4.54734755368335));
#129983=CARTESIAN_POINT('Ctrl Pts',(17.4207499273195,15.1292214351756,4.54192516827173));
#129984=CARTESIAN_POINT('Ctrl Pts',(17.4180865590031,15.0890400321146,4.53650565572536));
#129985=CARTESIAN_POINT('Ctrl Pts',(17.4154231906867,15.0484956747044,4.53361535292633));
#129986=CARTESIAN_POINT('Ctrl Pts',(17.4127598223703,15.0079316105748,4.53328253762866));
#129987=CARTESIAN_POINT('Ctrl Pts',(17.4100945224049,14.9673381267315,4.53294948095155));
#129988=CARTESIAN_POINT('Ctrl Pts',(17.4074292224396,14.9267254937623,4.53517763170673));
#129989=CARTESIAN_POINT('Ctrl Pts',(17.4047639224742,14.8864379853199,4.5399431103722));
#129990=CARTESIAN_POINT('Ctrl Pts',(17.4020977916883,14.8461379185584,4.54471007452049));
#129991=CARTESIAN_POINT('Ctrl Pts',(17.3994316609024,14.8061637568535,4.55201584731124));
#129992=CARTESIAN_POINT('Ctrl Pts',(17.3967655301166,14.7668516193589,4.56178499526791));
#129993=CARTESIAN_POINT('Ctrl Pts',(17.3940939978403,14.7274598368098,4.57157393518635));
#129994=CARTESIAN_POINT('Ctrl Pts',(17.3914224655641,14.6887333202173,4.58383605050688));
#129995=CARTESIAN_POINT('Ctrl Pts',(17.3887509332878,14.6509931797788,4.59844589627739));
#129996=CARTESIAN_POINT('Ctrl Pts',(17.3864421644805,14.6183777179312,4.6110718924128));
#129997=CARTESIAN_POINT('Ctrl Pts',(17.3841333956731,14.5864988586795,4.62545041278623));
#129998=CARTESIAN_POINT('Ctrl Pts',(17.3818246268657,14.5555490039028,4.64147284575955));
#129999=CARTESIAN_POINT('Ctrl Pts',(17.3791531481338,14.5197368955058,4.66001241922649));
#130000=CARTESIAN_POINT('Ctrl Pts',(17.3764816694018,14.4850043907671,4.68083925012965));
#130001=CARTESIAN_POINT('Ctrl Pts',(17.3738101906699,14.4516595701061,4.70380383356625));
#130002=CARTESIAN_POINT('Ctrl Pts',(17.3711427162105,14.4183647299116,4.72673399544748));
#130003=CARTESIAN_POINT('Ctrl Pts',(17.3684752417512,14.3864539404335,4.75179524771507));
#130004=CARTESIAN_POINT('Ctrl Pts',(17.3658077672919,14.3562100113391,4.77879266989304));
#130005=CARTESIAN_POINT('Ctrl Pts',(17.363142998639,14.3259967607829,4.80576270669245));
#130006=CARTESIAN_POINT('Ctrl Pts',(17.3604782299861,14.2974474614101,4.83466464131405));
#130007=CARTESIAN_POINT('Ctrl Pts',(17.3578134613331,14.2708127406299,4.86526265016752));
#130008=CARTESIAN_POINT('Ctrl Pts',(17.3551501047518,14.2441921336945,4.89584444501406));
#130009=CARTESIAN_POINT('Ctrl Pts',(17.3524867481704,14.219484480074,4.92812009391392));
#130010=CARTESIAN_POINT('Ctrl Pts',(17.349823391589,14.1969021358283,4.96181844786091));
#130011=CARTESIAN_POINT('Ctrl Pts',(17.3471581036054,14.174303415409,4.99554123904472));
#130012=CARTESIAN_POINT('Ctrl Pts',(17.3444928156218,14.1538334176651,5.03068831470276));
#130013=CARTESIAN_POINT('Ctrl Pts',(17.3418275276382,14.135661498133,5.06695898959753));
#130014=CARTESIAN_POINT('Ctrl Pts',(17.3391614089887,14.1174839151253,5.10324096864127));
#130015=CARTESIAN_POINT('Ctrl Pts',(17.3364952903393,14.1016060760367,5.14064670903404));
#130016=CARTESIAN_POINT('Ctrl Pts',(17.3338291716898,14.0881497917777,5.17885398918091));
#130017=CARTESIAN_POINT('Ctrl Pts',(17.3311576516337,14.0746662458428,5.21713867513091));
#130018=CARTESIAN_POINT('Ctrl Pts',(17.3284861315776,14.0636142227846,5.25622758181451));
#130019=CARTESIAN_POINT('Ctrl Pts',(17.3258146115215,14.0550655082373,5.29578352471683));
#130020=CARTESIAN_POINT('Ctrl Pts',(17.3235057609149,14.0476773156149,5.32996959139418));
#130021=CARTESIAN_POINT('Ctrl Pts',(17.3211969103082,14.0421580952794,5.36450406953048));
#130022=CARTESIAN_POINT('Ctrl Pts',(17.3188880597015,14.0385229231138,5.39916650793299));
#130023=CARTESIAN_POINT('Ctrl Pts',(17.3166706787643,14.0350317654615,5.43245572549052));
#130024=CARTESIAN_POINT('Ctrl Pts',(17.314453297827,14.0332691004685,5.46592930822326));
#130025=CARTESIAN_POINT('Ctrl Pts',(17.3122359168897,14.0332501543841,5.49945364696662));
#130026=CARTESIAN_POINT('Ctrl Pts',(17.2535748450812,14.0332501519173,5.49945802948715));
#130027=CARTESIAN_POINT('Ctrl Pts',(17.2543247186306,14.0332569092666,5.48740448371654));
#130028=CARTESIAN_POINT('Ctrl Pts',(17.2550815808894,14.033489093376,5.47535260252305));
#130029=CARTESIAN_POINT('Ctrl Pts',(17.2563749225964,14.0342612417695,5.45502252247803));
#130030=CARTESIAN_POINT('Ctrl Pts',(17.2569064296428,14.0346825426573,5.4467410188117));
#130031=CARTESIAN_POINT('Ctrl Pts',(17.2577766650328,14.0355383683539,5.4333224954904));
#130032=CARTESIAN_POINT('Ctrl Pts',(17.2581122261669,14.0359075574332,5.42818156267272));
#130033=CARTESIAN_POINT('Ctrl Pts',(17.2587475267943,14.0366793379702,5.41851693893325));
#130034=CARTESIAN_POINT('Ctrl Pts',(17.2590467783054,14.0370727373995,5.4139926012123));
#130035=CARTESIAN_POINT('Ctrl Pts',(17.2596966591357,14.0379907536201,5.40423224631418));
#130036=CARTESIAN_POINT('Ctrl Pts',(17.2600478721077,14.0385262668562,5.39899747504598));
#130037=CARTESIAN_POINT('Ctrl Pts',(17.2609882981898,14.0400649873054,5.38507942314247));
#130038=CARTESIAN_POINT('Ctrl Pts',(17.2615812900937,14.0411432500638,5.37640514692402));
#130039=CARTESIAN_POINT('Ctrl Pts',(17.2650899701888,14.0481586513915,5.32560569562272));
#130040=CARTESIAN_POINT('Ctrl Pts',(17.2681139638864,14.0567530995382,5.28389840008284));
#130041=CARTESIAN_POINT('Ctrl Pts',(17.2728344407192,14.0743035346338,5.22028233959132));
#130042=CARTESIAN_POINT('Ctrl Pts',(17.2745170884469,14.0813636659866,5.19790197784353));
#130043=CARTESIAN_POINT('Ctrl Pts',(17.2801887364239,14.1079999099434,5.12307314134545));
#130044=CARTESIAN_POINT('Ctrl Pts',(17.2841245219664,14.1313146654974,5.07206824675988));
#130045=CARTESIAN_POINT('Ctrl Pts',(17.288848539852,14.165713509303,5.01136755965406));
#130046=CARTESIAN_POINT('Ctrl Pts',(17.2897731553977,14.1727663841989,4.99952004229735));
#130047=CARTESIAN_POINT('Ctrl Pts',(17.2912917530246,14.1848801836336,4.9801272614319));
#130048=CARTESIAN_POINT('Ctrl Pts',(17.2918907397198,14.1897981504352,4.97249554343377));
#130049=CARTESIAN_POINT('Ctrl Pts',(17.2930625396891,14.1996926542071,4.95760611543204));
#130050=CARTESIAN_POINT('Ctrl Pts',(17.2936355339779,14.2046622110789,4.95034485027512));
#130051=CARTESIAN_POINT('Ctrl Pts',(17.2948991109822,14.2159089136869,4.93438370532776));
#130052=CARTESIAN_POINT('Ctrl Pts',(17.2955878557477,14.222233179841,4.92571835106705));
#130053=CARTESIAN_POINT('Ctrl Pts',(17.2980893158884,14.2458956577073,4.89440469950239));
#130054=CARTESIAN_POINT('Ctrl Pts',(17.2998695798597,14.2640902908091,4.87242040683532));
#130055=CARTESIAN_POINT('Ctrl Pts',(17.306033034434,14.3313142839145,4.79814587828379));
#130056=CARTESIAN_POINT('Ctrl Pts',(17.3102464203683,14.3851508415495,4.75053374347122));
#130057=CARTESIAN_POINT('Ctrl Pts',(17.3163390737033,14.4664145230372,4.69336508121755));
#130058=CARTESIAN_POINT('Ctrl Pts',(17.3180646058462,14.4897503101519,4.67840501264147));
#130059=CARTESIAN_POINT('Ctrl Pts',(17.3203539007209,14.5205407997681,4.66048394963582));
#130060=CARTESIAN_POINT('Ctrl Pts',(17.3208673639943,14.5274361509142,4.65658330445516));
#130061=CARTESIAN_POINT('Ctrl Pts',(17.3217191201378,14.5388396574904,4.65031616741772));
#130062=CARTESIAN_POINT('Ctrl Pts',(17.3220544277231,14.543320138849,4.64789966581242));
#130063=CARTESIAN_POINT('Ctrl Pts',(17.322699950325,14.5519240376989,4.64334659261929));
#130064=CARTESIAN_POINT('Ctrl Pts',(17.3230097547151,14.5560441410294,4.64120414448304));
#130065=CARTESIAN_POINT('Ctrl Pts',(17.3238729909078,14.5675035250802,4.63534977886605));
#130066=CARTESIAN_POINT('Ctrl Pts',(17.3244300347971,14.5748747948989,4.63170180539624));
#130067=CARTESIAN_POINT('Ctrl Pts',(17.3269903693181,14.6086881961767,4.61550162918485));
#130068=CARTESIAN_POINT('Ctrl Pts',(17.3290450071617,14.6356434328545,4.60406123260561));
#130069=CARTESIAN_POINT('Ctrl Pts',(17.3356706448702,14.7230975461629,4.57154341720252));
#130070=CARTESIAN_POINT('Ctrl Pts',(17.3403033159443,14.7851969536707,4.55524219321351));
#130071=CARTESIAN_POINT('Ctrl Pts',(17.3471188038722,14.8811975021898,4.54000481284117));
#130072=CARTESIAN_POINT('Ctrl Pts',(17.3494039966905,14.9141906918192,4.53649495359746));
#130073=CARTESIAN_POINT('Ctrl Pts',(17.3524628050184,14.9595146006904,4.53402066352866));
#130074=CARTESIAN_POINT('Ctrl Pts',(17.3532799664084,14.9717388478542,4.53358576358348));
#130075=CARTESIAN_POINT('Ctrl Pts',(17.3546724677809,14.992760900117,4.53323711037753));
#130076=CARTESIAN_POINT('Ctrl Pts',(17.3552511607009,15.0015550704157,4.53321125389845));
#130077=CARTESIAN_POINT('Ctrl Pts',(17.3564308241142,15.0195943127416,4.5334043668191));
#130078=CARTESIAN_POINT('Ctrl Pts',(17.3570313468656,15.0288383612637,4.53363598280809));
#130079=CARTESIAN_POINT('Ctrl Pts',(17.3585721514065,15.052701092411,4.53457660767245));
#130080=CARTESIAN_POINT('Ctrl Pts',(17.3595062896233,15.0673098426854,4.53548501714557));
#130081=CARTESIAN_POINT('Ctrl Pts',(17.365240279008,15.1576935768077,4.54316900210194));
#130082=CARTESIAN_POINT('Ctrl Pts',(17.3697588957289,15.2324679043734,4.55853704378782));
#130083=CARTESIAN_POINT('Ctrl Pts',(17.3761754626059,15.3332796845443,4.59201382937322));
#130084=CARTESIAN_POINT('Ctrl Pts',(17.3780084369784,15.3614260895656,4.60284606015946));
#130085=CARTESIAN_POINT('Ctrl Pts',(17.3810078208716,15.4054584835517,4.62220078124195));
#130086=CARTESIAN_POINT('Ctrl Pts',(17.3821436838015,15.4216926694521,4.62988319636871));
#130087=CARTESIAN_POINT('Ctrl Pts',(17.3837481257597,15.4438421035046,4.64113029723895));
#130088=CARTESIAN_POINT('Ctrl Pts',(17.3841963320234,15.4499481767441,4.64431336880373));
#130089=CARTESIAN_POINT('Ctrl Pts',(17.3849710463743,15.4603517326595,4.64987884160691));
#130090=CARTESIAN_POINT('Ctrl Pts',(17.3852956344526,15.4646659447153,4.65222924066097));
#130091=CARTESIAN_POINT('Ctrl Pts',(17.3860021857633,15.4739575250388,4.65738356375072));
#130092=CARTESIAN_POINT('Ctrl Pts',(17.386384782454,15.478928012001,4.66019874404365));
#130093=CARTESIAN_POINT('Ctrl Pts',(17.387484479889,15.4930501913619,4.66836339641623));
#130094=CARTESIAN_POINT('Ctrl Pts',(17.3882075669692,15.502138950625,4.67381939996979));
#130095=CARTESIAN_POINT('Ctrl Pts',(17.3918081718366,15.5465199913123,4.70146427338571));
#130096=CARTESIAN_POINT('Ctrl Pts',(17.3947789304895,15.58043867426,4.72576892131138));
#130097=CARTESIAN_POINT('Ctrl Pts',(17.4013641814037,15.6516085659239,4.78407786977893));
#130098=CARTESIAN_POINT('Ctrl Pts',(17.4049723311714,15.6879904429575,4.81896540390468));
#130099=CARTESIAN_POINT('Ctrl Pts',(17.4106325598203,15.7418935243969,4.8794042834374));
#130100=CARTESIAN_POINT('Ctrl Pts',(17.4127396245306,15.7611970837907,4.90323842277798));
#130101=CARTESIAN_POINT('Ctrl Pts',(17.4156066956423,15.7863979188752,4.93757110732959));
#130102=CARTESIAN_POINT('Ctrl Pts',(17.4164032909988,15.7932801822665,4.94732059932046));
#130103=CARTESIAN_POINT('Ctrl Pts',(17.4177720556238,15.8048911089773,4.9644326763853));
#130104=CARTESIAN_POINT('Ctrl Pts',(17.4183472795598,15.8097034617819,4.97173645991493));
#130105=CARTESIAN_POINT('Ctrl Pts',(17.4195297898079,15.8194526393979,4.98697923258663));
#130106=CARTESIAN_POINT('Ctrl Pts',(17.4201364989245,15.8243747739359,4.99492656173603));
#130107=CARTESIAN_POINT('Ctrl Pts',(17.4217152577608,15.8369645600532,5.01592865626018));
#130108=CARTESIAN_POINT('Ctrl Pts',(17.4226805492907,15.8444423507405,5.02909459981354));
#130109=CARTESIAN_POINT('Ctrl Pts',(17.4282058164764,15.8858677349724,5.10619383633156));
#130110=CARTESIAN_POINT('Ctrl Pts',(17.432517540193,15.912858330038,5.17360203602639));
#130111=CARTESIAN_POINT('Ctrl Pts',(17.4388135335007,15.9405570262538,5.27421311593733));
#130112=CARTESIAN_POINT('Ctrl Pts',(17.4407524753761,15.9475070326552,5.30543019800855));
#130113=CARTESIAN_POINT('Ctrl Pts',(17.443902198176,15.9560387204902,5.35528562815933));
#130114=CARTESIAN_POINT('Ctrl Pts',(17.4450785629847,15.9586484157231,5.37372490594616));
#130115=CARTESIAN_POINT('Ctrl Pts',(17.4467307551215,15.9615015170068,5.39915830271393));
#130116=CARTESIAN_POINT('Ctrl Pts',(17.447184582137,15.9622040380042,5.40609793651254));
#130117=CARTESIAN_POINT('Ctrl Pts',(17.4479656952311,15.9632743754465,5.4179494274931));
#130118=CARTESIAN_POINT('Ctrl Pts',(17.4482909708854,15.9636798529462,5.42285754211342));
#130119=CARTESIAN_POINT('Ctrl Pts',(17.4489949317035,15.9644710497425,5.4334173962096));
#130120=CARTESIAN_POINT('Ctrl Pts',(17.449374196241,15.9648446082729,5.43906949119331));
#130121=CARTESIAN_POINT('Ctrl Pts',(17.4504550506527,15.9657616477409,5.45508192825005));
#130122=CARTESIAN_POINT('Ctrl Pts',(17.4511623302768,15.9661880372743,5.46544787575962));
#130123=CARTESIAN_POINT('Ctrl Pts',(17.4555514392557,15.9677834103671,5.52920830409514));
#130124=CARTESIAN_POINT('Ctrl Pts',(17.4593888343635,15.9646927261921,5.58261315710402));
#130125=CARTESIAN_POINT('Ctrl Pts',(17.4663269727654,15.9511106693,5.67857121028968));
#130126=CARTESIAN_POINT('Ctrl Pts',(17.4694258533113,15.9421095332945,5.72119994474269));
#130127=CARTESIAN_POINT('Ctrl Pts',(17.474351203117,15.9228414270807,5.78933302169659));
#130128=CARTESIAN_POINT('Ctrl Pts',(17.4762196120331,15.9143085705217,5.81526175722135));
#130129=CARTESIAN_POINT('Ctrl Pts',(17.4788253529677,15.9006418498044,5.85154182627666));
#130130=CARTESIAN_POINT('Ctrl Pts',(17.479590859813,15.8964030207263,5.86221408137099));
#130131=CARTESIAN_POINT('Ctrl Pts',(17.480924177662,15.8886270661105,5.88081868121039));
#130132=CARTESIAN_POINT('Ctrl Pts',(17.4814946012313,15.885171388768,5.88878342462708));
#130133=CARTESIAN_POINT('Ctrl Pts',(17.4826839592794,15.8776967484638,5.90539470777142));
#130134=CARTESIAN_POINT('Ctrl Pts',(17.4833020952871,15.8736562043767,5.91403055250293));
#130135=CARTESIAN_POINT('Ctrl Pts',(17.4849506705226,15.8624655915626,5.93705464785389));
#130136=CARTESIAN_POINT('Ctrl Pts',(17.4859731639266,15.8550833538701,5.95132711630148));
#130137=CARTESIAN_POINT('Ctrl Pts',(17.4902776954715,15.8221811756167,6.01123049800135));
#130138=CARTESIAN_POINT('Ctrl Pts',(17.493445343203,15.7933377245919,6.05493651589568));
#130139=CARTESIAN_POINT('Ctrl Pts',(17.4993161377708,15.7332430423628,6.13166533256069));
#130140=CARTESIAN_POINT('Ctrl Pts',(17.5020184159081,15.7029301948823,6.16523314486186));
#130141=CARTESIAN_POINT('Ctrl Pts',(17.5062097999904,15.6540619704933,6.21226516050319));
#130142=CARTESIAN_POINT('Ctrl Pts',(17.5076312694427,15.6371944093681,6.22739386612571));
#130143=CARTESIAN_POINT('Ctrl Pts',(17.5095698968696,15.6140924768739,6.24669374511524));
#130144=CARTESIAN_POINT('Ctrl Pts',(17.5100538705391,15.6083174555036,6.25140600494245));
#130145=CARTESIAN_POINT('Ctrl Pts',(17.5108701863821,15.5985772398406,6.25916787747479));
#130146=CARTESIAN_POINT('Ctrl Pts',(17.5112000395516,15.5946416795074,6.26225445238271));
#130147=CARTESIAN_POINT('Ctrl Pts',(17.5118941843601,15.5863645099912,6.26864294309396));
#130148=CARTESIAN_POINT('Ctrl Pts',(17.5122588203172,15.582018663705,6.27193884739973));
#130149=CARTESIAN_POINT('Ctrl Pts',(17.5132750763057,15.5699062613803,6.28096450903728));
#130150=CARTESIAN_POINT('Ctrl Pts',(17.5139315421207,15.5620816558534,6.28661483981535));
#130151=CARTESIAN_POINT('Ctrl Pts',(17.5189325533948,15.5023774749667,6.32838299748462));
#130152=CARTESIAN_POINT('Ctrl Pts',(17.523501858163,15.4471553896278,6.35944899401651));
#130153=CARTESIAN_POINT('Ctrl Pts',(17.5315640670774,15.3438536024578,6.40489528995907));
#130154=CARTESIAN_POINT('Ctrl Pts',(17.5350680773101,15.2969285134284,6.42136062366709));
#130155=CARTESIAN_POINT('Ctrl Pts',(17.5396775990968,15.2317886964276,6.43871968290166));
#130156=CARTESIAN_POINT('Ctrl Pts',(17.540877289752,15.2145132795484,6.4428174611121));
#130157=CARTESIAN_POINT('Ctrl Pts',(17.5427208828995,15.1874734168911,6.44844960478174));
#130158=CARTESIAN_POINT('Ctrl Pts',(17.5433748886528,15.1777824787674,6.45031380985332));
#130159=CARTESIAN_POINT('Ctrl Pts',(17.5445913458023,15.1595784924271,6.45352741008591));
#130160=CARTESIAN_POINT('Ctrl Pts',(17.5451548372646,15.1510727303776,6.45491196195982));
#130161=CARTESIAN_POINT('Ctrl Pts',(17.5464223225942,15.1317819692474,6.45778786196739));
#130162=CARTESIAN_POINT('Ctrl Pts',(17.5471241504801,15.1209879019671,6.45921114403649));
#130163=CARTESIAN_POINT('Ctrl Pts',(17.549317642329,15.0869263807489,6.4631182810499));
#130164=CARTESIAN_POINT('Ctrl Pts',(17.5507891959852,15.0635906654162,6.46494008961774));
#130165=CARTESIAN_POINT('Ctrl Pts',(17.5571157939137,14.9617290484488,6.46918052216765));
#130166=CARTESIAN_POINT('Ctrl Pts',(17.5617210334738,14.883147257417,6.46287090851723));
#130167=CARTESIAN_POINT('Ctrl Pts',(17.5682810597497,14.7782206204251,6.44140048680865));
#130168=CARTESIAN_POINT('Ctrl Pts',(17.5700571487987,14.7505148751223,6.43443985104588));
#130169=CARTESIAN_POINT('Ctrl Pts',(17.5724043745192,14.7155065406645,6.42397665060791));
#130170=CARTESIAN_POINT('Ctrl Pts',(17.5729220113832,14.7078814923477,6.42159435046795));
#130171=CARTESIAN_POINT('Ctrl Pts',(17.5737788423868,14.6954345783482,6.41753556752393));
#130172=CARTESIAN_POINT('Ctrl Pts',(17.5741149794583,14.6905947169296,6.41591483373247));
#130173=CARTESIAN_POINT('Ctrl Pts',(17.5748038979303,14.6807686339591,6.41253758476846));
#130174=CARTESIAN_POINT('Ctrl Pts',(17.5751568066441,14.6757835911033,6.4107783625274));
#130175=CARTESIAN_POINT('Ctrl Pts',(17.5761066583923,14.6624886528917,6.40596359918072));
#130176=CARTESIAN_POINT('Ctrl Pts',(17.5767075064352,14.6542060932035,6.40283470970285));
#130177=CARTESIAN_POINT('Ctrl Pts',(17.5806300311369,14.6008800162927,6.38184839362959));
#130178=CARTESIAN_POINT('Ctrl Pts',(17.5840914117939,14.5571940102271,6.36074114409454));
#130179=CARTESIAN_POINT('Ctrl Pts',(17.5910606773516,14.4729855407954,6.31194254903599));
#130180=CARTESIAN_POINT('Ctrl Pts',(17.5945580840589,14.4326087417535,6.28425943123633));
#130181=CARTESIAN_POINT('Ctrl Pts',(17.5999988500447,14.3717973896715,6.23540119820824));
#130182=CARTESIAN_POINT('Ctrl Pts',(17.6019971815238,14.3499317188028,6.21614590805787));
#130183=CARTESIAN_POINT('Ctrl Pts',(17.6047458632091,14.3205190879945,6.18778555181103));
#130184=CARTESIAN_POINT('Ctrl Pts',(17.6055288379672,14.3122200995737,6.17948664738948));
#130185=CARTESIAN_POINT('Ctrl Pts',(17.6068820224609,14.2980234200164,6.16476343726271));
#130186=CARTESIAN_POINT('Ctrl Pts',(17.6074550915398,14.2920578707101,6.15840678628417));
#130187=CARTESIAN_POINT('Ctrl Pts',(17.6086402517664,14.279823319005,6.14501157071517));
#130188=CARTESIAN_POINT('Ctrl Pts',(17.6092516726875,14.2735696094926,6.13796024649898));
#130189=CARTESIAN_POINT('Ctrl Pts',(17.6108591205679,14.2572933458136,6.11905834358368));
#130190=CARTESIAN_POINT('Ctrl Pts',(17.6118479114037,14.2474511012525,6.10705568425469));
#130191=CARTESIAN_POINT('Ctrl Pts',(17.617900139376,14.1884068283506,6.03140676819867));
#130192=CARTESIAN_POINT('Ctrl Pts',(17.6226489626738,14.14702138127,5.96206570421902));
#130193=CARTESIAN_POINT('Ctrl Pts',(17.6291128673259,14.1041879164194,5.86443256604884));
#130194=CARTESIAN_POINT('Ctrl Pts',(17.6307133812222,14.0946523389052,5.84005268703975));
#130195=CARTESIAN_POINT('Ctrl Pts',(17.6333773049893,14.0807674273744,5.79981019181811));
#130196=CARTESIAN_POINT('Ctrl Pts',(17.6344179423211,14.0758127903135,5.78417002629577));
#130197=CARTESIAN_POINT('Ctrl Pts',(17.6359095793583,14.0694085299031,5.76201047148965));
#130198=CARTESIAN_POINT('Ctrl Pts',(17.636343790383,14.0676246171125,5.75558973129185));
#130199=CARTESIAN_POINT('Ctrl Pts',(17.6371028621737,14.0646476253452,5.74442869572332));
#130200=CARTESIAN_POINT('Ctrl Pts',(17.6374260274492,14.0634238817683,5.73969694483293));
#130201=CARTESIAN_POINT('Ctrl Pts',(17.6381403118093,14.0608151650847,5.7292849480221));
#130202=CARTESIAN_POINT('Ctrl Pts',(17.6385322127395,14.0594458173628,5.72360135686545));
#130203=CARTESIAN_POINT('Ctrl Pts',(17.6397095731124,14.0555130697071,5.70660252963761));
#130204=CARTESIAN_POINT('Ctrl Pts',(17.6405025074394,14.0531018178137,5.69525360683657));
#130205=CARTESIAN_POINT('Ctrl Pts',(17.6455439360664,14.0392124345504,5.62355697933958));
#130206=CARTESIAN_POINT('Ctrl Pts',(17.6499852011548,14.0333046373484,5.56227671970015));
#130207=CARTESIAN_POINT('Ctrl Pts',(17.6543706060827,14.033250377214,5.50085401588055));
#130208=CARTESIAN_POINT('Origin',(16.125,15.,5.5));
#130209=CARTESIAN_POINT('',(18.1122363826056,14.0332503335345,5.49919695023161));
#130210=CARTESIAN_POINT('',(18.0542644868187,14.0332501467026,5.49946741256401));
#130211=CARTESIAN_POINT('',(16.125,14.03325,5.5));
#130212=CARTESIAN_POINT('Ctrl Pts',(18.1116014980396,14.0336172045748,5.49916088635316));
#130213=CARTESIAN_POINT('Ctrl Pts',(18.1088658687755,14.0336893782224,5.53997545647357));
#130214=CARTESIAN_POINT('Ctrl Pts',(18.1061935292842,14.0363249574671,5.58078098174216));
#130215=CARTESIAN_POINT('Ctrl Pts',(18.1035215018489,14.0413803580352,5.6212698696751));
#130216=CARTESIAN_POINT('Ctrl Pts',(18.1008461429723,14.0464420615965,5.66180923851073));
#130217=CARTESIAN_POINT('Ctrl Pts',(18.0982503860392,14.0540669973466,5.70201867661375));
#130218=CARTESIAN_POINT('Ctrl Pts',(18.0957117391143,14.0641887759179,5.74155657413911));
#130219=CARTESIAN_POINT('Ctrl Pts',(18.0931714984445,14.0743169088717,5.78111929328233));
#130220=CARTESIAN_POINT('Ctrl Pts',(18.0906756150031,14.0869242328612,5.82001513743482));
#130221=CARTESIAN_POINT('Ctrl Pts',(18.0881817228849,14.1019116579752,5.85791351849397));
#130222=CARTESIAN_POINT('Ctrl Pts',(18.0856819955985,14.1169341504223,5.89590057356776));
#130223=CARTESIAN_POINT('Ctrl Pts',(18.0831837022177,14.1343484255732,5.93288515096058));
#130224=CARTESIAN_POINT('Ctrl Pts',(18.0806279241079,14.1540096713151,5.96854122302932));
#130225=CARTESIAN_POINT('Ctrl Pts',(18.0787455098085,14.1684908228622,5.99480308812046));
#130226=CARTESIAN_POINT('Ctrl Pts',(18.0768314636631,14.184190028169,6.02034430119852));
#130227=CARTESIAN_POINT('Ctrl Pts',(18.0748600895335,14.2010311060696,6.04503941695895));
#130228=CARTESIAN_POINT('Ctrl Pts',(18.0748590319094,14.2010401411531,6.04505266566168));
#130229=CARTESIAN_POINT('Ctrl Pts',(18.0748579742688,14.2010491765653,6.04506591412149));
#130230=CARTESIAN_POINT('Ctrl Pts',(18.0748569166117,14.2010582123061,6.04507916233835));
#130231=CARTESIAN_POINT('Ctrl Pts',(18.0724065240528,14.2219923238445,6.07577278846326));
#130232=CARTESIAN_POINT('Ctrl Pts',(18.0698604177907,14.244781920386,6.1052840748042));
#130233=CARTESIAN_POINT('Ctrl Pts',(18.0672739372776,14.2692511598286,6.13340288117519));
#130234=CARTESIAN_POINT('Ctrl Pts',(18.0670480255632,14.271388383675,6.1358588701997));
#130235=CARTESIAN_POINT('Ctrl Pts',(18.0668218058398,14.2735383898142,6.13830422664061));
#130236=CARTESIAN_POINT('Ctrl Pts',(18.0665953149815,14.2757010429266,6.14073880552423));
#130237=CARTESIAN_POINT('Ctrl Pts',(18.0637799385348,14.3025837289705,6.17100164305548));
#130238=CARTESIAN_POINT('Ctrl Pts',(18.0609233217478,14.3314258555293,6.1996013612969));
#130239=CARTESIAN_POINT('Ctrl Pts',(18.0580817228216,14.361975897788,6.22630679014228));
#130240=CARTESIAN_POINT('Ctrl Pts',(18.0552430158035,14.39249484913,6.25298504075157));
#130241=CARTESIAN_POINT('Ctrl Pts',(18.0524196050428,14.4247180905576,6.27777315290609));
#130242=CARTESIAN_POINT('Ctrl Pts',(18.0496459487321,14.4583756431876,6.30047312464432));
#130243=CARTESIAN_POINT('Ctrl Pts',(18.046873781404,14.4920151274242,6.32316091035027));
#130244=CARTESIAN_POINT('Ctrl Pts',(18.0441514015046,14.5270873595618,6.34376286150736));
#130245=CARTESIAN_POINT('Ctrl Pts',(18.041488724339,14.5633047650662,6.36211106595343));
#130246=CARTESIAN_POINT('Ctrl Pts',(18.0388241827983,14.5995475295694,6.38047211759518));
#130247=CARTESIAN_POINT('Ctrl Pts',(18.0362193552178,14.6369370964161,6.39657613249006));
#130248=CARTESIAN_POINT('Ctrl Pts',(18.0336595581491,14.6751671758804,6.41028521668761));
#130249=CARTESIAN_POINT('Ctrl Pts',(18.0310989935289,14.7134087185792,6.4239984115344));
#130250=CARTESIAN_POINT('Ctrl Pts',(18.0285832355814,14.7524913169899,6.4353149186364));
#130251=CARTESIAN_POINT('Ctrl Pts',(18.026075344813,14.792089783369,6.44413046985751));
#130252=CARTESIAN_POINT('Ctrl Pts',(18.0235624718859,14.8317669157916,6.4529635339926));
#130253=CARTESIAN_POINT('Ctrl Pts',(18.0210570003867,14.8719619543096,6.45928512125692));
#130254=CARTESIAN_POINT('Ctrl Pts',(18.0185049586738,14.9123287521555,6.46303089420097));
#130255=CARTESIAN_POINT('Ctrl Pts',(18.0163245790278,14.9468168030184,6.4662311581483));
#130256=CARTESIAN_POINT('Ctrl Pts',(18.0141096076922,14.9814297928223,6.46755158034023));
#130257=CARTESIAN_POINT('Ctrl Pts',(18.0118220857894,15.0159418679715,6.46698121831073));
#130258=CARTESIAN_POINT('Ctrl Pts',(18.0118211641835,15.0159557723331,6.46698098852101));
#130259=CARTESIAN_POINT('Ctrl Pts',(18.0118202425658,15.0159696766789,6.46698075842474));
#130260=CARTESIAN_POINT('Ctrl Pts',(18.0118193209363,15.0159835810087,6.46698052802191));
#130261=CARTESIAN_POINT('Ctrl Pts',(18.0093419444725,15.0533589702906,6.46636119609794));
#130262=CARTESIAN_POINT('Ctrl Pts',(18.0067725382995,15.0907651161667,6.46351754675653));
#130263=CARTESIAN_POINT('Ctrl Pts',(18.0041666197859,15.1279257633553,6.45848168359273));
#130264=CARTESIAN_POINT('Ctrl Pts',(18.0039548448629,15.1309456940077,6.45807243459736));
#130265=CARTESIAN_POINT('Ctrl Pts',(18.0037428288012,15.1339639811941,6.45764872549634));
#130266=CARTESIAN_POINT('Ctrl Pts',(18.0035306013974,15.1369804652223,6.45721058335147));
#130267=CARTESIAN_POINT('Ctrl Pts',(18.0007110077786,15.1770566239422,6.45138954999749));
#130268=CARTESIAN_POINT('Ctrl Pts',(17.9978547419002,15.2168191808931,6.44301782903751));
#130269=CARTESIAN_POINT('Ctrl Pts',(17.9950167387749,15.2559371188899,6.43217817789313));
#130270=CARTESIAN_POINT('Ctrl Pts',(17.9921815149166,15.2950167485457,6.4213491420591));
#130271=CARTESIAN_POINT('Ctrl Pts',(17.9893648137686,15.33345317573,6.40805728346844));
#130272=CARTESIAN_POINT('Ctrl Pts',(17.986599669708,15.3709325477281,6.39241895397032));
#130273=CARTESIAN_POINT('Ctrl Pts',(17.98383590699,15.4083931967048,6.37678843668359));
#130274=CARTESIAN_POINT('Ctrl Pts',(17.9811237283587,15.4448977780505,6.35881384072439));
#130275=CARTESIAN_POINT('Ctrl Pts',(17.978471672925,15.4801476626227,6.3386428554526));
#130276=CARTESIAN_POINT('Ctrl Pts',(17.9758176195666,15.5154241026782,6.31845667437889));
#130277=CARTESIAN_POINT('Ctrl Pts',(17.9732237007733,15.5494438505318,6.29607069449121));
#130278=CARTESIAN_POINT('Ctrl Pts',(17.9706740015162,15.581922932576,6.27166493845294));
#130279=CARTESIAN_POINT('Ctrl Pts',(17.9681234609455,15.6144127316072,6.2472511293493));
#130280=CARTESIAN_POINT('Ctrl Pts',(17.9656169089056,15.6453605939784,6.22081599670884));
#130281=CARTESIAN_POINT('Ctrl Pts',(17.9631164361356,15.6745002420025,6.19257410705889));
#130282=CARTESIAN_POINT('Ctrl Pts',(17.9606108920038,15.7036989899298,6.16427493830445));
#130283=CARTESIAN_POINT('Ctrl Pts',(17.9581109411544,15.7310816816463,6.13416136866688));
#130284=CARTESIAN_POINT('Ctrl Pts',(17.9555620680015,15.7564040080915,6.10248778276124));
#130285=CARTESIAN_POINT('Ctrl Pts',(17.9533945604248,15.7779375765114,6.07555323823291));
#130286=CARTESIAN_POINT('Ctrl Pts',(17.9511910843983,15.7979812735429,6.0474911579514));
#130287=CARTESIAN_POINT('Ctrl Pts',(17.9489142448659,15.8164036574049,6.01848213947661));
#130288=CARTESIAN_POINT('Ctrl Pts',(17.9489132820208,15.8164114479853,6.0184698719496));
#130289=CARTESIAN_POINT('Ctrl Pts',(17.9489123191626,15.8164192382764,6.01845760425303));
#130290=CARTESIAN_POINT('Ctrl Pts',(17.9489113562913,15.8164270282781,6.01844533638694));
#130291=CARTESIAN_POINT('Ctrl Pts',(17.9464450745537,15.8363802024246,5.98702263882757));
#130292=CARTESIAN_POINT('Ctrl Pts',(17.9438855878723,15.8545098229505,5.95435673608956));
#130293=CARTESIAN_POINT('Ctrl Pts',(17.9412885873555,15.870690772421,5.92069341892059));
#130294=CARTESIAN_POINT('Ctrl Pts',(17.9410745755695,15.8720242006868,5.91791931603396));
#130295=CARTESIAN_POINT('Ctrl Pts',(17.9408603090284,15.8733443984736,5.91513846888866));
#130296=CARTESIAN_POINT('Ctrl Pts',(17.9406458188985,15.8746512977548,5.91235103064029));
#130297=CARTESIAN_POINT('Ctrl Pts',(17.9378328046746,15.891791136628,5.87579408770548));
#130298=CARTESIAN_POINT('Ctrl Pts',(17.9349819647332,15.9066436051444,5.83809783774839));
#130299=CARTESIAN_POINT('Ctrl Pts',(17.9321487179927,15.9190952188582,5.79958219943527));
#130300=CARTESIAN_POINT('Ctrl Pts',(17.9293183943032,15.9315339862841,5.76110629757619));
#130301=CARTESIAN_POINT('Ctrl Pts',(17.9265059236572,15.9415771629589,5.72181272334531));
#130302=CARTESIAN_POINT('Ctrl Pts',(17.9237448700913,15.9491487441809,5.68202569232012));
#130303=CARTESIAN_POINT('Ctrl Pts',(17.920985318238,15.9567162072869,5.64226030110872));
#130304=CARTESIAN_POINT('Ctrl Pts',(17.9182772075239,15.9618148199288,5.60200199529049));
#130305=CARTESIAN_POINT('Ctrl Pts',(17.9156296451895,15.9644031220143,5.56157960489602));
#130306=CARTESIAN_POINT('Ctrl Pts',(17.9129801843571,15.966993280104,5.52112822865665));
#130307=CARTESIAN_POINT('Ctrl Pts',(17.9103912828771,15.9670693890494,5.4805125711672));
#130308=CARTESIAN_POINT('Ctrl Pts',(17.9078476039144,15.9646250281175,5.44006701231661));
#130309=CARTESIAN_POINT('Ctrl Pts',(17.9053031489214,15.9621799214554,5.39960911425793));
#130310=CARTESIAN_POINT('Ctrl Pts',(17.9028036904404,15.9572124955404,5.35932151722426));
#130311=CARTESIAN_POINT('Ctrl Pts',(17.9003118363484,15.949754806761,5.31954275906698));
#130312=CARTESIAN_POINT('Ctrl Pts',(17.8978149108835,15.9422819402388,5.27968304395688));
#130313=CARTESIAN_POINT('Ctrl Pts',(17.8953251213505,15.932308143317,5.24033448709196));
#130314=CARTESIAN_POINT('Ctrl Pts',(17.8927882747748,15.9199105622351,5.20183911645171));
#130315=CARTESIAN_POINT('Ctrl Pts',(17.8905719613089,15.9090794279603,5.16820767451102));
#130316=CARTESIAN_POINT('Ctrl Pts',(17.8883191088923,15.8963987108305,5.13522773161351));
#130317=CARTESIAN_POINT('Ctrl Pts',(17.8859891485143,15.8819531603237,5.10312470204307));
#130318=CARTESIAN_POINT('Ctrl Pts',(17.8859881712975,15.881947101665,5.10311123759953));
#130319=CARTESIAN_POINT('Ctrl Pts',(17.8859871940672,15.881941042696,5.10309777330959));
#130320=CARTESIAN_POINT('Ctrl Pts',(17.8859862168232,15.8819349834168,5.10308430917325));
#130321=CARTESIAN_POINT('Ctrl Pts',(17.8835206934754,15.8666478131493,5.06911516255648));
#130322=CARTESIAN_POINT('Ctrl Pts',(17.8809616614798,15.8493173518981,5.0359889359937));
#130323=CARTESIAN_POINT('Ctrl Pts',(17.8783646711916,15.8300807044715,5.00394517438977));
#130324=CARTESIAN_POINT('Ctrl Pts',(17.8781482371223,15.8284775156175,5.00127463620797));
#130325=CARTESIAN_POINT('Ctrl Pts',(17.8779315394092,15.8268611136928,4.99861163024406));
#130326=CARTESIAN_POINT('Ctrl Pts',(17.8777146102079,15.8252315927147,4.99595630226268));
#130327=CARTESIAN_POINT('Ctrl Pts',(17.8748989717401,15.8040811808644,4.96149140051695));
#130328=CARTESIAN_POINT('Ctrl Pts',(17.872044972252,15.7807158849934,4.92831692112204));
#130329=CARTESIAN_POINT('Ctrl Pts',(17.8692081040133,15.7553417304167,4.89670397818174));
#130330=CARTESIAN_POINT('Ctrl Pts',(17.8663741108469,15.7299932917073,4.86512307391465));
#130331=CARTESIAN_POINT('Ctrl Pts',(17.8635575134749,15.7026402592037,4.83510028959648));
#130332=CARTESIAN_POINT('Ctrl Pts',(17.8607919502432,15.6735127620098,4.80687764311701));
#130333=CARTESIAN_POINT('Ctrl Pts',(17.8580278519906,15.6444006942861,4.7786699467885));
#130334=CARTESIAN_POINT('Ctrl Pts',(17.8553148149984,15.6135160758515,4.75226043225306));
#130335=CARTESIAN_POINT('Ctrl Pts',(17.8526619882167,15.5811117946709,4.72786472603724));
#130336=CARTESIAN_POINT('Ctrl Pts',(17.8500072446075,15.54868409944,4.7034513924503));
#130337=CARTESIAN_POINT('Ctrl Pts',(17.8474127222728,15.5147344984511,4.68105491162952));
#130338=CARTESIAN_POINT('Ctrl Pts',(17.8448630843471,15.4795397257855,4.66086466929473));
#130339=CARTESIAN_POINT('Ctrl Pts',(17.8423126543957,15.4443340201285,4.64066815501296));
#130340=CARTESIAN_POINT('Ctrl Pts',(17.8398068819401,15.4078822766436,4.62267956406072));
#130341=CARTESIAN_POINT('Ctrl Pts',(17.8373083419198,15.3704858537613,4.60705842571141));
#130342=CARTESIAN_POINT('Ctrl Pts',(17.8348047545454,15.3330138855656,4.59140573076653));
#130343=CARTESIAN_POINT('Ctrl Pts',(17.8323079267811,15.294593333726,4.57813063592173));
#130344=CARTESIAN_POINT('Ctrl Pts',(17.8297636306789,15.2555532947734,4.56735689974287));
#130345=CARTESIAN_POINT('Ctrl Pts',(17.8275707465065,15.2219053701346,4.55807120554918));
#130346=CARTESIAN_POINT('Ctrl Pts',(17.8253419942227,15.1877977496348,4.55064338818002));
#130347=CARTESIAN_POINT('Ctrl Pts',(17.8230384246179,15.1534565324485,4.54512473143032));
#130348=CARTESIAN_POINT('Ctrl Pts',(17.8230374665369,15.1534422495422,4.54512243615765));
#130349=CARTESIAN_POINT('Ctrl Pts',(17.8230365084429,15.1534279665951,4.54512014121477));
#130350=CARTESIAN_POINT('Ctrl Pts',(17.823035550336,15.1534136836072,4.54511784660166));
#130351=CARTESIAN_POINT('Ctrl Pts',(17.8205667211352,15.116609588965,4.53920513712671));
#130352=CARTESIAN_POINT('Ctrl Pts',(17.8180048593831,15.0793856105227,4.53546526148694));
#130353=CARTESIAN_POINT('Ctrl Pts',(17.815405549373,15.0420177039287,4.53391545663618));
#130354=CARTESIAN_POINT('Ctrl Pts',(17.8151910551426,15.0389341162328,4.53378756723577));
#130355=CARTESIAN_POINT('Ctrl Pts',(17.8149763059084,15.0358495741346,4.53367457686729));
#130356=CARTESIAN_POINT('Ctrl Pts',(17.8147613329042,15.0327642462848,4.53357648715621));
#130357=CARTESIAN_POINT('Ctrl Pts',(17.8119454617059,14.9923504005498,4.53229163749196));
#130358=CARTESIAN_POINT('Ctrl Pts',(17.8090918310268,14.9517965738512,4.53356564647681));
#130359=CARTESIAN_POINT('Ctrl Pts',(17.8062557657168,14.9114423675895,4.53737558507123));
#130360=CARTESIAN_POINT('Ctrl Pts',(17.803422565318,14.8711289259787,4.54118167497597));
#130361=CARTESIAN_POINT('Ctrl Pts',(17.8006071922017,14.8310145990644,4.54751827374003));
#130362=CARTESIAN_POINT('Ctrl Pts',(17.7978431046286,14.7914279990699,4.55632633642105));
#130363=CARTESIAN_POINT('Ctrl Pts',(17.7950804715473,14.7518622299594,4.56512976420715));
#130364=CARTESIAN_POINT('Ctrl Pts',(17.7923691501625,14.7128236115966,4.57640200068218));
#130365=CARTESIAN_POINT('Ctrl Pts',(17.7897181174785,14.6746312654799,4.5900504708212));
#130366=CARTESIAN_POINT('Ctrl Pts',(17.7870651525617,14.6364110824744,4.60370888878966));
#130367=CARTESIAN_POINT('Ctrl Pts',(17.7844724874549,14.5990384927188,4.61974711801268));
#130368=CARTESIAN_POINT('Ctrl Pts',(17.7819246340463,14.5628238351016,4.6380382139017));
#130369=CARTESIAN_POINT('Ctrl Pts',(17.7793759806,14.5265978059157,4.65633505327878));
#130370=CARTESIAN_POINT('Ctrl Pts',(17.7768719111538,14.491530648528,4.67688642475008));
#130371=CARTESIAN_POINT('Ctrl Pts',(17.7743748836567,14.4579213097127,4.6995283670398));
#130372=CARTESIAN_POINT('Ctrl Pts',(17.7718727953186,14.4242438532984,4.72221619879956));
#130373=CARTESIAN_POINT('Ctrl Pts',(17.7693772739804,14.3920305644859,4.74700346924696));
#130374=CARTESIAN_POINT('Ctrl Pts',(17.7668340263732,14.3615657555603,4.77368333767468));
#130375=CARTESIAN_POINT('Ctrl Pts',(17.764640735305,14.3352929722413,4.79669199674406));
#130376=CARTESIAN_POINT('Ctrl Pts',(17.7624113416266,14.3103206576772,4.82110770405281));
#130377=CARTESIAN_POINT('Ctrl Pts',(17.7601068293578,14.2868162319021,4.84676948192799));
#130378=CARTESIAN_POINT('Ctrl Pts',(17.76010586425,14.2868063884718,4.84678022883692));
#130379=CARTESIAN_POINT('Ctrl Pts',(17.7601048991289,14.2867965452982,4.84679097596449));
#130380=CARTESIAN_POINT('Ctrl Pts',(17.7601039339947,14.2867867023815,4.84680172331068));
#130381=CARTESIAN_POINT('Ctrl Pts',(17.7576574878544,14.2618366328468,4.87404436308077));
#130382=CARTESIAN_POINT('Ctrl Pts',(17.7551188439162,14.2384353630941,4.90281317730129));
#130383=CARTESIAN_POINT('Ctrl Pts',(17.7525424071133,14.2167495663272,4.93289180029561));
#130384=CARTESIAN_POINT('Ctrl Pts',(17.7523372409479,14.2150226884312,4.93528701361191));
#130385=CARTESIAN_POINT('Ctrl Pts',(17.7521318351298,14.2133066900175,4.93769050538471));
#130386=CARTESIAN_POINT('Ctrl Pts',(17.7519262171315,14.2116016555307,4.94010215220752));
#130387=CARTESIAN_POINT('Ctrl Pts',(17.7491428756289,14.1885215103621,4.97274733281705));
#130388=CARTESIAN_POINT('Ctrl Pts',(17.7463212722676,14.1674496164549,5.00689228645096));
#130389=CARTESIAN_POINT('Ctrl Pts',(17.7435155809644,14.1485526504879,5.04224773268058));
#130390=CARTESIAN_POINT('Ctrl Pts',(17.740712090522,14.1296705078165,5.07757544513362));
#130391=CARTESIAN_POINT('Ctrl Pts',(17.7379247838215,14.1129596062418,5.11411163420977));
#130392=CARTESIAN_POINT('Ctrl Pts',(17.7351870199387,14.0985500750757,5.15155536242206));
#130393=CARTESIAN_POINT('Ctrl Pts',(17.7324507313258,14.0841483086208,5.18897891372959));
#130394=CARTESIAN_POINT('Ctrl Pts',(17.7297640154077,14.0720453839529,5.22730897157081));
#130395=CARTESIAN_POINT('Ctrl Pts',(17.7271367399864,14.0623374688623,5.26623394088526));
#130396=CARTESIAN_POINT('Ctrl Pts',(17.7245073209853,14.0526216331362,5.30519066887156));
#130397=CARTESIAN_POINT('Ctrl Pts',(17.7219373687409,14.0453048495426,5.34474322479761));
#130398=CARTESIAN_POINT('Ctrl Pts',(17.7194132115611,14.0404490318487,5.38456887519119));
#130399=CARTESIAN_POINT('Ctrl Pts',(17.716966696999,14.0357425782276,5.423169495792));
#130400=CARTESIAN_POINT('Ctrl Pts',(17.7145628866741,14.0333481032163,5.46202654932006));
#130401=CARTESIAN_POINT('Ctrl Pts',(17.7121702600549,14.0332882759794,5.5008377736384));
#130402=CARTESIAN_POINT('Ctrl Pts',(17.6543706060827,14.033250377214,5.50085401588055));
#130403=CARTESIAN_POINT('Ctrl Pts',(17.6580115786231,14.0332053278599,5.44985795470837));
#130404=CARTESIAN_POINT('Ctrl Pts',(17.6616032851967,14.0371953487123,5.39893238786557));
#130405=CARTESIAN_POINT('Ctrl Pts',(17.6661790796772,14.0477171410936,5.33259644850869));
#130406=CARTESIAN_POINT('Ctrl Pts',(17.6672679536018,14.0506478613156,5.31670471445997));
#130407=CARTESIAN_POINT('Ctrl Pts',(17.6689809790593,14.0559428155606,5.29154659700883));
#130408=CARTESIAN_POINT('Ctrl Pts',(17.669613021814,14.0580484002325,5.28222951675262));
#130409=CARTESIAN_POINT('Ctrl Pts',(17.6708108916401,14.0623293641528,5.26451198174632));
#130410=CARTESIAN_POINT('Ctrl Pts',(17.6713774194988,14.0644804217476,5.25610667322801));
#130411=CARTESIAN_POINT('Ctrl Pts',(17.6726829194021,14.0697299905992,5.23668615780269));
#130412=CARTESIAN_POINT('Ctrl Pts',(17.6734191856156,14.0729115258471,5.2256946070088));
#130413=CARTESIAN_POINT('Ctrl Pts',(17.6758736512411,14.0842552382558,5.18895925274585));
#130414=CARTESIAN_POINT('Ctrl Pts',(17.6775638706208,14.0933009978729,5.16350048160501));
#130415=CARTESIAN_POINT('Ctrl Pts',(17.6818686155903,14.119393435123,5.09879415316991));
#130416=CARTESIAN_POINT('Ctrl Pts',(17.6844408186437,14.1379994756611,5.06023935469139));
#130417=CARTESIAN_POINT('Ctrl Pts',(17.690296652061,14.1859945388744,4.97562147997777));
#130418=CARTESIAN_POINT('Ctrl Pts',(17.6935702910173,14.2168514121737,4.93056640225068));
#130419=CARTESIAN_POINT('Ctrl Pts',(17.697698802244,14.2579118665586,4.88030748678154));
#130420=CARTESIAN_POINT('Ctrl Pts',(17.6983669334397,14.2646173592589,4.87236478751426));
#130421=CARTESIAN_POINT('Ctrl Pts',(17.6994124619425,14.2751752687108,4.86026036363062));
#130422=CARTESIAN_POINT('Ctrl Pts',(17.6997839218796,14.2789386394842,4.85602158116335));
#130423=CARTESIAN_POINT('Ctrl Pts',(17.7004831499036,14.2860400500654,4.84816336917266));
#130424=CARTESIAN_POINT('Ctrl Pts',(17.70081027332,14.2893687961256,4.84453597262604));
#130425=CARTESIAN_POINT('Ctrl Pts',(17.7016050430806,14.297473697085,4.83583821566285));
#130426=CARTESIAN_POINT('Ctrl Pts',(17.7020746228493,14.3022771489473,4.83079382977349));
#130427=CARTESIAN_POINT('Ctrl Pts',(17.7038074811637,14.3200713914113,4.81250689341262));
#130428=CARTESIAN_POINT('Ctrl Pts',(17.7050913746803,14.333387349295,4.79958786553665));
#130429=CARTESIAN_POINT('Ctrl Pts',(17.7086161400394,14.3704922149092,4.76560594466785));
#130430=CARTESIAN_POINT('Ctrl Pts',(17.7108844139193,14.3949609245833,4.7453198049455));
#130431=CARTESIAN_POINT('Ctrl Pts',(17.7183690740793,14.4786318883733,4.68263961848548));
#130432=CARTESIAN_POINT('Ctrl Pts',(17.7235653945706,14.5416333941749,4.64571302630296));
#130433=CARTESIAN_POINT('Ctrl Pts',(17.729537574548,14.6219856202463,4.61009080760766));
#130434=CARTESIAN_POINT('Ctrl Pts',(17.7305524166336,14.6359217801681,4.60429897020812));
#130435=CARTESIAN_POINT('Ctrl Pts',(17.7321778766288,14.6586924988455,4.59545484336193));
#130436=CARTESIAN_POINT('Ctrl Pts',(17.7327950267675,14.6674452645428,4.59220040267388));
#130437=CARTESIAN_POINT('Ctrl Pts',(17.7339824999806,14.6844890955603,4.58614279051585));
#130438=CARTESIAN_POINT('Ctrl Pts',(17.7345532700782,14.6927737388548,4.58332439605747));
#130439=CARTESIAN_POINT('Ctrl Pts',(17.7358957042201,14.7124696402621,4.57692097069132));
#130440=CARTESIAN_POINT('Ctrl Pts',(17.7366641504585,14.7239115617762,4.5734344079247));
#130441=CARTESIAN_POINT('Ctrl Pts',(17.7393935801319,14.7651088767559,4.56171177196163));
#130442=CARTESIAN_POINT('Ctrl Pts',(17.7413167216283,14.7951915373875,4.55468925577576));
#130443=CARTESIAN_POINT('Ctrl Pts',(17.7463446052182,14.8757702247164,4.53990712662917));
#130444=CARTESIAN_POINT('Ctrl Pts',(17.7493892273225,14.9266299750044,4.53468742770296));
#130445=CARTESIAN_POINT('Ctrl Pts',(17.7549337463581,15.0183906809525,4.53256689340583));
#130446=CARTESIAN_POINT('Ctrl Pts',(17.7574155375176,15.0591311931225,4.53420092219245));
#130447=CARTESIAN_POINT('Ctrl Pts',(17.7606764942316,15.1101487158995,4.5394874352612));
#130448=CARTESIAN_POINT('Ctrl Pts',(17.7613551030031,15.120635806784,4.54074815227532));
#130449=CARTESIAN_POINT('Ctrl Pts',(17.7624136300875,15.1367517353785,4.54295398741473));
#130450=CARTESIAN_POINT('Ctrl Pts',(17.7627873817123,15.1423967156238,4.54377759973275));
#130451=CARTESIAN_POINT('Ctrl Pts',(17.7634884725191,15.1528934855495,4.54540410270926));
#130452=CARTESIAN_POINT('Ctrl Pts',(17.7638151279656,15.1577469403971,4.54619412687196));
#130453=CARTESIAN_POINT('Ctrl Pts',(17.7646053537182,15.16940183953,4.54818264645704));
#130454=CARTESIAN_POINT('Ctrl Pts',(17.765070795136,15.1761967571458,4.54941704529846));
#130455=CARTESIAN_POINT('Ctrl Pts',(17.7667677982586,15.2007408557987,4.55414804159278));
#130456=CARTESIAN_POINT('Ctrl Pts',(17.7680189063515,15.2184032547852,4.55806967188822));
#130457=CARTESIAN_POINT('Ctrl Pts',(17.7714198517377,15.2655213676021,4.56992785198217));
#130458=CARTESIAN_POINT('Ctrl Pts',(17.7735950741786,15.2947285186452,4.57876674661313));
#130459=CARTESIAN_POINT('Ctrl Pts',(17.7811626291963,15.394380518069,4.61414889493831));
#130460=CARTESIAN_POINT('Ctrl Pts',(17.7865415504299,15.4621248191605,4.64752556447274));
#130461=CARTESIAN_POINT('Ctrl Pts',(17.7926525082424,15.5376947484774,4.69644085618685));
#130462=CARTESIAN_POINT('Ctrl Pts',(17.793643411322,15.5498875094492,4.70473481959738));
#130463=CARTESIAN_POINT('Ctrl Pts',(17.795240653009,15.5694301527178,4.71869288783753));
#130464=CARTESIAN_POINT('Ctrl Pts',(17.7958531007874,15.5768962618671,4.7241893172971));
#130465=CARTESIAN_POINT('Ctrl Pts',(17.7970380765168,15.5912824493956,4.73510273395075));
#130466=CARTESIAN_POINT('Ctrl Pts',(17.797610961855,15.5982099825225,4.74050833597131));
#130467=CARTESIAN_POINT('Ctrl Pts',(17.7989688216112,15.6145554668192,4.75362524662387));
#130468=CARTESIAN_POINT('Ctrl Pts',(17.7997503683703,15.6239035044796,4.7614215462063));
#130469=CARTESIAN_POINT('Ctrl Pts',(17.8026020408453,15.6577473610206,4.79074867648136));
#130470=CARTESIAN_POINT('Ctrl Pts',(17.8046294022459,15.6812976802206,4.81333937561477));
#130471=CARTESIAN_POINT('Ctrl Pts',(17.8103987448658,15.7458968658224,4.8819087227117));
#130472=CARTESIAN_POINT('Ctrl Pts',(17.8140431190923,15.783748718739,4.93066998390617));
#130473=CARTESIAN_POINT('Ctrl Pts',(17.8197536055054,15.8338638310769,5.00979080711079));
#130474=CARTESIAN_POINT('Ctrl Pts',(17.8217374707134,15.8496631023992,5.03771638027573));
#130475=CARTESIAN_POINT('Ctrl Pts',(17.8243325212409,15.8678155763205,5.07388689022333));
#130476=CARTESIAN_POINT('Ctrl Pts',(17.8248765231526,15.8714885644254,5.08145020911602));
#130477=CARTESIAN_POINT('Ctrl Pts',(17.8257656235734,15.8772691371133,5.09375945900256));
#130478=CARTESIAN_POINT('Ctrl Pts',(17.8261072007205,15.8794380314579,5.09847632467666));
#130479=CARTESIAN_POINT('Ctrl Pts',(17.8267943576951,15.8836953580494,5.1079350533619));
#130480=CARTESIAN_POINT('Ctrl Pts',(17.8271399195935,15.8857838666308,5.11267668981902));
#130481=CARTESIAN_POINT('Ctrl Pts',(17.8280496370066,15.8911483488441,5.12512625262244));
#130482=CARTESIAN_POINT('Ctrl Pts',(17.8286171765238,15.8943623758075,5.13286019648734));
#130483=CARTESIAN_POINT('Ctrl Pts',(17.8315568780144,15.9103550484467,5.17280012892302));
#130484=CARTESIAN_POINT('Ctrl Pts',(17.8340017071513,15.921494975487,5.20563184071929));
#130485=CARTESIAN_POINT('Ctrl Pts',(17.8418093038422,15.9510672660986,5.3110951678131));
#130486=CARTESIAN_POINT('Ctrl Pts',(17.8472138362182,15.9628425058149,5.38532108675831));
#130487=CARTESIAN_POINT('Ctrl Pts',(17.8538390623054,15.9668062015164,5.48143769786327));
#130488=CARTESIAN_POINT('Ctrl Pts',(17.855285833799,15.9669805777599,5.50273319879022));
#130489=CARTESIAN_POINT('Ctrl Pts',(17.8574160014287,15.9661901780335,5.53453708969768));
#130490=CARTESIAN_POINT('Ctrl Pts',(17.8581152511595,15.9657570567328,5.54505100174174));
#130491=CARTESIAN_POINT('Ctrl Pts',(17.8593757071274,15.9646588094596,5.56413037953826));
#130492=CARTESIAN_POINT('Ctrl Pts',(17.8599386086797,15.9640510076316,5.57269791483708));
#130493=CARTESIAN_POINT('Ctrl Pts',(17.8611577557631,15.962477800191,5.5913489456024));
#130494=CARTESIAN_POINT('Ctrl Pts',(17.8618125682031,15.9614679260809,5.6014277344616));
#130495=CARTESIAN_POINT('Ctrl Pts',(17.863691000132,15.9580931089762,5.6304963702171));
#130496=CARTESIAN_POINT('Ctrl Pts',(17.8649021777186,15.955322469334,5.64943481144132));
#130497=CARTESIAN_POINT('Ctrl Pts',(17.8687284953191,15.9446744232055,5.70967295325515));
#130498=CARTESIAN_POINT('Ctrl Pts',(17.8712831119922,15.9346652906083,5.7505468834835));
#130499=CARTESIAN_POINT('Ctrl Pts',(17.8771298191637,15.9055236214757,5.84299519021532));
#130500=CARTESIAN_POINT('Ctrl Pts',(17.8803963691972,15.8845932497051,5.89384340318341));
#130501=CARTESIAN_POINT('Ctrl Pts',(17.8849663129955,15.8509738216589,5.95912194267895));
#130502=CARTESIAN_POINT('Ctrl Pts',(17.8861369572696,15.842011792829,5.97535822906351));
#130503=CARTESIAN_POINT('Ctrl Pts',(17.8877936426604,15.8289576550394,5.99747947368217));
#130504=CARTESIAN_POINT('Ctrl Pts',(17.8882582010315,15.8252581573867,6.00359267958698));
#130505=CARTESIAN_POINT('Ctrl Pts',(17.8890515430426,15.8188829220634,6.01386846878965));
#130506=CARTESIAN_POINT('Ctrl Pts',(17.8893781393811,15.8162423926746,6.01805250572704));
#130507=CARTESIAN_POINT('Ctrl Pts',(17.8900774441743,15.8105571822718,6.02690959357493));
#130508=CARTESIAN_POINT('Ctrl Pts',(17.8904506344504,15.8075041429159,6.03157663696451));
#130509=CARTESIAN_POINT('Ctrl Pts',(17.891516327873,15.7987273185627,6.04474327616203));
#130510=CARTESIAN_POINT('Ctrl Pts',(17.8922144326168,15.7929087105019,6.05317838262196));
#130511=CARTESIAN_POINT('Ctrl Pts',(17.8954404229621,15.7656607638038,6.09136582416341));
#130512=CARTESIAN_POINT('Ctrl Pts',(17.8980414806253,15.7426851363144,6.11997440359137));
#130513=CARTESIAN_POINT('Ctrl Pts',(17.9062791616073,15.6655148338207,6.20560287283945));
#130514=CARTESIAN_POINT('Ctrl Pts',(17.9119253599867,15.6059495699985,6.25737353337065));
#130515=CARTESIAN_POINT('Ctrl Pts',(17.9183626049519,15.5275801394844,6.31025782333974));
#130516=CARTESIAN_POINT('Ctrl Pts',(17.9194340767841,15.5141776415332,6.31882839896031));
#130517=CARTESIAN_POINT('Ctrl Pts',(17.9211267538669,15.4924382626409,6.33198584526223));
#130518=CARTESIAN_POINT('Ctrl Pts',(17.9217555171401,15.4842351005887,6.3367868709464));
#130519=CARTESIAN_POINT('Ctrl Pts',(17.9229512914854,15.4683942502812,6.34574699965837));
#130520=CARTESIAN_POINT('Ctrl Pts',(17.9235189444294,15.4607686785824,6.34992552266441));
#130521=CARTESIAN_POINT('Ctrl Pts',(17.9248330694812,15.442875853715,6.35941850816268));
#130522=CARTESIAN_POINT('Ctrl Pts',(17.9255767240289,15.4325674633394,6.36465287936762));
#130523=CARTESIAN_POINT('Ctrl Pts',(17.9280897440018,15.3971416346311,6.38184915926701));
#130524=CARTESIAN_POINT('Ctrl Pts',(17.9298292038722,15.3716018682482,6.39291190815713));
#130525=CARTESIAN_POINT('Ctrl Pts',(17.9343188705862,15.3035698191934,6.41895491018199));
#130526=CARTESIAN_POINT('Ctrl Pts',(17.937021449321,15.2604463229174,6.43209481573727));
#130527=CARTESIAN_POINT('Ctrl Pts',(17.9428039886906,15.1668658533833,6.4536045624667));
#130528=CARTESIAN_POINT('Ctrl Pts',(17.9458777623418,15.1163480766884,6.4610763861211));
#130529=CARTESIAN_POINT('Ctrl Pts',(17.9497843096605,15.055072894217,6.46523645738158));
#130530=CARTESIAN_POINT('Ctrl Pts',(17.9504549526995,15.0446520395152,6.4657746202088));
#130531=CARTESIAN_POINT('Ctrl Pts',(17.9515038550019,15.0285472907884,6.46634512041499));
#130532=CARTESIAN_POINT('Ctrl Pts',(17.9518761349435,15.0228680701773,6.46649619090531));
#130533=CARTESIAN_POINT('Ctrl Pts',(17.9525772418382,15.0122490788378,6.46668501768854));
#130534=CARTESIAN_POINT('Ctrl Pts',(17.9529054264019,15.0073098410021,6.46673498188979));
#130535=CARTESIAN_POINT('Ctrl Pts',(17.9537030219731,14.9953781813697,6.46676423970374));
#130536=CARTESIAN_POINT('Ctrl Pts',(17.9541743767159,14.9883860522446,6.46670552167659));
#130537=CARTESIAN_POINT('Ctrl Pts',(17.9559149629149,14.9627592710454,6.46621225703878));
#130538=CARTESIAN_POINT('Ctrl Pts',(17.9572048927681,14.9441386915784,6.46531466938631));
#130539=CARTESIAN_POINT('Ctrl Pts',(17.960752642355,14.8936380092983,6.46141437290753));
#130540=CARTESIAN_POINT('Ctrl Pts',(17.9630380382578,14.8618625687701,6.4573653012614));
#130541=CARTESIAN_POINT('Ctrl Pts',(17.970463928082,14.7596968017413,6.43915396490156));
#130542=CARTESIAN_POINT('Ctrl Pts',(17.9755830178685,14.6906549627653,6.41872997247535));
#130543=CARTESIAN_POINT('Ctrl Pts',(17.9814919137304,14.6105259787636,6.38495515043246));
#130544=CARTESIAN_POINT('Ctrl Pts',(17.9825121388226,14.5966888272792,6.37873532585098));
#130545=CARTESIAN_POINT('Ctrl Pts',(17.9841449370835,14.5745517127815,6.36815152473711));
#130546=CARTESIAN_POINT('Ctrl Pts',(17.9847641080932,14.5661592685921,6.36398816258358));
#130547=CARTESIAN_POINT('Ctrl Pts',(17.9859547903937,14.5500309856751,6.35569289597671));
#130548=CARTESIAN_POINT('Ctrl Pts',(17.9865267589366,14.5422882810484,6.35157644207727));
#130549=CARTESIAN_POINT('Ctrl Pts',(17.9878710868155,14.5241104634479,6.34159253811574));
#130550=CARTESIAN_POINT('Ctrl Pts',(17.9886402366176,14.5137260751381,6.3356354116798));
#130551=CARTESIAN_POINT('Ctrl Pts',(17.9913669829866,14.4770128624685,6.31365823603719));
#130552=CARTESIAN_POINT('Ctrl Pts',(17.9932869518528,14.4513414938149,6.29657352718076));
#130553=CARTESIAN_POINT('Ctrl Pts',(17.9982959936048,14.3856432203931,6.24816471367412));
#130554=CARTESIAN_POINT('Ctrl Pts',(18.0013257193629,14.3471955686309,6.21486448611302));
#130555=CARTESIAN_POINT('Ctrl Pts',(18.0068795629692,14.2826349551585,6.14937532031835));
#130556=CARTESIAN_POINT('Ctrl Pts',(18.0093867889278,14.2556343426971,6.11823942649461));
#130557=CARTESIAN_POINT('Ctrl Pts',(18.0126766367787,14.2242945267007,6.07706027901792));
#130558=CARTESIAN_POINT('Ctrl Pts',(18.0133564858849,14.2180247176223,6.06853512044301));
#130559=CARTESIAN_POINT('Ctrl Pts',(18.0144165957525,14.2085894660936,6.05525447456439));
#130560=CARTESIAN_POINT('Ctrl Pts',(18.0147906644586,14.2053239244271,6.05057069996892));
#130561=CARTESIAN_POINT('Ctrl Pts',(18.0154901102102,14.1993402768648,6.04182419855143));
#130562=CARTESIAN_POINT('Ctrl Pts',(18.0158147731818,14.1966112122535,6.03776938015437));
#130563=CARTESIAN_POINT('Ctrl Pts',(18.0165979786235,14.1901419401326,6.0279982474826));
#130564=CARTESIAN_POINT('Ctrl Pts',(18.0170583404214,14.1864314394967,6.02226278562051));
#130565=CARTESIAN_POINT('Ctrl Pts',(18.0187284688762,14.1732882583315,6.00146689548224));
#130566=CARTESIAN_POINT('Ctrl Pts',(18.0199572759245,14.1642110047314,5.98618722333599));
#130567=CARTESIAN_POINT('Ctrl Pts',(18.0232779348797,14.1411125904707,5.94474561044486));
#130568=CARTESIAN_POINT('Ctrl Pts',(18.0253942376146,14.1278665469322,5.91817376006185));
#130569=CARTESIAN_POINT('Ctrl Pts',(18.030008532074,14.10179961599,5.85923626695958));
#130570=CARTESIAN_POINT('Ctrl Pts',(18.032506000554,14.0894604934114,5.82669949922358));
#130571=CARTESIAN_POINT('Ctrl Pts',(18.0381744012657,14.0652153082359,5.75062782529277));
#130572=CARTESIAN_POINT('Ctrl Pts',(18.0413173170397,14.0545475253697,5.70677847415103));
#130573=CARTESIAN_POINT('Ctrl Pts',(18.0452697394032,14.0447346602697,5.64917142230363));
#130574=CARTESIAN_POINT('Ctrl Pts',(18.0461648294619,14.0427647067609,5.6359581039228));
#130575=CARTESIAN_POINT('Ctrl Pts',(18.0475864180532,14.0400460673616,5.61471258456415));
#130576=CARTESIAN_POINT('Ctrl Pts',(18.0481182525748,14.0391230005478,5.60670486581259));
#130577=CARTESIAN_POINT('Ctrl Pts',(18.0491809742467,14.0374691850684,5.59058840811177));
#130578=CARTESIAN_POINT('Ctrl Pts',(18.0497117561455,14.0367404989088,5.58248011649193));
#130579=CARTESIAN_POINT('Ctrl Pts',(18.0507941390795,14.0354560278096,5.56583101652093));
#130580=CARTESIAN_POINT('Ctrl Pts',(18.0513453645958,14.0349110656988,5.55729008100414));
#130581=CARTESIAN_POINT('Ctrl Pts',(18.0529443477483,14.033651848075,5.53234690915795));
#130582=CARTESIAN_POINT('Ctrl Pts',(18.053982926214,14.0332418710457,5.51593207069491));
#130583=CARTESIAN_POINT('Ctrl Pts',(18.0550108970343,14.0332501220858,5.49951414732463));
#130584=CARTESIAN_POINT('Origin',(13.2437274406976,15.,5.5));
#130585=CARTESIAN_POINT('',(14.3005175290658,14.3042076641721,5.74898599439144));
#130586=CARTESIAN_POINT('',(14.2215869807902,14.3043221293274,5.74892323211324));
#130587=CARTESIAN_POINT('',(13.2437274406976,14.3042076641721,5.74898599439144));
#130588=CARTESIAN_POINT('',(14.2111241293531,15.1353891683142,6.22635393211075));
#130589=CARTESIAN_POINT('Ctrl Pts',(14.3005175290658,14.3042076641721,5.74898599439144));
#130590=CARTESIAN_POINT('Ctrl Pts',(14.2989144299391,14.310124946029,5.76552186170024));
#130591=CARTESIAN_POINT('Ctrl Pts',(14.2973221359364,14.3166336622363,5.78185228783364));
#130592=CARTESIAN_POINT('Ctrl Pts',(14.2949908712359,14.327164580291,5.8057553425873));
#130593=CARTESIAN_POINT('Ctrl Pts',(14.2942349309219,14.3307405840018,5.81350547873262));
#130594=CARTESIAN_POINT('Ctrl Pts',(14.2930767780573,14.3364790020146,5.82539617763793));
#130595=CARTESIAN_POINT('Ctrl Pts',(14.29266952052,14.3385475893906,5.82958079351132));
#130596=CARTESIAN_POINT('Ctrl Pts',(14.2918147405124,14.3429990359836,5.83837502079495));
#130597=CARTESIAN_POINT('Ctrl Pts',(14.2913678469936,14.3453910720543,5.842979703518));
#130598=CARTESIAN_POINT('Ctrl Pts',(14.2901888210751,14.3518693914283,5.85513578615727));
#130599=CARTESIAN_POINT('Ctrl Pts',(14.2894615431732,14.35603928679,5.86264215447201));
#130600=CARTESIAN_POINT('Ctrl Pts',(14.2858238669878,14.3777300403012,5.90013383873696));
#130601=CARTESIAN_POINT('Ctrl Pts',(14.2830113999811,14.3972205376587,5.92893426075455));
#130602=CARTESIAN_POINT('Ctrl Pts',(14.2760109154024,14.4508371041792,5.99724846229244));
#130603=CARTESIAN_POINT('Ctrl Pts',(14.2718496518594,14.4872475473401,6.0347149362366));
#130604=CARTESIAN_POINT('Ctrl Pts',(14.2664203483292,14.5374462877555,6.07648898730475));
#130605=CARTESIAN_POINT('Ctrl Pts',(14.2653130928246,14.5478238941084,6.08466418975156));
#130606=CARTESIAN_POINT('Ctrl Pts',(14.263514522439,14.5648616265861,6.09736106981975));
#130607=CARTESIAN_POINT('Ctrl Pts',(14.2628300919144,14.5713865962394,6.10205995638556));
#130608=CARTESIAN_POINT('Ctrl Pts',(14.2613774595412,14.5853120572962,6.11174712042919));
#130609=CARTESIAN_POINT('Ctrl Pts',(14.2606084378468,14.592728781948,6.11670963095666));
#130610=CARTESIAN_POINT('Ctrl Pts',(14.2586925803046,14.6113032768607,6.12865658437628));
#130611=CARTESIAN_POINT('Ctrl Pts',(14.2575401565641,14.6225607862165,6.13547921693106));
#130612=CARTESIAN_POINT('Ctrl Pts',(14.2526482115671,14.6706594508275,6.1629005437584));
#130613=CARTESIAN_POINT('Ctrl Pts',(14.2488148988832,14.7090419758722,6.18062071603704));
#130614=CARTESIAN_POINT('Ctrl Pts',(14.2408477729093,14.7906608743542,6.21013179820528));
#130615=CARTESIAN_POINT('Ctrl Pts',(14.2367251712402,14.8338921033393,6.22146994500351));
#130616=CARTESIAN_POINT('Ctrl Pts',(14.2319785368801,14.886342120804,6.23025777311806));
#130617=CARTESIAN_POINT('Ctrl Pts',(14.2312189746746,14.8948237283986,6.23152751170346));
#130618=CARTESIAN_POINT('Ctrl Pts',(14.230011268403,14.9084733731188,6.23332859796016));
#130619=CARTESIAN_POINT('Ctrl Pts',(14.229558538495,14.9136279980075,6.23395356793651));
#130620=CARTESIAN_POINT('Ctrl Pts',(14.2286433800297,14.924131127763,6.23511482116643));
#130621=CARTESIAN_POINT('Ctrl Pts',(14.2281811636339,14.9294796988879,6.23564718368991));
#130622=CARTESIAN_POINT('Ctrl Pts',(14.2272289140466,14.9405795405494,6.23662981240413));
#130623=CARTESIAN_POINT('Ctrl Pts',(14.2267393538851,14.9463312415515,6.23707119196986));
#130624=CARTESIAN_POINT('Ctrl Pts',(14.225483544493,14.9611861936966,6.23803632629154));
#130625=CARTESIAN_POINT('Ctrl Pts',(14.224721774194,14.9702953122305,6.23845905905128));
#130626=CARTESIAN_POINT('Ctrl Pts',(14.2196286246053,15.0316935426315,6.24017036159618));
#130627=CARTESIAN_POINT('Ctrl Pts',(14.2154840848789,15.083988662881,6.23607315801718));
#130628=CARTESIAN_POINT('Ctrl Pts',(14.2112487597337,15.1354171833248,6.2264868797579));
#130629=CARTESIAN_POINT('',(14.2104374411951,14.3543584447163,5.86069344365419));
#130630=CARTESIAN_POINT('Origin',(14.211,15.,5.5));
#130631=CARTESIAN_POINT('Ctrl Pts',(14.210553733114,14.3548588757739,5.86043574993653));
#130632=CARTESIAN_POINT('Ctrl Pts',(14.2112419750398,14.3509984596515,5.85352602137142));
#130633=CARTESIAN_POINT('Ctrl Pts',(14.2119342498727,14.3472494500005,5.84655498469671));
#130634=CARTESIAN_POINT('Ctrl Pts',(14.2137122629482,14.3379642055853,5.82860430238041));
#130635=CARTESIAN_POINT('Ctrl Pts',(14.2148034098591,14.3325889791096,5.81754475279969));
#130636=CARTESIAN_POINT('Ctrl Pts',(14.2177517409103,14.3189282362072,5.78755701600778));
#130637=CARTESIAN_POINT('Ctrl Pts',(14.2196239758872,14.3111569531308,5.76840805509445));
#130638=CARTESIAN_POINT('Ctrl Pts',(14.2215130984838,14.3041985386328,5.74896049156307));
#130639=CARTESIAN_POINT('Origin',(13.2437274406976,15.,5.5));
#130640=CARTESIAN_POINT('',(14.7015708502323,14.3042076642092,5.74898599449524));
#130641=CARTESIAN_POINT('',(14.6223301870619,14.3039706980243,5.74911183878948));
#130642=CARTESIAN_POINT('',(13.2437274406976,14.3042076641721,5.74898599439144));
#130643=CARTESIAN_POINT('Ctrl Pts',(14.7015708502323,14.3042076642463,5.74898599459905));
#130644=CARTESIAN_POINT('Ctrl Pts',(14.701267806545,14.3053884691484,5.75228575851628));
#130645=CARTESIAN_POINT('Ctrl Pts',(14.700963995868,14.3065927345564,5.75557708635813));
#130646=CARTESIAN_POINT('Ctrl Pts',(14.699411568657,14.312849886356,5.77230843738443));
#130647=CARTESIAN_POINT('Ctrl Pts',(14.6981511326319,14.3182698787912,5.78560662306213));
#130648=CARTESIAN_POINT('Ctrl Pts',(14.6953173478509,14.3311929782285,5.81484656144697));
#130649=CARTESIAN_POINT('Ctrl Pts',(14.6937386979415,14.3388856121142,5.83069450392347));
#130650=CARTESIAN_POINT('Ctrl Pts',(14.6879994437572,14.3686134650661,5.88674695541637));
#130651=CARTESIAN_POINT('Ctrl Pts',(14.683760741336,14.393810839229,5.92515436181349));
#130652=CARTESIAN_POINT('Ctrl Pts',(14.6774540830455,14.4368037430779,5.97902419704531));
#130653=CARTESIAN_POINT('Ctrl Pts',(14.6753575046946,14.4520473638091,5.9963893161148));
#130654=CARTESIAN_POINT('Ctrl Pts',(14.6726381683769,14.4732803807093,6.01840480435905));
#130655=CARTESIAN_POINT('Ctrl Pts',(14.6719769805336,14.4785618480709,6.02371687581842));
#130656=CARTESIAN_POINT('Ctrl Pts',(14.6708846891836,14.4874967262137,6.03243433077191));
#130657=CARTESIAN_POINT('Ctrl Pts',(14.6704504500508,14.4911053891,6.03588450647049));
#130658=CARTESIAN_POINT('Ctrl Pts',(14.6695259293109,14.4989133875257,6.04319956691947));
#130659=CARTESIAN_POINT('Ctrl Pts',(14.6690364567184,14.5031229749826,6.04705282319242));
#130660=CARTESIAN_POINT('Ctrl Pts',(14.6675936522134,14.5157444538783,6.05834001663442));
#130661=CARTESIAN_POINT('Ctrl Pts',(14.6666496488284,14.5242820147883,6.06563190129867));
#130662=CARTESIAN_POINT('Ctrl Pts',(14.6643956685121,14.5452626249511,6.08274005164855));
#130663=CARTESIAN_POINT('Ctrl Pts',(14.6630954446102,14.5578619550194,6.09235637360294));
#130664=CARTESIAN_POINT('Ctrl Pts',(14.6592979196196,14.595831125286,6.11944893541082));
#130665=CARTESIAN_POINT('Ctrl Pts',(14.6568315289693,14.62199520517,6.13575308447036));
#130666=CARTESIAN_POINT('Ctrl Pts',(14.651533144489,14.6798446657623,6.16696465836887));
#130667=CARTESIAN_POINT('Ctrl Pts',(14.6487024788669,14.7117220691834,6.18134916359588));
#130668=CARTESIAN_POINT('Ctrl Pts',(14.6446807964519,14.7571488775215,6.19808753652944));
#130669=CARTESIAN_POINT('Ctrl Pts',(14.6435510954004,14.7699277282347,6.20240271915735));
#130670=CARTESIAN_POINT('Ctrl Pts',(14.6417264575681,14.7905417391893,6.20874082345869));
#130671=CARTESIAN_POINT('Ctrl Pts',(14.6410388148323,14.7983048935685,6.2109890230949));
#130672=CARTESIAN_POINT('Ctrl Pts',(14.639587463633,14.8146663435325,6.21543775926846));
#130673=CARTESIAN_POINT('Ctrl Pts',(14.6388230311735,14.8232704705992,6.21761160113773));
#130674=CARTESIAN_POINT('Ctrl Pts',(14.6369362113905,14.8444605089657,6.22256109948304));
#130675=CARTESIAN_POINT('Ctrl Pts',(14.6358086117844,14.8570833776075,6.22516333971602));
#130676=CARTESIAN_POINT('Ctrl Pts',(14.6308007329605,14.9129187302258,6.23515958043277));
#130677=CARTESIAN_POINT('Ctrl Pts',(14.626817120478,14.9566643240459,6.23902870969415));
#130678=CARTESIAN_POINT('Ctrl Pts',(14.6188072372161,15.0438864757312,6.23897124817574));
#130679=CARTESIAN_POINT('Ctrl Pts',(14.6147977956115,15.087202768997,6.2351196229914));
#130680=CARTESIAN_POINT('Ctrl Pts',(14.6101461821876,15.1384849684717,6.22596030866754));
#130681=CARTESIAN_POINT('Ctrl Pts',(14.6093764317879,15.1470091997274,6.22428224605358));
#130682=CARTESIAN_POINT('Ctrl Pts',(14.6081570612918,15.1605950959485,6.22135799160512));
#130683=CARTESIAN_POINT('Ctrl Pts',(14.6077026917716,15.1656763226698,6.22020795544054));
#130684=CARTESIAN_POINT('Ctrl Pts',(14.6067904429232,15.1759222450937,6.21777480900454));
#130685=CARTESIAN_POINT('Ctrl Pts',(14.6063327045588,15.1810860681342,6.21648946553497));
#130686=CARTESIAN_POINT('Ctrl Pts',(14.6050881905973,15.1951750241103,6.2128204814137));
#130687=CARTESIAN_POINT('Ctrl Pts',(14.6043072683205,15.2040704470951,6.21032500006579));
#130688=CARTESIAN_POINT('Ctrl Pts',(14.6008266032506,15.2438522987441,6.19835568056725));
#130689=CARTESIAN_POINT('Ctrl Pts',(14.5982072210285,15.2741478773704,6.18702845060417));
#130690=CARTESIAN_POINT('Ctrl Pts',(14.5912731272345,15.352531799387,6.15170689407542));
#130691=CARTESIAN_POINT('Ctrl Pts',(14.5869924055877,15.3989031539572,6.12440053168542));
#130692=CARTESIAN_POINT('Ctrl Pts',(14.5814475175013,15.4523326473204,6.08453858548331));
#130693=CARTESIAN_POINT('Ctrl Pts',(14.5803567326554,15.4625500410934,6.07648729333851));
#130694=CARTESIAN_POINT('Ctrl Pts',(14.5785099034493,15.4793196965112,6.06253993614659));
#130695=CARTESIAN_POINT('Ctrl Pts',(14.5777596592846,15.4859888059428,6.0567884854284));
#130696=CARTESIAN_POINT('Ctrl Pts',(14.5762222352992,15.4993538943086,6.04483933894811));
#130697=CARTESIAN_POINT('Ctrl Pts',(14.57543483262,15.5060410232793,6.03863409054969));
#130698=CARTESIAN_POINT('Ctrl Pts',(14.5734005193417,15.5229035765834,6.02239546219996));
#130699=CARTESIAN_POINT('Ctrl Pts',(14.5721463754687,15.5329054375387,6.01218834660953));
#130700=CARTESIAN_POINT('Ctrl Pts',(14.5693299168533,15.5544796238679,5.9888551105171));
#130701=CARTESIAN_POINT('Ctrl Pts',(14.5677624109683,15.5658940131104,5.97559524729847));
#130702=CARTESIAN_POINT('Ctrl Pts',(14.5621063476228,15.604989822456,5.92677657142481));
#130703=CARTESIAN_POINT('Ctrl Pts',(14.557942324498,15.6298764863027,5.88910912300637));
#130704=CARTESIAN_POINT('Ctrl Pts',(14.5515937631531,15.6626598713458,5.82801341353703));
#130705=CARTESIAN_POINT('Ctrl Pts',(14.5493866804984,15.673083052649,5.80605617346355));
#130706=CARTESIAN_POINT('Ctrl Pts',(14.5465681749533,15.6852535609962,5.77677351284916));
#130707=CARTESIAN_POINT('Ctrl Pts',(14.5459135432988,15.6879972592758,5.7698810940452));
#130708=CARTESIAN_POINT('Ctrl Pts',(14.5448287443299,15.692409325123,5.75829274207759));
#130709=CARTESIAN_POINT('Ctrl Pts',(14.5443955369173,15.6941347552552,5.75361932627306));
#130710=CARTESIAN_POINT('Ctrl Pts',(14.5434693003087,15.6977461192832,5.74352472138963));
#130711=CARTESIAN_POINT('Ctrl Pts',(14.5429771317728,15.6996163813272,5.7380984305573));
#130712=CARTESIAN_POINT('Ctrl Pts',(14.5415165932995,15.7050138167016,5.72182558751973));
#130713=CARTESIAN_POINT('Ctrl Pts',(14.5405579002258,15.7083535273689,5.71091798445137));
#130714=CARTESIAN_POINT('Ctrl Pts',(14.5382593569631,15.7158264147139,5.68432700761366));
#130715=CARTESIAN_POINT('Ctrl Pts',(14.536929787555,15.7196986050995,5.66857609485616));
#130716=CARTESIAN_POINT('Ctrl Pts',(14.5331479054982,15.7293040133022,5.62309632964483));
#130717=CARTESIAN_POINT('Ctrl Pts',(14.5307237780026,15.7337334187486,5.59312600285986));
#130718=CARTESIAN_POINT('Ctrl Pts',(14.5254769870785,15.7392795147375,5.52827263108273));
#130719=CARTESIAN_POINT('Ctrl Pts',(14.5226550617432,15.7397903361777,5.49341529172412));
#130720=CARTESIAN_POINT('Ctrl Pts',(14.5186430831266,15.7370883270293,5.44519572933336));
#130721=CARTESIAN_POINT('Ctrl Pts',(14.5175138901773,15.7359660948069,5.43176092730023));
#130722=CARTESIAN_POINT('Ctrl Pts',(14.5156898996518,15.7335845841976,5.41033423059805));
#130723=CARTESIAN_POINT('Ctrl Pts',(14.5150023882257,15.7325603545599,5.40231884333171));
#130724=CARTESIAN_POINT('Ctrl Pts',(14.5135511865942,15.7301359609925,5.38553941311485));
#130725=CARTESIAN_POINT('Ctrl Pts',(14.512786770935,15.7287089420086,5.37678064127879));
#130726=CARTESIAN_POINT('Ctrl Pts',(14.5108997330682,15.7248231477976,5.35536754042156));
#130727=CARTESIAN_POINT('Ctrl Pts',(14.5097718935652,15.7221904173392,5.34274829258643));
#130728=CARTESIAN_POINT('Ctrl Pts',(14.5047524470521,15.7091275725118,5.28741574677365));
#130729=CARTESIAN_POINT('Ctrl Pts',(14.5007568151518,15.6952294455235,5.24562106055232));
#130730=CARTESIAN_POINT('Ctrl Pts',(14.4927490618646,15.6604595581773,5.16565844288695));
#130731=CARTESIAN_POINT('Ctrl Pts',(14.4887542532177,15.6397661571429,5.12758756581377));
#130732=CARTESIAN_POINT('Ctrl Pts',(14.4841152135233,15.611052223549,5.0842935642736));
#130733=CARTESIAN_POINT('Ctrl Pts',(14.4833443905735,15.6061165815586,5.07712960526417));
#130734=CARTESIAN_POINT('Ctrl Pts',(14.4821237836821,15.5980233966744,5.06581550691226));
#130735=CARTESIAN_POINT('Ctrl Pts',(14.4816692331542,15.5949466107293,5.06160897199963));
#130736=CARTESIAN_POINT('Ctrl Pts',(14.4807571432415,15.5886412558044,5.05317705768354));
#130737=CARTESIAN_POINT('Ctrl Pts',(14.4802997386425,15.5854110859988,5.04895328875033));
#130738=CARTESIAN_POINT('Ctrl Pts',(14.479057029991,15.5764559025559,5.0375017866286));
#130739=CARTESIAN_POINT('Ctrl Pts',(14.4782775529401,15.5706405294859,5.0303454298236));
#130740=CARTESIAN_POINT('Ctrl Pts',(14.4748114202874,15.5439558195449,4.99873513288063));
#130741=CARTESIAN_POINT('Ctrl Pts',(14.4722043739278,15.5216357405264,4.97554685669194));
#130742=CARTESIAN_POINT('Ctrl Pts',(14.4652595821577,15.4580068373192,4.91753882279555));
#130743=CARTESIAN_POINT('Ctrl Pts',(14.4609570448515,15.4142852308484,4.88567253461053));
#130744=CARTESIAN_POINT('Ctrl Pts',(14.455390681674,15.356231974462,4.85239820087444));
#130745=CARTESIAN_POINT('Ctrl Pts',(14.4543026260153,15.3448091395608,4.84624475101794));
#130746=CARTESIAN_POINT('Ctrl Pts',(14.4524590325502,15.3253759946238,4.83642716293709));
#130747=CARTESIAN_POINT('Ctrl Pts',(14.4517092484074,15.3174511469462,4.83259966805812));
#130748=CARTESIAN_POINT('Ctrl Pts',(14.4501716300559,15.3011696218219,4.82509170375196));
#130749=CARTESIAN_POINT('Ctrl Pts',(14.4493835582933,15.2928093376706,4.82142279370527));
#130750=CARTESIAN_POINT('Ctrl Pts',(14.4473449115132,15.2711571624565,4.81239535879327));
#130751=CARTESIAN_POINT('Ctrl Pts',(14.4460870403816,15.2577741557115,4.80726717132763));
#130752=CARTESIAN_POINT('Ctrl Pts',(14.4432602946794,15.227675073818,4.79672655537037));
#130753=CARTESIAN_POINT('Ctrl Pts',(14.4416861638558,15.2108983797514,4.79151481985206));
#130754=CARTESIAN_POINT('Ctrl Pts',(14.4359805401268,15.1500270897019,4.77495853504284));
#130755=CARTESIAN_POINT('Ctrl Pts',(14.4317720309761,15.1050931814404,4.76709615589753));
#130756=CARTESIAN_POINT('Ctrl Pts',(14.4254612377103,15.0363682778015,4.76152348289476));
#130757=CARTESIAN_POINT('Ctrl Pts',(14.423332631217,15.0129299258302,4.76074139673383));
#130758=CARTESIAN_POINT('Ctrl Pts',(14.4205794390972,14.9819697409277,4.7611816868809));
#130759=CARTESIAN_POINT('Ctrl Pts',(14.4199152893824,14.9744494679774,4.76140351050627));
#130760=CARTESIAN_POINT('Ctrl Pts',(14.4188238039256,14.9619891331639,4.76196160721052));
#130761=CARTESIAN_POINT('Ctrl Pts',(14.4183932385791,14.9570469051014,4.76223273741448));
#130762=CARTESIAN_POINT('Ctrl Pts',(14.4174750117101,14.9464449131299,4.76292127211181));
#130763=CARTESIAN_POINT('Ctrl Pts',(14.4169881692252,14.9407866108438,4.7633542374187));
#130764=CARTESIAN_POINT('Ctrl Pts',(14.4155632739837,14.9241334372702,4.76482164944413));
#130765=CARTESIAN_POINT('Ctrl Pts',(14.4146341952418,14.913155518348,4.76603745478489));
#130766=CARTESIAN_POINT('Ctrl Pts',(14.4124251720849,14.8868716735825,4.7695464557907));
#130767=CARTESIAN_POINT('Ctrl Pts',(14.4111544559741,14.8716021425636,4.77207523691253));
#130768=CARTESIAN_POINT('Ctrl Pts',(14.4050685100603,14.7983287413865,4.78658781886045));
#130769=CARTESIAN_POINT('Ctrl Pts',(14.4003940549879,14.7418306091224,4.8050345773885));
#130770=CARTESIAN_POINT('Ctrl Pts',(14.3941061036381,14.6726119777229,4.83725463359074));
#130771=CARTESIAN_POINT('Ctrl Pts',(14.3926821566971,14.6573418624367,4.84501935091343));
#130772=CARTESIAN_POINT('Ctrl Pts',(14.3904211205612,14.6338393552793,4.85801705124607));
#130773=CARTESIAN_POINT('Ctrl Pts',(14.3895962993838,14.6254167217405,4.86289477075438));
#130774=CARTESIAN_POINT('Ctrl Pts',(14.3880262539937,14.6096860749912,4.87242447266838));
#130775=CARTESIAN_POINT('Ctrl Pts',(14.3872823913848,14.6023586867983,4.87704143415004));
#130776=CARTESIAN_POINT('Ctrl Pts',(14.3855498704174,14.5855929893541,4.88802175376457));
#130777=CARTESIAN_POINT('Ctrl Pts',(14.3845579872634,14.5762174699572,4.89447635884686));
#130778=CARTESIAN_POINT('Ctrl Pts',(14.3809651740239,14.5430783396257,4.91843773119462));
#130779=CARTESIAN_POINT('Ctrl Pts',(14.3783205146754,14.5202224587935,4.93714557179297));
#130780=CARTESIAN_POINT('Ctrl Pts',(14.372655517622,14.4744377065392,4.9794399971453));
#130781=CARTESIAN_POINT('Ctrl Pts',(14.3696320534765,14.451838430233,5.00329374460986));
#130782=CARTESIAN_POINT('Ctrl Pts',(14.3638252711711,14.4115032183826,5.05198533481528));
#130783=CARTESIAN_POINT('Ctrl Pts',(14.3610463160058,14.3935668338413,5.07657957406272));
#130784=CARTESIAN_POINT('Ctrl Pts',(14.357654334462,14.3730477032107,5.10870574949459));
#130785=CARTESIAN_POINT('Ctrl Pts',(14.3569736187382,14.3690016131414,5.11526447580852));
#130786=CARTESIAN_POINT('Ctrl Pts',(14.3558632174351,14.3625122745119,5.12616157653991));
#130787=CARTESIAN_POINT('Ctrl Pts',(14.3554300567931,14.3600090464157,5.13046332624843));
#130788=CARTESIAN_POINT('Ctrl Pts',(14.3545163845745,14.3547869204473,5.13964971806609));
#130789=CARTESIAN_POINT('Ctrl Pts',(14.3540365641347,14.3520796497563,5.14454048084657));
#130790=CARTESIAN_POINT('Ctrl Pts',(14.3526542387923,14.3443910913841,5.15880985265868));
#130791=CARTESIAN_POINT('Ctrl Pts',(14.3517599418001,14.3395558549154,5.16826618446797));
#130792=CARTESIAN_POINT('Ctrl Pts',(14.3468403861918,14.313840845554,5.22135021339282));
#130793=CARTESIAN_POINT('Ctrl Pts',(14.3429902757745,14.2970768897113,5.26684676113759));
#130794=CARTESIAN_POINT('Ctrl Pts',(14.3360614301468,14.2754051121965,5.35001730955931));
#130795=CARTESIAN_POINT('Ctrl Pts',(14.3330136320369,14.2687191110345,5.38703878684167));
#130796=CARTESIAN_POINT('Ctrl Pts',(14.328878994262,14.2636493618928,5.43633933637818));
#130797=CARTESIAN_POINT('Ctrl Pts',(14.3278703137976,14.2627129722432,5.44830137806929));
#130798=CARTESIAN_POINT('Ctrl Pts',(14.3261122505771,14.2615990058168,5.46899715270202));
#130799=CARTESIAN_POINT('Ctrl Pts',(14.3253672087991,14.2612843243115,5.47772128158993));
#130800=CARTESIAN_POINT('Ctrl Pts',(14.3238068640553,14.2609512530727,5.49588156880129));
#130801=CARTESIAN_POINT('Ctrl Pts',(14.3229908963015,14.2609589130649,5.50531653813821));
#130802=CARTESIAN_POINT('Ctrl Pts',(14.3207746599572,14.2614667867423,5.53075971845945));
#130803=CARTESIAN_POINT('Ctrl Pts',(14.3193643716485,14.2623067408155,5.54675507378159));
#130804=CARTESIAN_POINT('Ctrl Pts',(14.3153935712907,14.2660927965288,5.59121109885985));
#130805=CARTESIAN_POINT('Ctrl Pts',(14.3128030662614,14.2701726250593,5.6195444446003));
#130806=CARTESIAN_POINT('Ctrl Pts',(14.3069704640862,14.2829054103019,5.68202472040388));
#130807=CARTESIAN_POINT('Ctrl Pts',(14.3037235300448,14.2923738286286,5.71591629464904));
#130808=CARTESIAN_POINT('Ctrl Pts',(14.3005175290658,14.3042076641721,5.74898599439144));
#130809=CARTESIAN_POINT('',(14.2442422781566,14.2606640288133,5.50021908758302));
#130810=CARTESIAN_POINT('Ctrl Pts',(14.2215869807902,14.3043221293274,5.74892323211324));
#130811=CARTESIAN_POINT('Ctrl Pts',(14.2248697646003,14.2919680803988,5.7146519512802));
#130812=CARTESIAN_POINT('Ctrl Pts',(14.2281873301198,14.2821560247849,5.67953294869403));
#130813=CARTESIAN_POINT('Ctrl Pts',(14.2314770181605,14.2749982774291,5.6439414857939));
#130814=CARTESIAN_POINT('Ctrl Pts',(14.234766709764,14.2678405223213,5.60834998434789));
#130815=CARTESIAN_POINT('Ctrl Pts',(14.2379949555046,14.2632814103378,5.57229160377229));
#130816=CARTESIAN_POINT('Ctrl Pts',(14.2411291090077,14.2614900739362,5.53615063568822));
#130817=CARTESIAN_POINT('Ctrl Pts',(14.2421667238184,14.2608970215604,5.52418555365778));
#130818=CARTESIAN_POINT('Ctrl Pts',(14.2432044289964,14.2606238001271,5.51220407947721));
#130819=CARTESIAN_POINT('Ctrl Pts',(14.2442421952123,14.2606640265644,5.50022005200379));
#130820=CARTESIAN_POINT('Ctrl Pts',(14.2442423611009,14.2606640310621,5.50021812316224));
#130821=CARTESIAN_POINT('Ctrl Pts',(14.2467604292871,14.2607084642982,5.47077714598032));
#130822=CARTESIAN_POINT('Ctrl Pts',(14.2492104808063,14.2625220578675,5.4412707827379));
#130823=CARTESIAN_POINT('Ctrl Pts',(14.2516428117451,14.2661106683047,5.41193170632528));
#130824=CARTESIAN_POINT('Ctrl Pts',(14.2519183407403,14.266517178049,5.40860824153004));
#130825=CARTESIAN_POINT('Ctrl Pts',(14.2521936423477,14.2669464382962,5.40528697174121));
#130826=CARTESIAN_POINT('Ctrl Pts',(14.2524687896758,14.2673984361738,5.40196827146818));
#130827=CARTESIAN_POINT('Ctrl Pts',(14.2551687278868,14.2718337557873,5.36940286100478));
#130828=CARTESIAN_POINT('Ctrl Pts',(14.257854511435,14.2784609639366,5.33708066115314));
#130829=CARTESIAN_POINT('Ctrl Pts',(14.2605672626014,14.2872101843153,5.30531268485562));
#130830=CARTESIAN_POINT('Ctrl Pts',(14.263277356756,14.2959508352457,5.27357582379153));
#130831=CARTESIAN_POINT('Ctrl Pts',(14.2660147514805,14.3068088742505,5.24239213419929));
#130832=CARTESIAN_POINT('Ctrl Pts',(14.2688013850528,14.3196770880376,5.21205406993458));
#130833=CARTESIAN_POINT('Ctrl Pts',(14.2716167631207,14.3326780391594,5.18140306450668));
#130834=CARTESIAN_POINT('Ctrl Pts',(14.2744826125123,14.3477306509699,5.15161525159242));
#130835=CARTESIAN_POINT('Ctrl Pts',(14.2773975710157,14.3646909466205,5.12297374166932));
#130836=CARTESIAN_POINT('Ctrl Pts',(14.2802840518035,14.3814855484971,5.09461204525697));
#130837=CARTESIAN_POINT('Ctrl Pts',(14.2832186288134,14.400150649726,5.06737434612188));
#130838=CARTESIAN_POINT('Ctrl Pts',(14.2861755727077,14.4205162102673,5.04151752419138));
#130839=CARTESIAN_POINT('Ctrl Pts',(14.2891762759477,14.4411831575227,5.01527805123663));
#130840=CARTESIAN_POINT('Ctrl Pts',(14.2921998140541,14.4636015705217,4.9904607738186));
#130841=CARTESIAN_POINT('Ctrl Pts',(14.2951957160754,14.4875607689585,4.96731456331708));
#130842=CARTESIAN_POINT('Ctrl Pts',(14.297962320326,14.509686198884,4.94593989755595));
#130843=CARTESIAN_POINT('Ctrl Pts',(14.3007048100857,14.5331262564948,4.92598991755922));
#130844=CARTESIAN_POINT('Ctrl Pts',(14.3033699190066,14.5576837540332,4.90764441773356));
#130845=CARTESIAN_POINT('Ctrl Pts',(14.3035908047853,14.559719093724,4.90612393202917));
#130846=CARTESIAN_POINT('Ctrl Pts',(14.3038111590203,14.5617621182262,4.90461443947957));
#130847=CARTESIAN_POINT('Ctrl Pts',(14.3040309513857,14.5638127205748,4.90311602720806));
#130848=CARTESIAN_POINT('Ctrl Pts',(14.3040321491743,14.5638238956124,4.90310786140567));
#130849=CARTESIAN_POINT('Ctrl Pts',(14.3040333469478,14.5638350708957,4.90309969591605));
#130850=CARTESIAN_POINT('Ctrl Pts',(14.3040345447063,14.5638462464246,4.90309153073925));
#130851=CARTESIAN_POINT('Ctrl Pts',(14.306629244969,14.5880557571609,4.88540333561519));
#130852=CARTESIAN_POINT('Ctrl Pts',(14.3091535475,14.6134222131576,4.86918317244379));
#130853=CARTESIAN_POINT('Ctrl Pts',(14.3116484096287,14.6397327828386,4.85456421835864));
#130854=CARTESIAN_POINT('Ctrl Pts',(14.3119018982887,14.6424060492192,4.8530788701146));
#130855=CARTESIAN_POINT('Ctrl Pts',(14.3121550830228,14.6450890177863,4.85161004932618));
#130856=CARTESIAN_POINT('Ctrl Pts',(14.3124080067914,14.6477814354157,4.85015789303608));
#130857=CARTESIAN_POINT('Ctrl Pts',(14.3151471500034,14.6769400926496,4.83443116214175));
#130858=CARTESIAN_POINT('Ctrl Pts',(14.3178565197513,14.7072125808724,4.82065887681126));
#130859=CARTESIAN_POINT('Ctrl Pts',(14.3205827364436,14.7382976380876,4.8089675697619));
#130860=CARTESIAN_POINT('Ctrl Pts',(14.3233062437292,14.7693518019183,4.79728788193015));
#130861=CARTESIAN_POINT('Ctrl Pts',(14.3260470428033,14.8012165799276,4.78768458369584));
#130862=CARTESIAN_POINT('Ctrl Pts',(14.3288339245698,14.8335851856984,4.78024081182856));
#130863=CARTESIAN_POINT('Ctrl Pts',(14.3316195658775,14.8659393839971,4.77280035323145));
#130864=CARTESIAN_POINT('Ctrl Pts',(14.3344514718522,14.8987968133817,4.76751722030853));
#130865=CARTESIAN_POINT('Ctrl Pts',(14.3373355482926,14.9318482118683,4.76443694336892));
#130866=CARTESIAN_POINT('Ctrl Pts',(14.3402220634959,14.9649275584783,4.76135406176011));
#130867=CARTESIAN_POINT('Ctrl Pts',(14.3431608765856,14.9982011697976,4.76047767289296));
#130868=CARTESIAN_POINT('Ctrl Pts',(14.3461330712643,15.0313574370878,4.7618186309569));
#130869=CARTESIAN_POINT('Ctrl Pts',(14.3491067426328,15.0645301775666,4.76316025525552));
#130870=CARTESIAN_POINT('Ctrl Pts',(14.3521136607897,15.0975855176736,4.76672157718414));
#130871=CARTESIAN_POINT('Ctrl Pts',(14.3551109360268,15.1302095814376,4.7724783327648));
#130872=CARTESIAN_POINT('Ctrl Pts',(14.3581140312821,15.1628969936191,4.77824626663885));
#130873=CARTESIAN_POINT('Ctrl Pts',(14.3611069637679,15.1951515006022,4.78621869460513));
#130874=CARTESIAN_POINT('Ctrl Pts',(14.3640272845584,15.2266545773731,4.79633101960155));
#130875=CARTESIAN_POINT('Ctrl Pts',(14.3650241516788,15.2374083211149,4.79978291582225));
#130876=CARTESIAN_POINT('Ctrl Pts',(14.366012429098,15.2480744791746,4.8034837759039));
#130877=CARTESIAN_POINT('Ctrl Pts',(14.3669893251901,15.2586403193246,4.80742974171195));
#130878=CARTESIAN_POINT('Ctrl Pts',(14.366990579758,15.2586538883866,4.80743480927438));
#130879=CARTESIAN_POINT('Ctrl Pts',(14.366991834309,15.2586674573113,4.80743987725041));
#130880=CARTESIAN_POINT('Ctrl Pts',(14.3669930888434,15.2586810260987,4.80744494564005));
#130881=CARTESIAN_POINT('Ctrl Pts',(14.3695787610439,15.2866471297844,4.81789120778495));
#130882=CARTESIAN_POINT('Ctrl Pts',(14.372093138749,15.3140323479414,4.83009815532248));
#130883=CARTESIAN_POINT('Ctrl Pts',(14.3745772892216,15.340609796519,4.84396317939131));
#130884=CARTESIAN_POINT('Ctrl Pts',(14.374832750069,15.343342923039,4.84538900718936));
#130885=CARTESIAN_POINT('Ctrl Pts',(14.3750878912543,15.3460674842986,4.84683233036716));
#130886=CARTESIAN_POINT('Ctrl Pts',(14.375342757439,15.348783218757,4.84829300993393));
#130887=CARTESIAN_POINT('Ctrl Pts',(14.3780727997337,15.3778732682692,4.86393932645365));
#130888=CARTESIAN_POINT('Ctrl Pts',(14.3807721227504,15.4059536841026,4.88158174700822));
#130889=CARTESIAN_POINT('Ctrl Pts',(14.3834877411975,15.432753730036,4.90104012195106));
#130890=CARTESIAN_POINT('Ctrl Pts',(14.3862005110504,15.4595256636047,4.92047808570009));
#130891=CARTESIAN_POINT('Ctrl Pts',(14.3889300205994,15.4850200982898,4.94172766113073));
#130892=CARTESIAN_POINT('Ctrl Pts',(14.3917055192335,15.5089994042371,4.96458005592421));
#130893=CARTESIAN_POINT('Ctrl Pts',(14.3944796550394,15.5329669358409,4.98742122971137));
#130894=CARTESIAN_POINT('Ctrl Pts',(14.3972999585682,15.555420971719,5.01186336788663));
#130895=CARTESIAN_POINT('Ctrl Pts',(14.4001728576909,15.576153906496,5.03767480536044));
#130896=CARTESIAN_POINT('Ctrl Pts',(14.4030480836802,15.5969036336391,5.06350714846636));
#130897=CARTESIAN_POINT('Ctrl Pts',(14.4059760321815,15.615929524449,5.09071092442181));
#130898=CARTESIAN_POINT('Ctrl Pts',(14.4089383556134,15.6330516845592,5.11903341319642));
#130899=CARTESIAN_POINT('Ctrl Pts',(14.4119020789529,15.6501819361021,5.14736928635192));
#130900=CARTESIAN_POINT('Ctrl Pts',(14.4149000481656,15.6654065699473,5.17682504842975));
#130901=CARTESIAN_POINT('Ctrl Pts',(14.4178899265822,15.6785738204058,5.20712690092421));
#130902=CARTESIAN_POINT('Ctrl Pts',(14.4208856284582,15.6917667170405,5.23748777307884));
#130903=CARTESIAN_POINT('Ctrl Pts',(14.4238727389467,15.7028938078213,5.26869835220417));
#130904=CARTESIAN_POINT('Ctrl Pts',(14.4267892002207,15.7118343797676,5.30045907912811));
#130905=CARTESIAN_POINT('Ctrl Pts',(14.4278482484995,15.7150809503346,5.3119922832492));
#130906=CARTESIAN_POINT('Ctrl Pts',(14.4288978335193,15.7180395400288,5.32359777545549));
#130907=CARTESIAN_POINT('Ctrl Pts',(14.4299345986302,15.7207056368008,5.33526029301637));
#130908=CARTESIAN_POINT('Ctrl Pts',(14.4299358766582,15.7207089233179,5.33527466948756));
#130909=CARTESIAN_POINT('Ctrl Pts',(14.4299371546687,15.7207122093985,5.33528904607521));
#130910=CARTESIAN_POINT('Ctrl Pts',(14.4299384326618,15.7207154950427,5.33530342277929));
#130911=CARTESIAN_POINT('Ctrl Pts',(14.4325273633362,15.7273714814289,5.36442743691014));
#130912=CARTESIAN_POINT('Ctrl Pts',(14.4350448117096,15.7322344141166,5.39403323947481));
#130913=CARTESIAN_POINT('Ctrl Pts',(14.4375316836577,15.7352656946264,5.42387472832081));
#130914=CARTESIAN_POINT('Ctrl Pts',(14.4377898328919,15.7355803560801,5.42697241797076));
#130915=CARTESIAN_POINT('Ctrl Pts',(14.4380476526519,15.7358753014408,5.43007260585816));
#130916=CARTESIAN_POINT('Ctrl Pts',(14.4383051886924,15.7361505028073,5.4331749885224));
#130917=CARTESIAN_POINT('Ctrl Pts',(14.4410405763686,15.7390735205912,5.46612656798922));
#130918=CARTESIAN_POINT('Ctrl Pts',(14.4437447966235,15.7397669865307,5.4993309370506));
#130919=CARTESIAN_POINT('Ctrl Pts',(14.4464648946848,15.7382331285503,5.53246191912244));
#130920=CARTESIAN_POINT('Ctrl Pts',(14.4491821912515,15.7367008503272,5.56555877879707));
#130921=CARTESIAN_POINT('Ctrl Pts',(14.4519158152569,15.732946388313,5.59858226648247));
#130922=CARTESIAN_POINT('Ctrl Pts',(14.454695072665,15.7270141370407,5.63121826876531));
#130923=CARTESIAN_POINT('Ctrl Pts',(14.457473005414,15.7210847132182,5.66383871596583));
#130924=CARTESIAN_POINT('Ctrl Pts',(14.460296753895,15.7129798930243,5.69607201826397));
#130925=CARTESIAN_POINT('Ctrl Pts',(14.4631727829094,15.7027796686425,5.727616673456));
#130926=CARTESIAN_POINT('Ctrl Pts',(14.4660511555404,15.6925711323083,5.75918703373707));
#130927=CARTESIAN_POINT('Ctrl Pts',(14.468981936248,15.6802638759292,5.79006762672038));
#130928=CARTESIAN_POINT('Ctrl Pts',(14.4719467740945,15.6659706856688,5.819968566145));
#130929=CARTESIAN_POINT('Ctrl Pts',(14.4749130271505,15.6516706728234,5.84988377821943));
#130930=CARTESIAN_POINT('Ctrl Pts',(14.4779132075223,15.6353826794534,5.87881839691178));
#130931=CARTESIAN_POINT('Ctrl Pts',(14.4809049351614,15.6172525632722,5.90649442785779));
#130932=CARTESIAN_POINT('Ctrl Pts',(14.4839024479596,15.5990873885497,5.93422397645728));
#130933=CARTESIAN_POINT('Ctrl Pts',(14.4868910033293,15.5790724690893,5.96068990556623));
#130934=CARTESIAN_POINT('Ctrl Pts',(14.4898084895584,15.5573923142399,5.98562596341381));
#130935=CARTESIAN_POINT('Ctrl Pts',(14.4908357699898,15.5497584825504,5.99440623596856));
#130936=CARTESIAN_POINT('Ctrl Pts',(14.4918541001814,15.5419185708745,6.00299696561843));
#130937=CARTESIAN_POINT('Ctrl Pts',(14.4928604199827,15.5338819616943,6.0113870284288));
#130938=CARTESIAN_POINT('Ctrl Pts',(14.4928616695749,15.5338719822782,6.01139744674406));
#130939=CARTESIAN_POINT('Ctrl Pts',(14.4928629191505,15.5338620025394,6.01140786477173));
#130940=CARTESIAN_POINT('Ctrl Pts',(14.4928641687095,15.5338520224779,6.01141828251177));
#130941=CARTESIAN_POINT('Ctrl Pts',(14.4954536365896,15.5131702878352,6.0330070207212));
#130942=CARTESIAN_POINT('Ctrl Pts',(14.4979719606962,15.4910984741824,6.05336125999676));
#130943=CARTESIAN_POINT('Ctrl Pts',(14.500460108996,15.467821300313,6.07231315241162));
#130944=CARTESIAN_POINT('Ctrl Pts',(14.5007162406014,15.4654251328845,6.074264072552));
#130945=CARTESIAN_POINT('Ctrl Pts',(14.5009720524405,15.46301623774,6.07620012694115));
#130946=CARTESIAN_POINT('Ctrl Pts',(14.5012275892028,15.4605948474988,6.07812112976851));
#130947=CARTESIAN_POINT('Ctrl Pts',(14.5039623658394,15.4346809187121,6.0986798689671));
#130948=CARTESIAN_POINT('Ctrl Pts',(14.5066664734542,15.4073303639171,6.11751573878081));
#130949=CARTESIAN_POINT('Ctrl Pts',(14.5093868373066,15.3788167160486,6.13445131519405));
#130950=CARTESIAN_POINT('Ctrl Pts',(14.5121044090448,15.3503323338847,6.15136950934962));
#130951=CARTESIAN_POINT('Ctrl Pts',(14.5148386837705,15.3206876622895,6.16639169543563));
#130952=CARTESIAN_POINT('Ctrl Pts',(14.5176188159135,15.2901693561779,6.17938224246889));
#130953=CARTESIAN_POINT('Ctrl Pts',(14.5203976335316,15.2596654799822,6.1923666472051));
#130954=CARTESIAN_POINT('Ctrl Pts',(14.5232224896802,15.228288993506,6.20332158140069));
#130955=CARTESIAN_POINT('Ctrl Pts',(14.5260996919465,15.1963356147579,6.21214804855116));
#130956=CARTESIAN_POINT('Ctrl Pts',(14.5289792573594,15.1643559915855,6.22098176518695));
#130957=CARTESIAN_POINT('Ctrl Pts',(14.53191129621,15.1317985810812,6.22768360115573));
#130958=CARTESIAN_POINT('Ctrl Pts',(14.534877310697,15.0989674590039,6.23218832584451));
#130959=CARTESIAN_POINT('Ctrl Pts',(14.5378447518066,15.0661205454935,6.23669521725968));
#130960=CARTESIAN_POINT('Ctrl Pts',(14.540846037674,15.0329995778638,6.23900275407254));
#130961=CARTESIAN_POINT('Ctrl Pts',(14.5438386677894,14.9999169121041,6.23907987489896));
#130962=CARTESIAN_POINT('Ctrl Pts',(14.5468371037384,14.9667700645224,6.23915714534316));
#130963=CARTESIAN_POINT('Ctrl Pts',(14.5498263765233,14.9336615313222,6.23699483779894));
#130964=CARTESIAN_POINT('Ctrl Pts',(14.5527443018251,14.9009151441113,6.23260066238511));
#130965=CARTESIAN_POINT('Ctrl Pts',(14.5537731552654,14.8893688467756,6.23105128670754));
#130966=CARTESIAN_POINT('Ctrl Pts',(14.5547929997385,14.8778676704415,6.22922482656027));
#130967=CARTESIAN_POINT('Ctrl Pts',(14.5558007613404,14.8664261254646,6.22712301133068));
#130968=CARTESIAN_POINT('Ctrl Pts',(14.5558020208007,14.8664118262776,6.22712038456576));
#130969=CARTESIAN_POINT('Ctrl Pts',(14.5558032802441,14.8663975271542,6.22711775736648));
#130970=CARTESIAN_POINT('Ctrl Pts',(14.5558045396706,14.8663832280945,6.2271151297328));
#130971=CARTESIAN_POINT('Ctrl Pts',(14.5583928450922,14.8369965725034,6.2217149588477));
#130972=CARTESIAN_POINT('Ctrl Pts',(14.5609098652777,14.8078758271027,6.21447688966069));
#130973=CARTESIAN_POINT('Ctrl Pts',(14.5633965756876,14.7792625071587,6.20546269975056));
#130974=CARTESIAN_POINT('Ctrl Pts',(14.5636531362126,14.776310394859,6.20453268180936));
#130975=CARTESIAN_POINT('Ctrl Pts',(14.5639093741022,14.7733637133995,6.20358379273608));
#130976=CARTESIAN_POINT('Ctrl Pts',(14.5641653343571,14.7704227475361,6.20261612504836));
#130977=CARTESIAN_POINT('Ctrl Pts',(14.5668990455627,14.7390125923053,6.19228122362686));
#130978=CARTESIAN_POINT('Ctrl Pts',(14.5696019248745,14.7082504869431,6.17980028029817));
#130979=CARTESIAN_POINT('Ctrl Pts',(14.5723209571294,14.6784349284052,6.16530399818331));
#130980=CARTESIAN_POINT('Ctrl Pts',(14.5750371794267,14.6486501824671,6.15082269711056));
#130981=CARTESIAN_POINT('Ctrl Pts',(14.5777700016255,14.6198099352693,6.13433078180673));
#130982=CARTESIAN_POINT('Ctrl Pts',(14.5805486486701,14.5921850016099,6.11599291589402));
#130983=CARTESIAN_POINT('Ctrl Pts',(14.5833259653237,14.5645732945172,6.09766382998459));
#130984=CARTESIAN_POINT('Ctrl Pts',(14.5861492876469,14.5381756402627,6.07749086301158));
#130985=CARTESIAN_POINT('Ctrl Pts',(14.5890250021544,14.5132372397542,6.05566640702311));
#130986=CARTESIAN_POINT('Ctrl Pts',(14.5919030643459,14.488278479964,6.0338241339238));
#130987=CARTESIAN_POINT('Ctrl Pts',(14.594833646003,14.4647813168602,6.01032776578187));
#130988=CARTESIAN_POINT('Ctrl Pts',(14.5977983330731,14.4429673372083,5.98539524459405));
#130989=CARTESIAN_POINT('Ctrl Pts',(14.6007644363182,14.4211429374295,5.96045081361087));
#130990=CARTESIAN_POINT('Ctrl Pts',(14.6037645148987,14.4010033938592,5.93406872166128));
#130991=CARTESIAN_POINT('Ctrl Pts',(14.6067561477313,14.3827462972326,5.90649259827256));
#130992=CARTESIAN_POINT('Ctrl Pts',(14.6097535849123,14.3644537782952,5.87886297185255));
#130993=CARTESIAN_POINT('Ctrl Pts',(14.6127420715505,14.3480513587491,5.85003428955134));
#130994=CARTESIAN_POINT('Ctrl Pts',(14.6156594784949,14.3337105588627,5.82028104282061));
#130995=CARTESIAN_POINT('Ctrl Pts',(14.6166958198584,14.3286163212775,5.80971188984606));
#130996=CARTESIAN_POINT('Ctrl Pts',(14.6177230509408,14.3237819537905,5.79902636994269));
#130997=CARTESIAN_POINT('Ctrl Pts',(14.6187380291237,14.319214131938,5.78823783860755));
#130998=CARTESIAN_POINT('Ctrl Pts',(14.6187392905008,14.3192084552189,5.78822443102196));
#130999=CARTESIAN_POINT('Ctrl Pts',(14.6187405518606,14.3192027789012,5.78821102325586));
#131000=CARTESIAN_POINT('Ctrl Pts',(14.6187418132029,14.3191971029851,5.78819761530927));
#131001=CARTESIAN_POINT('Ctrl Pts',(14.6199525060722,14.3137491045748,5.77532806779205));
#131002=CARTESIAN_POINT('Ctrl Pts',(14.6211471738604,14.3086710787256,5.76229203155521));
#131003=CARTESIAN_POINT('Ctrl Pts',(14.6223301869987,14.3039706982751,5.74911183949278));
#131004=CARTESIAN_POINT('Origin',(13.2437274406976,15.,5.5));
#131005=CARTESIAN_POINT('',(15.1006177988695,14.3042076755364,5.74898602614905));
#131006=CARTESIAN_POINT('',(15.0214324762185,14.3044236561645,5.74887185968306));
#131007=CARTESIAN_POINT('',(13.2437274406976,14.3042076641721,5.74898599439144));
#131008=CARTESIAN_POINT('Ctrl Pts',(15.1006178015771,14.3042076756101,5.74898602635499));
#131009=CARTESIAN_POINT('Ctrl Pts',(15.0992510192417,14.3099072116453,5.76491339980638));
#131010=CARTESIAN_POINT('Ctrl Pts',(15.0978904180461,14.3161552982477,5.78064972156567));
#131011=CARTESIAN_POINT('Ctrl Pts',(15.093390819992,14.3385505614446,5.83184683983702));
#131012=CARTESIAN_POINT('Ctrl Pts',(15.0902464920784,14.3569524182242,5.8662334633876));
#131013=CARTESIAN_POINT('Ctrl Pts',(15.0858797728196,14.3853466982996,5.91049808107278));
#131014=CARTESIAN_POINT('Ctrl Pts',(15.0847366692995,14.3930338554862,5.92178123176599));
#131015=CARTESIAN_POINT('Ctrl Pts',(15.0828203115642,14.4063039757117,5.9401444676008));
#131016=CARTESIAN_POINT('Ctrl Pts',(15.082053692695,14.4117121382454,5.94734717856612));
#131017=CARTESIAN_POINT('Ctrl Pts',(15.0805099531525,14.4227906268988,5.96155336360282));
#131018=CARTESIAN_POINT('Ctrl Pts',(15.0797329617558,14.4284600943739,5.9685555340117));
#131019=CARTESIAN_POINT('Ctrl Pts',(15.0777644185759,14.4430479769367,5.98591377213543));
#131020=CARTESIAN_POINT('Ctrl Pts',(15.0765665553399,14.4521278952372,5.99612886703441));
#131021=CARTESIAN_POINT('Ctrl Pts',(15.0716718426609,14.4900118650182,6.03644038352152));
#131022=CARTESIAN_POINT('Ctrl Pts',(15.0678855158728,14.5210490774347,6.06432354481301));
#131023=CARTESIAN_POINT('Ctrl Pts',(15.0612003791751,14.5791218903357,6.10823837756831));
#131024=CARTESIAN_POINT('Ctrl Pts',(15.0583260855716,14.6051452695217,6.12544557981788));
#131025=CARTESIAN_POINT('Ctrl Pts',(15.053961666409,14.6467939978574,6.14934620534783));
#131026=CARTESIAN_POINT('Ctrl Pts',(15.0524437184848,14.6616940170464,6.1572321888255));
#131027=CARTESIAN_POINT('Ctrl Pts',(15.0504128388405,14.6823065920435,6.16725458701378));
#131028=CARTESIAN_POINT('Ctrl Pts',(15.0498786775349,14.6877938167225,6.16983960168206));
#131029=CARTESIAN_POINT('Ctrl Pts',(15.048915078788,14.697820390212,6.17441310211501));
#131030=CARTESIAN_POINT('Ctrl Pts',(15.0484844380467,14.702349016998,6.17642401488885));
#131031=CARTESIAN_POINT('Ctrl Pts',(15.04755263282,14.7122550908629,6.18070399108053));
#131032=CARTESIAN_POINT('Ctrl Pts',(15.0470524775739,14.7176397343954,6.18295515495054));
#131033=CARTESIAN_POINT('Ctrl Pts',(15.0455391195859,14.7341209558929,6.1896172177964));
#131034=CARTESIAN_POINT('Ctrl Pts',(15.0445366597996,14.7452989279717,6.19382345416604));
#131035=CARTESIAN_POINT('Ctrl Pts',(15.0427771264441,14.7652920474885,6.20079841242744));
#131036=CARTESIAN_POINT('Ctrl Pts',(15.0420161564255,14.7740658742122,6.20367607948708));
#131037=CARTESIAN_POINT('Ctrl Pts',(15.0382466569616,14.8180405759767,6.21719168559805));
#131038=CARTESIAN_POINT('Ctrl Pts',(15.0353073111224,14.853948845698,6.22535684117382));
#131039=CARTESIAN_POINT('Ctrl Pts',(15.0292970284429,14.9276752155475,6.23642185235241));
#131040=CARTESIAN_POINT('Ctrl Pts',(15.0262329249709,14.9654027549854,6.23915523361877));
#131041=CARTESIAN_POINT('Ctrl Pts',(15.0220803935836,15.0151755727269,6.23894169353115));
#131042=CARTESIAN_POINT('Ctrl Pts',(15.0210710440379,15.0271768690993,6.23859766360036));
#131043=CARTESIAN_POINT('Ctrl Pts',(15.0193116929085,15.0478880541387,6.23749851625121));
#131044=CARTESIAN_POINT('Ctrl Pts',(15.0185660325591,15.0566030089313,6.2368808673125));
#131045=CARTESIAN_POINT('Ctrl Pts',(15.0170042035901,15.074712021765,6.23527430959483));
#131046=CARTESIAN_POINT('Ctrl Pts',(15.0161873673796,15.0841021043392,6.23425950078802));
#131047=CARTESIAN_POINT('Ctrl Pts',(15.0139680421021,15.1093804572255,6.2310363763011));
#131048=CARTESIAN_POINT('Ctrl Pts',(15.0125555061944,15.1252195258054,6.22849039262709));
#131049=CARTESIAN_POINT('Ctrl Pts',(15.0092925418075,15.1612085404964,6.22149719907432));
#131050=CARTESIAN_POINT('Ctrl Pts',(15.0074337210017,15.1812796098589,6.21671748540461));
#131051=CARTESIAN_POINT('Ctrl Pts',(15.0011466615815,15.2477916384619,6.19790580054746));
#131052=CARTESIAN_POINT('Ctrl Pts',(14.9966477496338,15.293045151734,6.18014518120771));
#131053=CARTESIAN_POINT('Ctrl Pts',(14.9907704098767,15.3506817466176,6.15069703538824));
#131054=CARTESIAN_POINT('Ctrl Pts',(14.9893100632424,15.3648863762643,6.14283929197273));
#131055=CARTESIAN_POINT('Ctrl Pts',(14.9873428381708,15.3839576946009,6.13145329586703));
#131056=CARTESIAN_POINT('Ctrl Pts',(14.9868162700791,15.3890562119405,6.12832479442541));
#131057=CARTESIAN_POINT('Ctrl Pts',(14.9858615664064,15.398295630209,6.12249979814702));
#131058=CARTESIAN_POINT('Ctrl Pts',(14.9854323194997,15.4024484581214,6.11982308186187));
#131059=CARTESIAN_POINT('Ctrl Pts',(14.984496571616,15.4115006876899,6.11385909198455));
#131060=CARTESIAN_POINT('Ctrl Pts',(14.9839911754329,15.4163880697629,6.11055448848179));
#131061=CARTESIAN_POINT('Ctrl Pts',(14.982442271807,15.431343765723,6.10017906118955));
#131062=CARTESIAN_POINT('Ctrl Pts',(14.9814102569868,15.4412761239467,6.09291465206659));
#131063=CARTESIAN_POINT('Ctrl Pts',(14.9795878417004,15.4586660316979,6.07951665669839));
#131064=CARTESIAN_POINT('Ctrl Pts',(14.9787935703072,15.4661931091757,6.07347893334562));
#131065=CARTESIAN_POINT('Ctrl Pts',(14.9747267846272,15.5043410016406,6.04163158898095));
#131066=CARTESIAN_POINT('Ctrl Pts',(14.971533592717,15.532946586586,6.01351039144344));
#131067=CARTESIAN_POINT('Ctrl Pts',(14.9655705428336,15.5812245369672,5.95764662982539));
#131068=CARTESIAN_POINT('Ctrl Pts',(14.9628201953718,15.6015336224318,5.93060333829186));
#131069=CARTESIAN_POINT('Ctrl Pts',(14.9590079457786,15.6263988334279,5.89228452967835));
#131070=CARTESIAN_POINT('Ctrl Pts',(14.9580070100405,15.632634900863,5.88214617647201));
#131071=CARTESIAN_POINT('Ctrl Pts',(14.9562572898702,15.643012038641,5.86432484568326));
#131072=CARTESIAN_POINT('Ctrl Pts',(14.9555127098893,15.647266975387,5.85671070026271));
#131073=CARTESIAN_POINT('Ctrl Pts',(14.9539483345668,15.6558656316758,5.84066293815921));
#131074=CARTESIAN_POINT('Ctrl Pts',(14.953127808438,15.6601836813751,5.83221747811366));
#131075=CARTESIAN_POINT('Ctrl Pts',(14.9508851247262,15.6714602597545,5.8090736727205));
#131076=CARTESIAN_POINT('Ctrl Pts',(14.9494525407782,15.6780976678559,5.79422589767985));
#131077=CARTESIAN_POINT('Ctrl Pts',(14.9461312656242,15.6921881055925,5.75969085902998));
#131078=CARTESIAN_POINT('Ctrl Pts',(14.9442337026044,15.6993003008116,5.73988048365984));
#131079=CARTESIAN_POINT('Ctrl Pts',(14.9390407927451,15.7162696363072,5.68540785215006));
#131080=CARTESIAN_POINT('Ctrl Pts',(14.9357166858559,15.7244533880979,5.65028415998758));
#131081=CARTESIAN_POINT('Ctrl Pts',(14.9300516487741,15.7340472126008,5.58922461006446));
#131082=CARTESIAN_POINT('Ctrl Pts',(14.9277039454842,15.7367145526301,5.56354777485325));
#131083=CARTESIAN_POINT('Ctrl Pts',(14.924738245076,15.7384195392994,5.53024193681021));
#131084=CARTESIAN_POINT('Ctrl Pts',(14.9240716807826,15.7386899669246,5.52269664285404));
#131085=CARTESIAN_POINT('Ctrl Pts',(14.9229775170635,15.7389462435518,5.51019679462352));
#131086=CARTESIAN_POINT('Ctrl Pts',(14.9225466509125,15.7389979899954,5.50524434465818));
#131087=CARTESIAN_POINT('Ctrl Pts',(14.9216294637016,15.739002173277,5.49463281922514));
#131088=CARTESIAN_POINT('Ctrl Pts',(14.9211439399876,15.7389394133532,5.48897418326743));
#131089=CARTESIAN_POINT('Ctrl Pts',(14.9197266671525,15.7385640535688,5.47235172032866));
#131090=CARTESIAN_POINT('Ctrl Pts',(14.9188037579985,15.7380723662661,5.46139288454181));
#131091=CARTESIAN_POINT('Ctrl Pts',(14.9172097835843,15.7367896290749,5.44230559996862));
#131092=CARTESIAN_POINT('Ctrl Pts',(14.9165348536471,15.7361075475423,5.43417225694721));
#131093=CARTESIAN_POINT('Ctrl Pts',(14.9134330119992,15.732332784988,5.39663871326985));
#131094=CARTESIAN_POINT('Ctrl Pts',(14.9110545810954,15.7276123261766,5.36742765655907));
#131095=CARTESIAN_POINT('Ctrl Pts',(14.9051455899846,15.7115780966835,5.29579546764514));
#131096=CARTESIAN_POINT('Ctrl Pts',(14.9016211370708,15.6982155625316,5.25395679469438));
#131097=CARTESIAN_POINT('Ctrl Pts',(14.8968449257441,15.6759171420462,5.20092713878095));
#131098=CARTESIAN_POINT('Ctrl Pts',(14.895698249951,15.6702591044545,5.18845346430624));
#131099=CARTESIAN_POINT('Ctrl Pts',(14.8937776356104,15.6603076549552,5.16804207528852));
#131100=CARTESIAN_POINT('Ctrl Pts',(14.8930103972369,15.6562094111272,5.16001256416301));
#131101=CARTESIAN_POINT('Ctrl Pts',(14.891466742981,15.6477273766923,5.14411901902167));
#131102=CARTESIAN_POINT('Ctrl Pts',(14.8906904739429,15.6433447131643,5.13625614568605));
#131103=CARTESIAN_POINT('Ctrl Pts',(14.8887265447247,15.631971503005,5.1167004122829));
#131104=CARTESIAN_POINT('Ctrl Pts',(14.8875326364623,15.6247995277899,5.10511767440195));
#131105=CARTESIAN_POINT('Ctrl Pts',(14.8829024114174,15.5960280780468,5.06139939738936));
#131106=CARTESIAN_POINT('Ctrl Pts',(14.8793905681541,15.5722390326687,5.03078628246848));
#131107=CARTESIAN_POINT('Ctrl Pts',(14.8714493562617,15.5139144050625,4.96679721108965));
#131108=CARTESIAN_POINT('Ctrl Pts',(14.8670153539851,15.4782980048915,4.93462846425949));
#131109=CARTESIAN_POINT('Ctrl Pts',(14.8620152896383,15.4332247839639,4.90124747843356));
#131110=CARTESIAN_POINT('Ctrl Pts',(14.8612894015299,15.4265511590456,4.89647500314726));
#131111=CARTESIAN_POINT('Ctrl Pts',(14.8601659878828,15.4160034152996,4.88919444258697));
#131112=CARTESIAN_POINT('Ctrl Pts',(14.8597638784543,15.4121832036215,4.88661000914633));
#131113=CARTESIAN_POINT('Ctrl Pts',(14.8589076036269,15.4039478996683,4.88115038249094));
#131114=CARTESIAN_POINT('Ctrl Pts',(14.8584541901416,15.3995257025552,4.87828626110608));
#131115=CARTESIAN_POINT('Ctrl Pts',(14.857235676925,15.3874850252007,4.87066942366231));
#131116=CARTESIAN_POINT('Ctrl Pts',(14.8564760283747,15.3798096278646,4.86600765919918));
#131117=CARTESIAN_POINT('Ctrl Pts',(14.8532053519795,15.346111501072,4.84637234661793));
#131118=CARTESIAN_POINT('Ctrl Pts',(14.8507639365229,15.3192719560999,4.8328507165758));
#131119=CARTESIAN_POINT('Ctrl Pts',(14.8436848422111,15.238730209886,4.79825214950862));
#131120=CARTESIAN_POINT('Ctrl Pts',(14.8391010405225,15.1833068241211,4.78178001955737));
#131121=CARTESIAN_POINT('Ctrl Pts',(14.8332617275527,15.1142502652122,4.76977855293323));
#131122=CARTESIAN_POINT('Ctrl Pts',(14.8322146395045,15.1019137678445,4.76795489789314));
#131123=CARTESIAN_POINT('Ctrl Pts',(14.8304190098092,15.0808828638724,4.76538786728927));
#131124=CARTESIAN_POINT('Ctrl Pts',(14.8296755231385,15.0722103624063,4.76448475684657));
#131125=CARTESIAN_POINT('Ctrl Pts',(14.8281321975413,15.0542953182335,4.7629390618583));
#131126=CARTESIAN_POINT('Ctrl Pts',(14.8273318797121,15.0450526610542,4.762316430449));
#131127=CARTESIAN_POINT('Ctrl Pts',(14.8252163923668,15.0207618563589,4.76113826802042));
#131128=CARTESIAN_POINT('Ctrl Pts',(14.8238927955329,15.0057050106242,4.76086868905633));
#131129=CARTESIAN_POINT('Ctrl Pts',(14.8216616481105,14.9805807351554,4.76118653886527));
#131130=CARTESIAN_POINT('Ctrl Pts',(14.8207616595112,14.9705140477882,4.76151980568802));
#131131=CARTESIAN_POINT('Ctrl Pts',(14.8170055679276,14.9287816844488,4.76375601331087));
#131132=CARTESIAN_POINT('Ctrl Pts',(14.8141056028554,14.8972509648339,4.76749095783466));
#131133=CARTESIAN_POINT('Ctrl Pts',(14.8074490882703,14.8260082037432,4.78062071078683));
#131134=CARTESIAN_POINT('Ctrl Pts',(14.8036925335516,14.7866306668265,4.79130130157021));
#131135=CARTESIAN_POINT('Ctrl Pts',(14.7992634750848,14.7400177224675,4.80818471390117));
#131136=CARTESIAN_POINT('Ctrl Pts',(14.7984796360593,14.7317587105458,4.81134492898591));
#131137=CARTESIAN_POINT('Ctrl Pts',(14.7972435464586,14.7186978911827,4.81661315076737));
#131138=CARTESIAN_POINT('Ctrl Pts',(14.7967863301209,14.7138586603227,4.81862521212996));
#131139=CARTESIAN_POINT('Ctrl Pts',(14.7958741744206,14.7041819487624,4.82276988969222));
#131140=CARTESIAN_POINT('Ctrl Pts',(14.7954193076996,14.6993451344094,4.82490326694368));
#131141=CARTESIAN_POINT('Ctrl Pts',(14.7941920506198,14.6862763713661,4.83083583997955));
#131142=CARTESIAN_POINT('Ctrl Pts',(14.7934252455913,14.6780904203679,4.83473506488145));
#131143=CARTESIAN_POINT('Ctrl Pts',(14.7900854204252,14.6424452533595,4.85252607832617));
#131144=CARTESIAN_POINT('Ctrl Pts',(14.7875854670921,14.6157942225327,4.86797603600287));
#131145=CARTESIAN_POINT('Ctrl Pts',(14.7805574299694,14.5433417190661,4.91625987728089));
#131146=CARTESIAN_POINT('Ctrl Pts',(14.7760759011876,14.5002268733635,4.95272007232085));
#131147=CARTESIAN_POINT('Ctrl Pts',(14.7703358473794,14.4529976668205,5.00293896231947));
#131148=CARTESIAN_POINT('Ctrl Pts',(14.7692734165035,14.4445646180919,5.01238055271503));
#131149=CARTESIAN_POINT('Ctrl Pts',(14.7674598890912,14.4307200842893,5.02870612011047));
#131150=CARTESIAN_POINT('Ctrl Pts',(14.7667141064142,14.4251807116233,5.03547840158619));
#131151=CARTESIAN_POINT('Ctrl Pts',(14.7651733044624,14.4140597555829,5.04957814663552));
#131152=CARTESIAN_POINT('Ctrl Pts',(14.7643779002494,14.4084923603415,5.05691478079476));
#131153=CARTESIAN_POINT('Ctrl Pts',(14.762293224762,14.3943593622559,5.07628023475415));
#131154=CARTESIAN_POINT('Ctrl Pts',(14.760995986419,14.3860150780933,5.08846449791527));
#131155=CARTESIAN_POINT('Ctrl Pts',(14.7561136104232,14.3562991326642,5.13477266536349));
#131156=CARTESIAN_POINT('Ctrl Pts',(14.7524493425166,14.3373649994363,5.17037038815118));
#131157=CARTESIAN_POINT('Ctrl Pts',(14.7447968048354,14.3043652520063,5.24688155283492));
#131158=CARTESIAN_POINT('Ctrl Pts',(14.7408178834751,14.2907947303222,5.28785574283835));
#131159=CARTESIAN_POINT('Ctrl Pts',(14.736192517651,14.2788643549322,5.33825866313483));
#131160=CARTESIAN_POINT('Ctrl Pts',(14.7354205617058,14.2770078333285,5.34677067440099));
#131161=CARTESIAN_POINT('Ctrl Pts',(14.7341985789747,14.2742812896801,5.36042729313339));
#131162=CARTESIAN_POINT('Ctrl Pts',(14.7337437689779,14.2733145257646,5.36555144270778));
#131163=CARTESIAN_POINT('Ctrl Pts',(14.7328315984357,14.2714720138729,5.37591849172053));
#131164=CARTESIAN_POINT('Ctrl Pts',(14.7323743675612,14.270598430403,5.38116144121119));
#131165=CARTESIAN_POINT('Ctrl Pts',(14.7311327947591,14.2683660998827,5.39551253755506));
#131166=CARTESIAN_POINT('Ctrl Pts',(14.7303542612193,14.2671208402391,5.40463776989514));
#131167=CARTESIAN_POINT('Ctrl Pts',(14.7268976941268,14.2623081944379,5.44560789898914));
#131168=CARTESIAN_POINT('Ctrl Pts',(14.7242987576568,14.2606431863995,5.47764505514616));
#131169=CARTESIAN_POINT('Ctrl Pts',(14.7173492325736,14.2617732229955,5.56379314414781));
#131170=CARTESIAN_POINT('Ctrl Pts',(14.713034583888,14.2684215434994,5.61764566060312));
#131171=CARTESIAN_POINT('Ctrl Pts',(14.7074566166424,14.2838714680731,5.68288972529384));
#131172=CARTESIAN_POINT('Ctrl Pts',(14.7063703933084,14.2871863070076,5.69541065369431));
#131173=CARTESIAN_POINT('Ctrl Pts',(14.7045289722822,14.2933021330107,5.71627876396466));
#131174=CARTESIAN_POINT('Ctrl Pts',(14.7037794966573,14.2959264866741,5.72467499328519));
#131175=CARTESIAN_POINT('Ctrl Pts',(14.7025423363583,14.3004750904483,5.73836441285612));
#131176=CARTESIAN_POINT('Ctrl Pts',(14.7020575832709,14.3023111167124,5.74368608509744));
#131177=CARTESIAN_POINT('Ctrl Pts',(14.7015708502323,14.3042076642463,5.74898599459905));
#131178=CARTESIAN_POINT('',(14.643302331303,14.2612458317818,5.50031209173545));
#131179=CARTESIAN_POINT('Ctrl Pts',(14.6223301870619,14.3039706980243,5.74911183878948));
#131180=CARTESIAN_POINT('Ctrl Pts',(14.6250909116188,14.2930017110506,5.71835404013125));
#131181=CARTESIAN_POINT('Ctrl Pts',(14.6277888702942,14.2840924867556,5.68681257433633));
#131182=CARTESIAN_POINT('Ctrl Pts',(14.6304768935317,14.2773101411995,5.65476687587751));
#131183=CARTESIAN_POINT('Ctrl Pts',(14.6307891739804,14.2765222038469,5.65104397461897));
#131184=CARTESIAN_POINT('Ctrl Pts',(14.6311013203347,14.2757629754969,5.64731432574451));
#131185=CARTESIAN_POINT('Ctrl Pts',(14.6314134154308,14.2750325620636,5.64357841300164));
#131186=CARTESIAN_POINT('Ctrl Pts',(14.6343937879807,14.2680574311685,5.60790206970437));
#131187=CARTESIAN_POINT('Ctrl Pts',(14.6373704162079,14.2637087182105,5.57164788306008));
#131188=CARTESIAN_POINT('Ctrl Pts',(14.6403957909006,14.2620332555201,5.53519586439941));
#131189=CARTESIAN_POINT('Ctrl Pts',(14.6413595316584,14.2614995326438,5.52358398168926));
#131190=CARTESIAN_POINT('Ctrl Pts',(14.6423280172788,14.2612367984457,5.51195198761351));
#131191=CARTESIAN_POINT('Ctrl Pts',(14.643302331268,14.2612458317815,5.50031209215397));
#131192=CARTESIAN_POINT('Ctrl Pts',(14.6433023313447,14.2612458317821,5.50031209123629));
#131193=CARTESIAN_POINT('Ctrl Pts',(14.6461222215263,14.2612719763879,5.46662353982884));
#131194=CARTESIAN_POINT('Ctrl Pts',(14.6489879456295,14.2635801106923,5.4329480764385));
#131195=CARTESIAN_POINT('Ctrl Pts',(14.651906822104,14.268136916162,5.3996050731548));
#131196=CARTESIAN_POINT('Ctrl Pts',(14.6548299420279,14.272700346295,5.36621359596372));
#131197=CARTESIAN_POINT('Ctrl Pts',(14.6578064047676,14.2795188773573,5.3331554877905));
#131198=CARTESIAN_POINT('Ctrl Pts',(14.6608172228768,14.2885259866646,5.30074347405539));
#131199=CARTESIAN_POINT('Ctrl Pts',(14.6638305628729,14.2975406404034,5.26830431174162));
#131200=CARTESIAN_POINT('Ctrl Pts',(14.666878138236,14.3087477111867,5.23651223112942));
#131201=CARTESIAN_POINT('Ctrl Pts',(14.669915552554,14.3220470860818,5.20567390799831));
#131202=CARTESIAN_POINT('Ctrl Pts',(14.6729599034648,14.3353768329773,5.17476515888329));
#131203=CARTESIAN_POINT('Ctrl Pts',(14.6759935383719,14.3508090333046,5.14481454070596));
#131204=CARTESIAN_POINT('Ctrl Pts',(14.6789512632767,14.3682037596851,5.11612483749924));
#131205=CARTESIAN_POINT('Ctrl Pts',(14.6798666873083,14.3735874755691,5.10724529507469));
#131206=CARTESIAN_POINT('Ctrl Pts',(14.6807747262521,14.3791588651593,5.09848649185438));
#131207=CARTESIAN_POINT('Ctrl Pts',(14.6816732068274,14.384912854012,5.08985725627272));
#131208=CARTESIAN_POINT('Ctrl Pts',(14.6816744645226,14.3849209084587,5.08984517704912));
#131209=CARTESIAN_POINT('Ctrl Pts',(14.6816757222009,14.3849289632781,5.0898330980551));
#131210=CARTESIAN_POINT('Ctrl Pts',(14.6816769798624,14.3849370184703,5.08982101929069));
#131211=CARTESIAN_POINT('Ctrl Pts',(14.6842658152184,14.4015182417089,5.06495746740496));
#131212=CARTESIAN_POINT('Ctrl Pts',(14.6867833984792,14.4196830520397,5.04106536422739));
#131213=CARTESIAN_POINT('Ctrl Pts',(14.6892706941656,14.4392791137363,5.01834216308987));
#131214=CARTESIAN_POINT('Ctrl Pts',(14.6895272679287,14.4413005200847,5.01599818072507));
#131215=CARTESIAN_POINT('Ctrl Pts',(14.6897835194112,14.4433371121714,5.01366664954593));
#131216=CARTESIAN_POINT('Ctrl Pts',(14.6900394935768,14.4453886924276,5.01134779444572));
#131217=CARTESIAN_POINT('Ctrl Pts',(14.6927738171437,14.4673037330717,4.98657771605502));
#131218=CARTESIAN_POINT('Ctrl Pts',(14.6954773345768,14.4909342492166,4.96325204878176));
#131219=CARTESIAN_POINT('Ctrl Pts',(14.6981970141438,14.5160420502934,4.94159332122161));
#131220=CARTESIAN_POINT('Ctrl Pts',(14.7009138917455,14.5411239839168,4.91995690768748));
#131221=CARTESIAN_POINT('Ctrl Pts',(14.7036473786631,14.5676796812181,4.89998369340697));
#131222=CARTESIAN_POINT('Ctrl Pts',(14.7064266813217,14.5954507124083,4.88185734650776));
#131223=CARTESIAN_POINT('Ctrl Pts',(14.7092046604926,14.6232085191957,4.86373963126901));
#131224=CARTESIAN_POINT('Ctrl Pts',(14.7120286365145,14.6521802637181,4.84746681569434));
#131225=CARTESIAN_POINT('Ctrl Pts',(14.7149049737545,14.6820921812796,4.83318807667209));
#131226=CARTESIAN_POINT('Ctrl Pts',(14.717783664302,14.7120285716119,4.81889765533942));
#131227=CARTESIAN_POINT('Ctrl Pts',(14.7207148433939,14.7429066065502,4.80660450113035));
#131228=CARTESIAN_POINT('Ctrl Pts',(14.7236800711917,14.7744383906408,4.79642600147313));
#131229=CARTESIAN_POINT('Ctrl Pts',(14.7266467191728,14.8059852767468,4.78624262686631));
#131230=CARTESIAN_POINT('Ctrl Pts',(14.729647285496,14.8381866381599,4.77817604580261));
#131231=CARTESIAN_POINT('Ctrl Pts',(14.7326393224649,14.870740464133,4.77231145050326));
#131232=CARTESIAN_POINT('Ctrl Pts',(14.7356371621703,14.9033574247787,4.76643548144697));
#131233=CARTESIAN_POINT('Ctrl Pts',(14.7386259667064,14.9363284394209,4.76277051413231));
#131234=CARTESIAN_POINT('Ctrl Pts',(14.7415435871632,14.9693334407004,4.76136558621512));
#131235=CARTESIAN_POINT('Ctrl Pts',(14.7425759365491,14.9810116878562,4.7608684768433));
#131236=CARTESIAN_POINT('Ctrl Pts',(14.7435992340124,14.992694024955,4.7606539473331));
#131237=CARTESIAN_POINT('Ctrl Pts',(14.7446103736317,15.004365714554,4.76072284074558));
#131238=CARTESIAN_POINT('Ctrl Pts',(14.7446116328997,15.0043802504156,4.76072292654508));
#131239=CARTESIAN_POINT('Ctrl Pts',(14.7446128921509,15.0043947862905,4.76072301278323));
#131240=CARTESIAN_POINT('Ctrl Pts',(14.7446141513852,15.0044093221786,4.76072309946007));
#131241=CARTESIAN_POINT('Ctrl Pts',(14.7472028424028,15.0342917063171,4.76090128674805));
#131242=CARTESIAN_POINT('Ctrl Pts',(14.749720259795,15.0642334838074,4.76293605499652));
#131243=CARTESIAN_POINT('Ctrl Pts',(14.7522073680622,15.0939860074293,4.76680875635777));
#131244=CARTESIAN_POINT('Ctrl Pts',(14.7524640214252,15.0970562739498,4.76720839389724));
#131245=CARTESIAN_POINT('Ctrl Pts',(14.7527203520295,15.1001244899583,4.76762757411392));
#131246=CARTESIAN_POINT('Ctrl Pts',(14.7529764048909,15.1031903586769,4.76806625561962));
#131247=CARTESIAN_POINT('Ctrl Pts',(14.7557106121156,15.1359286001261,4.772750624838));
#131248=CARTESIAN_POINT('Ctrl Pts',(14.7584139868398,15.1684037434545,4.77966192216373));
#131249=CARTESIAN_POINT('Ctrl Pts',(14.76113350607,15.2002989631679,4.78872357659478));
#131250=CARTESIAN_POINT('Ctrl Pts',(14.7638502211033,15.2321612945413,4.797775887219));
#131251=CARTESIAN_POINT('Ctrl Pts',(14.7665835278909,15.2634448910942,4.80897355353244));
#131252=CARTESIAN_POINT('Ctrl Pts',(14.7693626433398,15.2938542563831,4.82220172931195));
#131253=CARTESIAN_POINT('Ctrl Pts',(14.7721404332908,15.3242491179393,4.83542359591917));
#131254=CARTESIAN_POINT('Ctrl Pts',(14.7749642129968,15.3537706252292,4.85067372086793));
#131255=CARTESIAN_POINT('Ctrl Pts',(14.7778403583777,15.3821436590195,4.86780548236156));
#131256=CARTESIAN_POINT('Ctrl Pts',(14.7807188549676,15.4105398873713,4.88495124883253));
#131257=CARTESIAN_POINT('Ctrl Pts',(14.7836498445575,15.4377857881248,4.90398163250348));
#131258=CARTESIAN_POINT('Ctrl Pts',(14.7866148992793,15.4636250257334,4.92472072884242));
#131259=CARTESIAN_POINT('Ctrl Pts',(14.7895813727922,15.4894766275264,4.9454697489265));
#131260=CARTESIAN_POINT('Ctrl Pts',(14.7925817811825,15.5139201802209,4.96792926253701));
#131261=CARTESIAN_POINT('Ctrl Pts',(14.795573687835,15.536718479835,4.99189387462251));
#131262=CARTESIAN_POINT('Ctrl Pts',(14.7985713967506,15.5595609926378,5.01590496174929));
#131263=CARTESIAN_POINT('Ctrl Pts',(14.8015600984603,15.5807515967063,5.0414274316669));
#131264=CARTESIAN_POINT('Ctrl Pts',(14.8044776515932,15.600073358392,5.06822093313735));
#131265=CARTESIAN_POINT('Ctrl Pts',(14.8055108580628,15.6069158624593,5.07770943867687));
#131266=CARTESIAN_POINT('Ctrl Pts',(14.8065350015697,15.6135242123974,5.08735700333458));
#131267=CARTESIAN_POINT('Ctrl Pts',(14.8075469683162,15.6198895788537,5.09715175176511));
#131268=CARTESIAN_POINT('Ctrl Pts',(14.8075482276661,15.6198975002832,5.09716394091554));
#131269=CARTESIAN_POINT('Ctrl Pts',(14.807549486999,15.6199054213535,5.09717613031826));
#131270=CARTESIAN_POINT('Ctrl Pts',(14.8075507463151,15.6199133420647,5.09718831997327));
#131271=CARTESIAN_POINT('Ctrl Pts',(14.8101395146416,15.6361958990002,5.12224651832175));
#131272=CARTESIAN_POINT('Ctrl Pts',(14.8126570102922,15.6509602865276,5.14837519478572));
#131273=CARTESIAN_POINT('Ctrl Pts',(14.8151441952392,15.6640853653416,5.17535639746759));
#131274=CARTESIAN_POINT('Ctrl Pts',(14.8154008763878,15.6654398927999,5.17814089730997));
#131275=CARTESIAN_POINT('Ctrl Pts',(14.8156572347108,15.6667769658503,5.18093443154027));
#131276=CARTESIAN_POINT('Ctrl Pts',(14.8159133152318,15.6680964558547,5.18373672943679));
#131277=CARTESIAN_POINT('Ctrl Pts',(14.8186476274682,15.682185374649,5.21365840172559));
#131278=CARTESIAN_POINT('Ctrl Pts',(14.8213511049492,15.6942694172094,5.24458482483895));
#131279=CARTESIAN_POINT('Ctrl Pts',(14.8240707235769,15.7042383377209,5.27620924200535));
#131280=CARTESIAN_POINT('Ctrl Pts',(14.8267875391592,15.7141969835058,5.30780106464581));
#131281=CARTESIAN_POINT('Ctrl Pts',(14.8295209432087,15.7220453368245,5.34008912491049));
#131282=CARTESIAN_POINT('Ctrl Pts',(14.8323001516207,15.7277168506456,5.37276343803394));
#131283=CARTESIAN_POINT('Ctrl Pts',(14.8350780355032,15.7333856615076,5.40542217906488));
#131284=CARTESIAN_POINT('Ctrl Pts',(14.8379019049028,15.7368799939699,5.43846666805591));
#131285=CARTESIAN_POINT('Ctrl Pts',(14.8407781342237,15.7381710464651,5.47158647040787));
#131286=CARTESIAN_POINT('Ctrl Pts',(14.8436567153987,15.7394631546366,5.50473335437838));
#131287=CARTESIAN_POINT('Ctrl Pts',(14.8465877838303,15.738548472643,5.5379556420415));
#131288=CARTESIAN_POINT('Ctrl Pts',(14.8495529094249,15.7354329855916,5.5709424875009));
#131289=CARTESIAN_POINT('Ctrl Pts',(14.852519454302,15.7323160072859,5.60394512239376));
#131290=CARTESIAN_POINT('Ctrl Pts',(14.855519926056,15.7269959735091,5.63671213662848));
#131291=CARTESIAN_POINT('Ctrl Pts',(14.8585118853793,15.7195140212916,5.66893244798056));
#131292=CARTESIAN_POINT('Ctrl Pts',(14.8615096464463,15.7120175607319,5.70121523811967));
#131293=CARTESIAN_POINT('Ctrl Pts',(14.8644983894872,15.7023502733526,5.73294922160899));
#131294=CARTESIAN_POINT('Ctrl Pts',(14.8674159709196,15.6905936409715,5.76382102498956));
#131295=CARTESIAN_POINT('Ctrl Pts',(14.8684485235098,15.6864328860796,5.77474677334788));
#131296=CARTESIAN_POINT('Ctrl Pts',(14.8694720231491,15.6820108469657,5.78556452871274));
#131297=CARTESIAN_POINT('Ctrl Pts',(14.8704833620264,15.6773325782012,5.79626041244684));
#131298=CARTESIAN_POINT('Ctrl Pts',(14.8704846209158,15.6773267548089,5.79627372641619));
#131299=CARTESIAN_POINT('Ctrl Pts',(14.8704858797884,15.6773209310087,5.7962870402244));
#131300=CARTESIAN_POINT('Ctrl Pts',(14.8704871386441,15.6773151068005,5.79630035387143));
#131301=CARTESIAN_POINT('Ctrl Pts',(14.8730759013494,15.6653379653543,5.82367908580836));
#131302=CARTESIAN_POINT('Ctrl Pts',(14.8755933965129,15.6516319005856,5.85037835679467));
#131303=CARTESIAN_POINT('Ctrl Pts',(14.8780805875388,15.6363123514682,5.87617713629024));
#131304=CARTESIAN_POINT('Ctrl Pts',(14.8783372320461,15.6347315809945,5.87883922174531));
#131305=CARTESIAN_POINT('Ctrl Pts',(14.8785935538916,15.6331336718161,5.88149169853617));
#131306=CARTESIAN_POINT('Ctrl Pts',(14.8788495980807,15.6315187792568,5.88413431046347));
#131307=CARTESIAN_POINT('Ctrl Pts',(14.8815838816912,15.6142734190979,5.91235463644495));
#131308=CARTESIAN_POINT('Ctrl Pts',(14.8842873387627,15.5950864649871,5.93945286103092));
#131309=CARTESIAN_POINT('Ctrl Pts',(14.8870069435193,15.5741535137537,5.96516823149236));
#131310=CARTESIAN_POINT('Ctrl Pts',(14.8897237451682,15.5532421381983,5.99085709701695));
#131311=CARTESIAN_POINT('Ctrl Pts',(14.8924571417644,15.5305888881882,6.01516617657772));
#131312=CARTESIAN_POINT('Ctrl Pts',(14.8952363470137,15.5064160849056,6.0378694409836));
#131313=CARTESIAN_POINT('Ctrl Pts',(14.8980142277164,15.4822548021852,6.06056188519767));
#131314=CARTESIAN_POINT('Ctrl Pts',(14.9008380981967,15.4565756861741,6.08165020872348));
#131315=CARTESIAN_POINT('Ctrl Pts',(14.9037143306719,15.4296221887639,6.10093966148744));
#131316=CARTESIAN_POINT('Ctrl Pts',(14.9065929151896,15.4026466500983,6.120244888225));
#131317=CARTESIAN_POINT('Ctrl Pts',(14.9095239890321,15.3743947243384,6.13774836173002));
#131318=CARTESIAN_POINT('Ctrl Pts',(14.9124891202093,15.3451293350402,6.1532841613303));
#131319=CARTESIAN_POINT('Ctrl Pts',(14.9154556707582,15.3158499367599,6.1688273977269));
#131320=CARTESIAN_POINT('Ctrl Pts',(14.9184561483448,15.2855559865514,6.18240098230982));
#131321=CARTESIAN_POINT('Ctrl Pts',(14.9214481122626,15.2545299341904,6.19386822545329));
#131322=CARTESIAN_POINT('Ctrl Pts',(14.924445878342,15.2234437146039,6.2053577064308));
#131323=CARTESIAN_POINT('Ctrl Pts',(14.9274346251376,15.1916222515561,6.21473224791747));
#131324=CARTESIAN_POINT('Ctrl Pts',(14.9303522083298,15.1593720926524,6.22188759901106));
#131325=CARTESIAN_POINT('Ctrl Pts',(14.9313849042293,15.1479569573624,6.22442027802899));
#131326=CARTESIAN_POINT('Ctrl Pts',(14.9324085444352,15.1364883406239,6.22667526330663));
#131327=CARTESIAN_POINT('Ctrl Pts',(14.9334200198331,15.124980619804,6.22864914415783));
#131328=CARTESIAN_POINT('Ctrl Pts',(14.9334212789608,15.1249662945023,6.2286516013289));
#131329=CARTESIAN_POINT('Ctrl Pts',(14.9334225380716,15.1249519691109,6.22865405807048));
#131330=CARTESIAN_POINT('Ctrl Pts',(14.9334237971656,15.1249376436298,6.22865651438255));
#131331=CARTESIAN_POINT('Ctrl Pts',(14.9360125426822,15.0954839052033,6.23370678617647));
#131332=CARTESIAN_POINT('Ctrl Pts',(14.9385300175094,15.065647035084,6.2369393898572));
#131333=CARTESIAN_POINT('Ctrl Pts',(14.9410171849092,15.0356751200762,6.23832921061113));
#131334=CARTESIAN_POINT('Ctrl Pts',(14.9412738427776,15.0325822330357,6.23847263016231));
#131335=CARTESIAN_POINT('Ctrl Pts',(14.9415301779094,15.0294879476791,6.23859644903481));
#131336=CARTESIAN_POINT('Ctrl Pts',(14.9417862353182,15.0263925634539,6.23870065608836));
#131337=CARTESIAN_POINT('Ctrl Pts',(14.9445205074269,14.9933389494504,6.23981341607999));
#131338=CARTESIAN_POINT('Ctrl Pts',(14.9472239489535,14.9601549780845,6.23868746473644));
#131339=CARTESIAN_POINT('Ctrl Pts',(14.9499435353598,14.9271659939967,6.23534279795633));
#131340=CARTESIAN_POINT('Ctrl Pts',(14.9526603183903,14.8942110152714,6.23200157889094));
#131341=CARTESIAN_POINT('Ctrl Pts',(14.9553936935767,14.8614507279703,6.2264467753758));
#131342=CARTESIAN_POINT('Ctrl Pts',(14.958172876127,14.8291961681283,6.21873979836838));
#131343=CARTESIAN_POINT('Ctrl Pts',(14.9609507338853,14.7969569835211,6.21103649515415));
#131344=CARTESIAN_POINT('Ctrl Pts',(14.9637745801328,14.7652230567194,6.20118338718233));
#131345=CARTESIAN_POINT('Ctrl Pts',(14.9666507887204,14.7342909163415,6.18927673425501));
#131346=CARTESIAN_POINT('Ctrl Pts',(14.9695293490742,14.7033334839295,6.17736034571067));
#131347=CARTESIAN_POINT('Ctrl Pts',(14.9724603990982,14.673179142556,6.1633871523955));
#131348=CARTESIAN_POINT('Ctrl Pts',(14.9754255084587,14.6441110472132,6.14748553004897));
#131349=CARTESIAN_POINT('Ctrl Pts',(14.9783920370114,14.6150290389907,6.13157629669957));
#131350=CARTESIAN_POINT('Ctrl Pts',(14.981392494618,14.5870343302754,6.11373663792384));
#131351=CARTESIAN_POINT('Ctrl Pts',(14.9843844420708,14.5603963968804,6.09412731152478));
#131352=CARTESIAN_POINT('Ctrl Pts',(14.9873821915862,14.5337068065101,6.07447995820843));
#131353=CARTESIAN_POINT('Ctrl Pts',(14.9903709253773,14.50837944566,6.05305558592979));
#131354=CARTESIAN_POINT('Ctrl Pts',(14.9932885001231,14.4846699455329,6.03005291635318));
#131355=CARTESIAN_POINT('Ctrl Pts',(14.9943212873573,14.4762770606222,6.02191024116567));
#131356=CARTESIAN_POINT('Ctrl Pts',(14.9953450178091,14.4680867496832,6.01357016871636));
#131357=CARTESIAN_POINT('Ctrl Pts',(14.9963565815236,14.4601097698342,6.00504283513605));
#131358=CARTESIAN_POINT('Ctrl Pts',(14.9963578406379,14.4600998407223,6.00503222098741));
#131359=CARTESIAN_POINT('Ctrl Pts',(14.9963590997355,14.4600899119181,6.00502160652613));
#131360=CARTESIAN_POINT('Ctrl Pts',(14.9963603588163,14.4600799834219,6.00501099175224));
#131361=CARTESIAN_POINT('Ctrl Pts',(14.9989264199637,14.4398452791334,5.98337762402734));
#131362=CARTESIAN_POINT('Ctrl Pts',(15.0014230133456,14.4208889613002,5.96044138623255));
#131363=CARTESIAN_POINT('Ctrl Pts',(15.0038897946441,14.4033688781723,5.93639150010391));
#131364=CARTESIAN_POINT('Ctrl Pts',(15.0041351714271,14.401626112554,5.9339991989736));
#131365=CARTESIAN_POINT('Ctrl Pts',(15.0043802532264,14.3998975597837,5.93159592106345));
#131366=CARTESIAN_POINT('Ctrl Pts',(15.0046250790734,14.3981833754518,5.92918188070301));
#131367=CARTESIAN_POINT('Ctrl Pts',(15.007427460399,14.3785620886504,5.90154974255911));
#131368=CARTESIAN_POINT('Ctrl Pts',(15.0101972648971,14.3608230937688,5.87250150924527));
#131369=CARTESIAN_POINT('Ctrl Pts',(15.0129847378888,14.3451451873103,5.84234467510009));
#131370=CARTESIAN_POINT('Ctrl Pts',(15.0157722078083,14.3294672981314,5.81218787419279));
#131371=CARTESIAN_POINT('Ctrl Pts',(15.0185779004322,14.315850069152,5.78092297439461));
#131372=CARTESIAN_POINT('Ctrl Pts',(15.0214324762185,14.3044236561645,5.74887185968306));
#131373=CARTESIAN_POINT('Origin',(13.2437274406976,15.,5.5));
#131374=CARTESIAN_POINT('',(15.5006844331709,14.3042076643853,5.74898599498742));
#131375=CARTESIAN_POINT('',(15.4218039449815,14.3042130191175,5.74898305899437));
#131376=CARTESIAN_POINT('',(13.2437274406976,14.3042076641721,5.74898599439144));
#131377=CARTESIAN_POINT('Ctrl Pts',(15.5006844331709,14.3042076645986,5.7489859955834));
#131378=CARTESIAN_POINT('Ctrl Pts',(15.4981861316207,14.3133756656007,5.77460601012787));
#131379=CARTESIAN_POINT('Ctrl Pts',(15.4956999505869,14.323953135999,5.7997040624191));
#131380=CARTESIAN_POINT('Ctrl Pts',(15.4924749873236,14.3397861202763,5.83214063832067));
#131381=CARTESIAN_POINT('Ctrl Pts',(15.4916880923997,14.3438229318855,5.84004624332186));
#131382=CARTESIAN_POINT('Ctrl Pts',(15.4904483724183,14.3504715583388,5.85250721549171));
#131383=CARTESIAN_POINT('Ctrl Pts',(15.4899905344219,14.3529910127437,5.85711050041579));
#131384=CARTESIAN_POINT('Ctrl Pts',(15.4890783641418,14.3581429899698,5.86629010920502));
#131385=CARTESIAN_POINT('Ctrl Pts',(15.4886240901128,14.360775939403,5.87086583989662));
#131386=CARTESIAN_POINT('Ctrl Pts',(15.4874003930892,14.368045271583,5.88319155650544));
#131387=CARTESIAN_POINT('Ctrl Pts',(15.4866365007217,14.372775230978,5.89088573748443));
#131388=CARTESIAN_POINT('Ctrl Pts',(15.4825581322327,14.3990044101059,5.93184981887718));
#131389=CARTESIAN_POINT('Ctrl Pts',(15.4793696563172,14.4230140590203,5.96344157916389));
#131390=CARTESIAN_POINT('Ctrl Pts',(15.4735867795493,14.4709293648759,6.01695517899527));
#131391=CARTESIAN_POINT('Ctrl Pts',(15.4709993584947,14.4939590227313,6.0395189884298));
#131392=CARTESIAN_POINT('Ctrl Pts',(15.467533367178,14.5260966204892,6.06713308338228));
#131393=CARTESIAN_POINT('Ctrl Pts',(15.4666976704082,14.5339427815203,6.07359829222213));
#131394=CARTESIAN_POINT('Ctrl Pts',(15.4646029116109,14.5538117770367,6.0892934278339));
#131395=CARTESIAN_POINT('Ctrl Pts',(15.4633378551875,14.5659893106941,6.09831875484494));
#131396=CARTESIAN_POINT('Ctrl Pts',(15.4612753539412,14.5860579269549,6.11225738392157));
#131397=CARTESIAN_POINT('Ctrl Pts',(15.4604868749982,14.5937796895815,6.11740763434963));
#131398=CARTESIAN_POINT('Ctrl Pts',(15.4589479082104,14.6089318202291,6.12710648327711));
#131399=CARTESIAN_POINT('Ctrl Pts',(15.4581981909701,14.6163496904144,6.13167182019241));
#131400=CARTESIAN_POINT('Ctrl Pts',(15.4563685962439,14.634527890282,6.14242130606061));
#131401=CARTESIAN_POINT('Ctrl Pts',(15.4552840565502,14.6453662676324,6.14846732575677));
#131402=CARTESIAN_POINT('Ctrl Pts',(15.4490720261915,14.7077482062829,6.18123447541211));
#131403=CARTESIAN_POINT('Ctrl Pts',(15.4437471548227,14.7621377636819,6.20207567475584));
#131404=CARTESIAN_POINT('Ctrl Pts',(15.4356778200098,14.8472672358452,6.22365820597087));
#131405=CARTESIAN_POINT('Ctrl Pts',(15.4329504935942,14.8765639018257,6.22922725943238));
#131406=CARTESIAN_POINT('Ctrl Pts',(15.4294875498167,14.9149986421132,6.23414978055329));
#131407=CARTESIAN_POINT('Ctrl Pts',(15.4286937201891,14.9238982713221,6.23512562207877));
#131408=CARTESIAN_POINT('Ctrl Pts',(15.4274457571045,14.9380549873666,6.23641802796965));
#131409=CARTESIAN_POINT('Ctrl Pts',(15.426986503302,14.9433011584626,6.236840514129));
#131410=CARTESIAN_POINT('Ctrl Pts',(15.426130337972,14.9531561764013,6.23752827819928));
#131411=CARTESIAN_POINT('Ctrl Pts',(15.4257327269203,14.9577638128169,6.23780648757034));
#131412=CARTESIAN_POINT('Ctrl Pts',(15.4246327235724,14.9705883729491,6.23846029568647));
#131413=CARTESIAN_POINT('Ctrl Pts',(15.4239351666281,14.9788097560181,6.23874193292489));
#131414=CARTESIAN_POINT('Ctrl Pts',(15.4192332868046,15.0347087120355,6.23972279956432));
#131415=CARTESIAN_POINT('Ctrl Pts',(15.4154228796418,15.0823597885935,6.23594351438948));
#131416=CARTESIAN_POINT('Ctrl Pts',(15.4084553561543,15.1675531638058,6.22080152425317));
#131417=CARTESIAN_POINT('Ctrl Pts',(15.4053197640139,15.2051861723463,6.21100421524594));
#131418=CARTESIAN_POINT('Ctrl Pts',(15.4009634553932,15.2547582025784,6.19383371255165));
#131419=CARTESIAN_POINT('Ctrl Pts',(15.3998215222683,15.2675170219097,6.18901491840268));
#131420=CARTESIAN_POINT('Ctrl Pts',(15.3979065588366,15.2884666321186,6.18043300737628));
#131421=CARTESIAN_POINT('Ctrl Pts',(15.3971401426835,15.2967353261543,6.17686793870034));
#131422=CARTESIAN_POINT('Ctrl Pts',(15.3955963724329,15.3131453657191,6.16943423457033));
#131423=CARTESIAN_POINT('Ctrl Pts',(15.3948191418274,15.3212851642268,6.16556595619604));
#131424=CARTESIAN_POINT('Ctrl Pts',(15.3928490714833,15.3415982260221,6.15545312448036));
#131425=CARTESIAN_POINT('Ctrl Pts',(15.391649899273,15.3536720440601,6.14901785601911));
#131426=CARTESIAN_POINT('Ctrl Pts',(15.3864062106976,15.4051746547766,6.11970338634263));
#131427=CARTESIAN_POINT('Ctrl Pts',(15.3822515733105,15.4426115822421,6.09354219936424));
#131428=CARTESIAN_POINT('Ctrl Pts',(15.3754570238094,15.4990455022024,6.04578299395352));
#131429=CARTESIAN_POINT('Ctrl Pts',(15.3728451000567,15.5196245068181,6.02622808863488));
#131430=CARTESIAN_POINT('Ctrl Pts',(15.3692426747452,15.5467720482305,5.99728204945637));
#131431=CARTESIAN_POINT('Ctrl Pts',(15.3682216878176,15.5543246964849,5.98884892663414));
#131432=CARTESIAN_POINT('Ctrl Pts',(15.3664214347519,15.5674204115569,5.97353254885324));
#131433=CARTESIAN_POINT('Ctrl Pts',(15.3656385026394,15.5730393481342,5.96671717902119));
#131434=CARTESIAN_POINT('Ctrl Pts',(15.3644034907934,15.5817944342483,5.95570130261518));
#131435=CARTESIAN_POINT('Ctrl Pts',(15.3639464592728,15.5850102212622,5.95156559618653));
#131436=CARTESIAN_POINT('Ctrl Pts',(15.3630343140923,15.5913833571592,5.9431869679682));
#131437=CARTESIAN_POINT('Ctrl Pts',(15.3625792773048,15.5945396805755,5.9389436608149));
#131438=CARTESIAN_POINT('Ctrl Pts',(15.3613509784014,15.6029887759995,5.92732647113087));
#131439=CARTESIAN_POINT('Ctrl Pts',(15.3605833178554,15.6081919191402,5.91988806795778));
#131440=CARTESIAN_POINT('Ctrl Pts',(15.3572242820411,15.6305500836759,5.88663687319953));
#131441=CARTESIAN_POINT('Ctrl Pts',(15.3547070761151,15.6462105001422,5.85985270889106));
#131442=CARTESIAN_POINT('Ctrl Pts',(15.3491478058262,15.6771699870741,5.79832311926794));
#131443=CARTESIAN_POINT('Ctrl Pts',(15.3461200694798,15.6915684577631,5.76322768508735));
#131444=CARTESIAN_POINT('Ctrl Pts',(15.3411306073947,15.7103716762329,5.70502521312085));
#131445=CARTESIAN_POINT('Ctrl Pts',(15.3392112253379,15.7164783274423,5.68254277834742));
#131446=CARTESIAN_POINT('Ctrl Pts',(15.3363677894907,15.7238127940514,5.64942930716048));
#131447=CARTESIAN_POINT('Ctrl Pts',(15.3354699313882,15.7258879153481,5.63899924116567));
#131448=CARTESIAN_POINT('Ctrl Pts',(15.333839906966,15.729219075678,5.62013799352749));
#131449=CARTESIAN_POINT('Ctrl Pts',(15.3331103914427,15.7305556783495,5.61172280685354));
#131450=CARTESIAN_POINT('Ctrl Pts',(15.3314975702183,15.733171771607,5.59318880634765));
#131451=CARTESIAN_POINT('Ctrl Pts',(15.3306124500743,15.7343878500848,5.58306300722543));
#131452=CARTESIAN_POINT('Ctrl Pts',(15.32793810052,15.737405704941,5.55262637472144));
#131453=CARTESIAN_POINT('Ctrl Pts',(15.3261303316822,15.73857669323,5.53226462500212));
#131454=CARTESIAN_POINT('Ctrl Pts',(15.3193640188557,15.7397887294718,5.45689514901511));
#131455=CARTESIAN_POINT('Ctrl Pts',(15.3142708877315,15.7345318580043,5.40198522419863));
#131456=CARTESIAN_POINT('Ctrl Pts',(15.3078648334357,15.7201306655421,5.33338267580967));
#131457=CARTESIAN_POINT('Ctrl Pts',(15.306491227146,15.7165716565863,5.31868637282943));
#131458=CARTESIAN_POINT('Ctrl Pts',(15.3041567068893,15.709684120363,5.29363263191981));
#131459=CARTESIAN_POINT('Ctrl Pts',(15.3031886952572,15.706573243469,5.28322054967123));
#131460=CARTESIAN_POINT('Ctrl Pts',(15.3017352799149,15.7015005157098,5.26751381355664));
#131461=CARTESIAN_POINT('Ctrl Pts',(15.3012417667802,15.69970594552,5.26216729266063));
#131462=CARTESIAN_POINT('Ctrl Pts',(15.3003207992447,15.696218298093,5.25215795151998));
#131463=CARTESIAN_POINT('Ctrl Pts',(15.2998926874294,15.6945392948091,5.24749104989162));
#131464=CARTESIAN_POINT('Ctrl Pts',(15.2988154875267,15.6901702798967,5.23572046527283));
#131465=CARTESIAN_POINT('Ctrl Pts',(15.2981699036334,15.687417486591,5.22864064195116));
#131466=CARTESIAN_POINT('Ctrl Pts',(15.2952657675121,15.6744431463359,5.19673765738197));
#131467=CARTESIAN_POINT('Ctrl Pts',(15.2930671921494,15.662981628611,5.17243725069471));
#131468=CARTESIAN_POINT('Ctrl Pts',(15.2883146328304,15.6351257756688,5.12086244949662));
#131469=CARTESIAN_POINT('Ctrl Pts',(15.285773677615,15.6182436975709,5.09391523288703));
#131470=CARTESIAN_POINT('Ctrl Pts',(15.2805032809056,15.5801223248354,5.04098028397749));
#131471=CARTESIAN_POINT('Ctrl Pts',(15.2777768154182,15.5587451870643,5.01518625713211));
#131472=CARTESIAN_POINT('Ctrl Pts',(15.2740035976647,15.5276184484873,4.98243138155775));
#131473=CARTESIAN_POINT('Ctrl Pts',(15.2730169406041,15.5193400941577,4.97412516970498));
#131474=CARTESIAN_POINT('Ctrl Pts',(15.2712834629087,15.5045826920972,4.96000650581688));
#131475=CARTESIAN_POINT('Ctrl Pts',(15.2705406162339,15.4981918959925,4.95410487465395));
#131476=CARTESIAN_POINT('Ctrl Pts',(15.2689713617391,15.484562719481,4.9419575785705));
#131477=CARTESIAN_POINT('Ctrl Pts',(15.268144110608,15.4773043849164,4.93573687113212));
#131478=CARTESIAN_POINT('Ctrl Pts',(15.2658586113336,15.4570647386553,4.91906058006096));
#131479=CARTESIAN_POINT('Ctrl Pts',(15.2643892260522,15.4438480076003,4.90890133232782));
#131480=CARTESIAN_POINT('Ctrl Pts',(15.2575325826782,15.3813012542295,4.86410470847991));
#131481=CARTESIAN_POINT('Ctrl Pts',(15.2519536994261,15.3281984521128,4.83514144674961));
#131482=CARTESIAN_POINT('Ctrl Pts',(15.2450221703642,15.2577225678547,4.80722152460192));
#131483=CARTESIAN_POINT('Ctrl Pts',(15.2436077959801,15.2430833708254,4.80195023186749));
#131484=CARTESIAN_POINT('Ctrl Pts',(15.2412130693636,15.2177471847386,4.79372102658508));
#131485=CARTESIAN_POINT('Ctrl Pts',(15.2402251711931,15.2071300646936,4.7905347082374));
#131486=CARTESIAN_POINT('Ctrl Pts',(15.2387485403647,15.1909688463192,4.78607832230386));
#131487=CARTESIAN_POINT('Ctrl Pts',(15.2382513241704,15.1854757189655,4.7846315450095));
#131488=CARTESIAN_POINT('Ctrl Pts',(15.2373278766807,15.1751699984046,4.78204392526856));
#131489=CARTESIAN_POINT('Ctrl Pts',(15.2369009265237,15.1703620395085,4.78088788677452));
#131490=CARTESIAN_POINT('Ctrl Pts',(15.2358329177675,15.1582333990356,4.77810012079674));
#131491=CARTESIAN_POINT('Ctrl Pts',(15.235195231477,15.1508987734924,4.77653139792875));
#131492=CARTESIAN_POINT('Ctrl Pts',(15.2324538033784,15.1190208130612,4.77021930481038));
#131493=CARTESIAN_POINT('Ctrl Pts',(15.2304017081464,15.0942666982995,4.76661065474652));
#131494=CARTESIAN_POINT('Ctrl Pts',(15.2247654725293,15.0251803396307,4.76009634469771));
#131495=CARTESIAN_POINT('Ctrl Pts',(15.2212347128843,14.9807009808366,4.75991952041867));
#131496=CARTESIAN_POINT('Ctrl Pts',(15.2162066937237,14.919151407828,4.76523009136065));
#131497=CARTESIAN_POINT('Ctrl Pts',(15.2147814187573,14.9018879048862,4.76733550905956));
#131498=CARTESIAN_POINT('Ctrl Pts',(15.2121603215073,14.8706624072444,4.77226707599984));
#131499=CARTESIAN_POINT('Ctrl Pts',(15.2109704525231,14.8566771217979,4.77489178694993));
#131500=CARTESIAN_POINT('Ctrl Pts',(15.2089982188837,14.8338749631326,4.77985662623833));
#131501=CARTESIAN_POINT('Ctrl Pts',(15.2082233541159,14.8250097866401,4.78195932132144));
#131502=CARTESIAN_POINT('Ctrl Pts',(15.2066885427285,14.8076493294858,4.7864175569321));
#131503=CARTESIAN_POINT('Ctrl Pts',(15.2059290575557,14.7991528282493,4.78876228837253));
#131504=CARTESIAN_POINT('Ctrl Pts',(15.2040324513256,14.778181147762,4.79495545918812));
#131505=CARTESIAN_POINT('Ctrl Pts',(15.2028897871548,14.7657626925221,4.79898342085638));
#131506=CARTESIAN_POINT('Ctrl Pts',(15.1970292133704,14.7032148559598,4.82111847343141));
#131507=CARTESIAN_POINT('Ctrl Pts',(15.1921511948226,14.6550518762363,4.84427891666842));
#131508=CARTESIAN_POINT('Ctrl Pts',(15.184262763908,14.5821777722817,4.88958696347024));
#131509=CARTESIAN_POINT('Ctrl Pts',(15.1812770768556,14.5557098490978,4.90857276570762));
#131510=CARTESIAN_POINT('Ctrl Pts',(15.1775375990922,14.5234239159424,4.93512654442446));
#131511=CARTESIAN_POINT('Ctrl Pts',(15.1767155536211,14.5163812516878,4.94114428040627));
#131512=CARTESIAN_POINT('Ctrl Pts',(15.1754340799272,14.5054699581362,4.9508284414386));
#131513=CARTESIAN_POINT('Ctrl Pts',(15.1749690821581,14.5015249425992,4.95440675797896));
#131514=CARTESIAN_POINT('Ctrl Pts',(15.1740559574324,14.493801619868,4.96156589058948));
#131515=CARTESIAN_POINT('Ctrl Pts',(15.1736077399166,14.4900218082253,4.96514456300887));
#131516=CARTESIAN_POINT('Ctrl Pts',(15.1724208269508,14.4800518053797,4.97478581602349));
#131517=CARTESIAN_POINT('Ctrl Pts',(15.1716871019361,14.4739296117049,4.98091808818721));
#131518=CARTESIAN_POINT('Ctrl Pts',(15.1669246907344,14.4345650743947,5.02175949748127));
#131519=CARTESIAN_POINT('Ctrl Pts',(15.1630883000331,14.4046634511938,5.05953834011732));
#131520=CARTESIAN_POINT('Ctrl Pts',(15.1564619839311,14.3601271268223,5.12871404094873));
#131521=CARTESIAN_POINT('Ctrl Pts',(15.1536987860371,14.343634509876,5.15871634376645));
#131522=CARTESIAN_POINT('Ctrl Pts',(15.1495995528462,14.3228219722918,5.20371045200673));
#131523=CARTESIAN_POINT('Ctrl Pts',(15.1483161873207,14.3168025245518,5.21786754736671));
#131524=CARTESIAN_POINT('Ctrl Pts',(15.1462316606304,14.3078509964003,5.24089060716967));
#131525=CARTESIAN_POINT('Ctrl Pts',(15.145439837054,14.3046373909379,5.24964276344141));
#131526=CARTESIAN_POINT('Ctrl Pts',(15.1438909747184,14.2987179708466,5.26675818771838));
#131527=CARTESIAN_POINT('Ctrl Pts',(15.1431346724125,14.295994096024,5.27511358406749));
#131528=CARTESIAN_POINT('Ctrl Pts',(15.1413035450768,14.2898016665464,5.29532491788782));
#131529=CARTESIAN_POINT('Ctrl Pts',(15.1402242320716,14.2864802519917,5.3072226904373));
#131530=CARTESIAN_POINT('Ctrl Pts',(15.1339829113367,14.2691561771627,5.3758799476414));
#131531=CARTESIAN_POINT('Ctrl Pts',(15.1286201460481,14.2616328904203,5.43404843570366));
#131532=CARTESIAN_POINT('Ctrl Pts',(15.1205345037587,14.2607373493634,5.52204944684244));
#131533=CARTESIAN_POINT('Ctrl Pts',(15.1178278533825,14.2622115112062,5.55161352494177));
#131534=CARTESIAN_POINT('Ctrl Pts',(15.114387174355,14.2664323502094,5.58988419383587));
#131535=CARTESIAN_POINT('Ctrl Pts',(15.1135957134548,14.2675715227852,5.59873810271899));
#131536=CARTESIAN_POINT('Ctrl Pts',(15.1123505665385,14.2696361944341,5.61277123840683));
#131537=CARTESIAN_POINT('Ctrl Pts',(15.1118917969224,14.2704569974679,5.61796462862891));
#131538=CARTESIAN_POINT('Ctrl Pts',(15.1110358145192,14.2721029791986,5.62770381912303));
#131539=CARTESIAN_POINT('Ctrl Pts',(15.1106379106869,14.2729154816681,5.63225144677907));
#131540=CARTESIAN_POINT('Ctrl Pts',(15.1095358525569,14.2752969886803,5.64489493903591));
#131541=CARTESIAN_POINT('Ctrl Pts',(15.1088365642261,14.2769589960563,5.65297294696688));
#131542=CARTESIAN_POINT('Ctrl Pts',(15.105572575207,14.2854161614428,5.69085398919124));
#131543=CARTESIAN_POINT('Ctrl Pts',(15.1030853361234,14.2939179596096,5.72023137888309));
#131544=CARTESIAN_POINT('Ctrl Pts',(15.1006178015771,14.3042076756101,5.74898602635499));
#131545=CARTESIAN_POINT('',(15.043709765672,14.2610104882535,5.49935386504384));
#131546=CARTESIAN_POINT('Ctrl Pts',(15.0212936472645,14.3041920192027,5.74894227013274));
#131547=CARTESIAN_POINT('Ctrl Pts',(15.0223182907216,14.3000436147494,5.73734724079242));
#131548=CARTESIAN_POINT('Ctrl Pts',(15.0233508648385,14.2961859397969,5.72565103150668));
#131549=CARTESIAN_POINT('Ctrl Pts',(15.0250923247468,14.2902294392276,5.7059493344584));
#131550=CARTESIAN_POINT('Ctrl Pts',(15.025795992383,14.287969522801,5.69799486144921));
#131551=CARTESIAN_POINT('Ctrl Pts',(15.0272756037324,14.2835264193999,5.68129488363134));
#131552=CARTESIAN_POINT('Ctrl Pts',(15.0280522266231,14.2813688318268,5.67254406693846));
#131553=CARTESIAN_POINT('Ctrl Pts',(15.0299512189619,14.2765178666212,5.651196858922));
#131554=CARTESIAN_POINT('Ctrl Pts',(15.03107861212,14.2739928573599,5.63856576440307));
#131555=CARTESIAN_POINT('Ctrl Pts',(15.0359616676643,14.264574940277,5.58408250794419));
#131556=CARTESIAN_POINT('Ctrl Pts',(15.0398126156169,14.2609631816662,5.54175221801516));
#131557=CARTESIAN_POINT('Ctrl Pts',(15.0437039207594,14.2610002829325,5.49935333612335));
#131558=CARTESIAN_POINT('Ctrl Pts',(15.043709765672,14.2610104882535,5.49935386504384));
#131559=CARTESIAN_POINT('Ctrl Pts',(15.046685545653,14.2609595334599,5.46642905352292));
#131560=CARTESIAN_POINT('Ctrl Pts',(15.0496697149401,14.2631076464298,5.43358447738546));
#131561=CARTESIAN_POINT('Ctrl Pts',(15.052610173577,14.2674364515606,5.40107731686082));
#131562=CARTESIAN_POINT('Ctrl Pts',(15.0535470231831,14.2688156375593,5.39072032011563));
#131563=CARTESIAN_POINT('Ctrl Pts',(15.0544794357131,14.2704163193918,5.38039720107147));
#131564=CARTESIAN_POINT('Ctrl Pts',(15.0554057261597,14.2722383764944,5.37011526689897));
#131565=CARTESIAN_POINT('Ctrl Pts',(15.0567161994914,14.2748161394955,5.35556885699023));
#131566=CARTESIAN_POINT('Ctrl Pts',(15.0580139727417,14.277836233072,5.34110642935388));
#131567=CARTESIAN_POINT('Ctrl Pts',(15.059293127905,14.2812964464757,5.32675188192325));
#131568=CARTESIAN_POINT('Ctrl Pts',(15.0592943869642,14.281299852328,5.32673775289072));
#131569=CARTESIAN_POINT('Ctrl Pts',(15.0592956460065,14.2813032586102,5.32672362394553));
#131570=CARTESIAN_POINT('Ctrl Pts',(15.059296905032,14.2813066653223,5.32670949508773));
#131571=CARTESIAN_POINT('Ctrl Pts',(15.0618856599462,14.2883114026749,5.29765833542018));
#131572=CARTESIAN_POINT('Ctrl Pts',(15.0644031451847,14.2971372223748,5.26897381748352));
#131573=CARTESIAN_POINT('Ctrl Pts',(15.0668903239177,14.3077091184231,5.24089375008832));
#131574=CARTESIAN_POINT('Ctrl Pts',(15.0671469791864,14.3088000463832,5.23799613073031));
#131575=CARTESIAN_POINT('Ctrl Pts',(15.0674033117378,14.3099095308069,5.23510497537456));
#131576=CARTESIAN_POINT('Ctrl Pts',(15.0676593665835,14.3110374635529,5.2322205634705));
#131577=CARTESIAN_POINT('Ctrl Pts',(15.0703936478333,14.3230820915351,5.2014193756733));
#131578=CARTESIAN_POINT('Ctrl Pts',(15.0730970996172,14.337234617664,5.17138346159711));
#131579=CARTESIAN_POINT('Ctrl Pts',(15.0758166969593,14.353348058333,5.14240376075178));
#131580=CARTESIAN_POINT('Ctrl Pts',(15.0785334910692,14.3694448900303,5.11345393080986));
#131581=CARTESIAN_POINT('Ctrl Pts',(15.0812668780129,14.3874980403923,5.0855580140648));
#131582=CARTESIAN_POINT('Ctrl Pts',(15.0840460724848,14.4073281408633,5.05897743470522));
#131583=CARTESIAN_POINT('Ctrl Pts',(15.0868239422916,14.4271487895874,5.03240952461625));
#131584=CARTESIAN_POINT('Ctrl Pts',(15.0896478007549,14.4487443984622,5.00715558422028));
#131585=CARTESIAN_POINT('Ctrl Pts',(15.0925240211446,14.4719093238968,4.98344993559047));
#131586=CARTESIAN_POINT('Ctrl Pts',(15.0954025934196,14.4950931912908,4.95972490285195));
#131587=CARTESIAN_POINT('Ctrl Pts',(15.0983336549516,14.5198488539283,4.93755064902295));
#131588=CARTESIAN_POINT('Ctrl Pts',(15.101298774781,14.5459464551747,4.91713651593686));
#131589=CARTESIAN_POINT('Ctrl Pts',(15.1042653138839,14.5720565482031,4.89671261149691));
#131590=CARTESIAN_POINT('Ctrl Pts',(15.1072657809954,14.5995099972452,4.87805058477965));
#131591=CARTESIAN_POINT('Ctrl Pts',(15.1102577363054,14.6280526088082,4.86133441152981));
#131592=CARTESIAN_POINT('Ctrl Pts',(15.1132554936804,14.6566505708263,4.84458582191203));
#131593=CARTESIAN_POINT('Ctrl Pts',(15.1162442336628,14.6863422917646,4.82979100185164));
#131594=CARTESIAN_POINT('Ctrl Pts',(15.1191618125078,14.7168441793445,4.81710620235439));
#131595=CARTESIAN_POINT('Ctrl Pts',(15.1201945367908,14.7276408164384,4.81261621213913));
#131596=CARTESIAN_POINT('Ctrl Pts',(15.1212182051605,14.7385386779047,4.80839029865132));
#131597=CARTESIAN_POINT('Ctrl Pts',(15.1222297082397,14.7495242032278,4.80443433472866));
#131598=CARTESIAN_POINT('Ctrl Pts',(15.1222309673336,14.7495378777366,4.80442941044312));
#131599=CARTESIAN_POINT('Ctrl Pts',(15.1222322264106,14.7495515524089,4.80442448656474));
#131600=CARTESIAN_POINT('Ctrl Pts',(15.1222334854708,14.7495652272445,4.80441956309354));
#131601=CARTESIAN_POINT('Ctrl Pts',(15.1248222384473,14.7776820501033,4.79429641640001));
#131602=CARTESIAN_POINT('Ctrl Pts',(15.1273397213037,14.80649396278,4.78589594207448));
#131603=CARTESIAN_POINT('Ctrl Pts',(15.1298268971727,14.8357610914496,4.77928625107586));
#131604=CARTESIAN_POINT('Ctrl Pts',(15.130083554543,14.8387812334403,4.77860418193421));
#131605=CARTESIAN_POINT('Ctrl Pts',(15.1303398891848,14.8418061797683,4.7779411668358));
#131606=CARTESIAN_POINT('Ctrl Pts',(15.1305959461108,14.8448356375512,4.77729726911286));
#131607=CARTESIAN_POINT('Ctrl Pts',(15.1333302264247,14.8771854236143,4.77042146655147));
#131608=CARTESIAN_POINT('Ctrl Pts',(15.1360336766783,14.9100550468417,4.76572709493435));
#131609=CARTESIAN_POINT('Ctrl Pts',(15.1387532720654,14.9431206775473,4.76325135956388));
#131610=CARTESIAN_POINT('Ctrl Pts',(15.1414700641897,14.9761522253698,4.76077817609391));
#131611=CARTESIAN_POINT('Ctrl Pts',(15.1442034487258,15.0093791747229,4.76051852538285));
#131612=CARTESIAN_POINT('Ctrl Pts',(15.1469826405762,15.0424845418505,4.76246633367419));
#131613=CARTESIAN_POINT('Ctrl Pts',(15.1497605077328,15.075574129401,4.76441321354837));
#131614=CARTESIAN_POINT('Ctrl Pts',(15.1525843633328,15.1085421829167,4.76856513821236));
#131615=CARTESIAN_POINT('Ctrl Pts',(15.1554605808695,15.1410799084982,4.77487918515324));
#131616=CARTESIAN_POINT('Ctrl Pts',(15.1583391502564,15.1736442398058,4.78119839501808));
#131617=CARTESIAN_POINT('Ctrl Pts',(15.1612702089108,15.205777528696,4.7896831650204));
#131618=CARTESIAN_POINT('Ctrl Pts',(15.1642353260955,15.2371785326199,4.8002566129381));
#131619=CARTESIAN_POINT('Ctrl Pts',(15.1672018625311,15.2685945666086,4.81083512182802));
#131620=CARTESIAN_POINT('Ctrl Pts',(15.17020232721,15.2992776274748,4.82350445858556));
#131621=CARTESIAN_POINT('Ctrl Pts',(15.1731942805184,15.3289342782322,4.83815346573462));
#131622=CARTESIAN_POINT('Ctrl Pts',(15.1761920358741,15.3586484396771,4.85283088049035));
#131623=CARTESIAN_POINT('Ctrl Pts',(15.1791807742738,15.3873321063918,4.8694961575027));
#131624=CARTESIAN_POINT('Ctrl Pts',(15.1820983521007,15.4146988337077,4.88799833915478));
#131625=CARTESIAN_POINT('Ctrl Pts',(15.1831310850357,15.4243858145872,4.89454754315068));
#131626=CARTESIAN_POINT('Ctrl Pts',(15.1841547619693,15.4339078788635,4.90132650367367));
#131627=CARTESIAN_POINT('Ctrl Pts',(15.1851662734444,15.4432526645573,4.90832712317662));
#131628=CARTESIAN_POINT('Ctrl Pts',(15.1851675325333,15.4432642965713,4.90833583726666));
#131629=CARTESIAN_POINT('Ctrl Pts',(15.1851687916053,15.4432759283351,4.9083445517171));
#131630=CARTESIAN_POINT('Ctrl Pts',(15.1851700506604,15.4432875598486,4.90835326652794));
#131631=CARTESIAN_POINT('Ctrl Pts',(15.1877588052003,15.4672032188393,4.92627186700164));
#131632=CARTESIAN_POINT('Ctrl Pts',(15.1902762897157,15.4900621955577,4.94571827013843));
#131633=CARTESIAN_POINT('Ctrl Pts',(15.1927634673064,15.5116757036713,4.96652956978407));
#131634=CARTESIAN_POINT('Ctrl Pts',(15.1930201247306,15.5139060499653,4.96867713439024));
#131635=CARTESIAN_POINT('Ctrl Pts',(15.1932764594274,15.5161231228628,4.9708391888316));
#131636=CARTESIAN_POINT('Ctrl Pts',(15.1935325164093,15.5183267084219,4.97301552329867));
#131637=CARTESIAN_POINT('Ctrl Pts',(15.196266798539,15.5418575044603,4.99625532092931));
#131638=CARTESIAN_POINT('Ctrl Pts',(15.1989702506808,15.5638520715764,5.02112879029918));
#131639=CARTESIAN_POINT('Ctrl Pts',(15.2016898479807,15.5841012741654,5.04738590659609));
#131640=CARTESIAN_POINT('Ctrl Pts',(15.2044066420413,15.6043296047826,5.07361595823274));
#131641=CARTESIAN_POINT('Ctrl Pts',(15.2071400285388,15.6228165004013,5.10122634451727));
#131642=CARTESIAN_POINT('Ctrl Pts',(15.2099192223221,15.6393927389725,5.12994896158249));
#131643=CARTESIAN_POINT('Ctrl Pts',(15.2126970914321,15.6559610766546,5.15865788831575));
#131644=CARTESIAN_POINT('Ctrl Pts',(15.2155209489576,15.6706208002561,5.1884777586313));
#131645=CARTESIAN_POINT('Ctrl Pts',(15.2183971683278,15.6832379692582,5.21912704786309));
#131646=CARTESIAN_POINT('Ctrl Pts',(15.2212757395646,15.695865455241,5.24980139882803));
#131647=CARTESIAN_POINT('Ctrl Pts',(15.2242067999771,15.7064471222298,5.28130646226646));
#131648=CARTESIAN_POINT('Ctrl Pts',(15.2271719187527,15.7148815470349,5.3133483479334));
#131649=CARTESIAN_POINT('Ctrl Pts',(15.2301384567909,15.7233200090017,5.3454055705418));
#131650=CARTESIAN_POINT('Ctrl Pts',(15.2331389229045,15.7296090546103,5.37800022275787));
#131651=CARTESIAN_POINT('Ctrl Pts',(15.2361308774017,15.7336801813444,5.41082608756029));
#131652=CARTESIAN_POINT('Ctrl Pts',(15.2391286339414,15.7377592028676,5.44371560876512));
#131653=CARTESIAN_POINT('Ctrl Pts',(15.2421173732762,15.7396112172276,5.47683743517485));
#131654=CARTESIAN_POINT('Ctrl Pts',(15.2450349517313,15.7392048101568,5.50986930580845));
#131655=CARTESIAN_POINT('Ctrl Pts',(15.2460676728476,15.7390609562141,5.52156143708696));
#131656=CARTESIAN_POINT('Ctrl Pts',(15.2470913381354,15.738634521863,5.53324215314183));
#131657=CARTESIAN_POINT('Ctrl Pts',(15.2481028382458,15.7379254733588,5.54489667652789));
#131658=CARTESIAN_POINT('Ctrl Pts',(15.2481040973284,15.7379245907582,5.54491118370096));
#131659=CARTESIAN_POINT('Ctrl Pts',(15.2481053563941,15.737923707719,5.54492569086321));
#131660=CARTESIAN_POINT('Ctrl Pts',(15.2481066154429,15.7379228242412,5.54494019801461));
#131661=CARTESIAN_POINT('Ctrl Pts',(15.2506953696104,15.7361062887758,5.57476862677589));
#131662=CARTESIAN_POINT('Ctrl Pts',(15.2532128538165,15.7324326186822,5.60455452190264));
#131663=CARTESIAN_POINT('Ctrl Pts',(15.2557000311894,15.7269340777126,5.63405062287497));
#131664=CARTESIAN_POINT('Ctrl Pts',(15.2559566880301,15.7263666721993,5.63709438492113));
#131665=CARTESIAN_POINT('Ctrl Pts',(15.2562130221458,15.7257798655446,5.64013502756024));
#131666=CARTESIAN_POINT('Ctrl Pts',(15.2564690785486,15.7251737153565,5.64317225673248));
#131667=CARTESIAN_POINT('Ctrl Pts',(15.2592033599,15.7187009806899,5.675605107434));
#131668=CARTESIAN_POINT('Ctrl Pts',(15.2619068113793,15.7100190027675,5.70765309131112));
#131669=CARTESIAN_POINT('Ctrl Pts',(15.2646264081145,15.699221622836,5.73900404841786));
#131670=CARTESIAN_POINT('Ctrl Pts',(15.2673432016053,15.6884353723836,5.77032269029389));
#131671=CARTESIAN_POINT('Ctrl Pts',(15.2700765876299,15.675538647215,5.80094576630405));
#131672=CARTESIAN_POINT('Ctrl Pts',(15.2728557810128,15.6606623359664,5.83058451380219));
#131673=CARTESIAN_POINT('Ctrl Pts',(15.2756336497183,15.6457931153766,5.86020913426015));
#131674=CARTESIAN_POINT('Ctrl Pts',(15.2784575069112,15.6289465071931,5.88885042484307));
#131675=CARTESIAN_POINT('Ctrl Pts',(15.281333725998,15.6102840096509,5.91624171263645));
#131676=CARTESIAN_POINT('Ctrl Pts',(15.2842122969514,15.5916062518994,5.94365539811724));
#131677=CARTESIAN_POINT('Ctrl Pts',(15.2871433571296,15.5711097293887,5.96981706546049));
#131678=CARTESIAN_POINT('Ctrl Pts',(15.2901084757038,15.5489841486601,5.9944804028846));
#131679=CARTESIAN_POINT('Ctrl Pts',(15.29307501354,15.5268479774629,6.01915554548136));
#131680=CARTESIAN_POINT('Ctrl Pts',(15.2960754794847,15.5030810452484,6.04233087613006));
#131681=CARTESIAN_POINT('Ctrl Pts',(15.2990674338381,15.4779014562307,6.06378080242425));
#131682=CARTESIAN_POINT('Ctrl Pts',(15.3020651902414,15.4526730385167,6.08527232478803));
#131683=CARTESIAN_POINT('Ctrl Pts',(15.3050539294653,15.4260260541295,6.10503145249076));
#131684=CARTESIAN_POINT('Ctrl Pts',(15.3079715078339,15.3982124013273,6.12285474959797));
#131685=CARTESIAN_POINT('Ctrl Pts',(15.3090042333416,15.3883672951876,6.12916360277261));
#131686=CARTESIAN_POINT('Ctrl Pts',(15.3100279029465,15.3783763441575,6.13523014918259));
#131687=CARTESIAN_POINT('Ctrl Pts',(15.3110394072595,15.3682518728438,6.14104623508441));
#131688=CARTESIAN_POINT('Ctrl Pts',(15.3110406663469,15.3682392702335,6.14105347475766));
#131689=CARTESIAN_POINT('Ctrl Pts',(15.3110419254175,15.3682266673911,6.14106071405862));
#131690=CARTESIAN_POINT('Ctrl Pts',(15.3110431844712,15.3682140643165,6.14106795298725));
#131691=CARTESIAN_POINT('Ctrl Pts',(15.3136319384367,15.3423007464737,6.15595199240796));
#131692=CARTESIAN_POINT('Ctrl Pts',(15.31614942238,15.3154018000945,6.1692614549191));
#131693=CARTESIAN_POINT('Ctrl Pts',(15.3186365994219,15.2877414922757,6.18088733164246));
#131694=CARTESIAN_POINT('Ctrl Pts',(15.3188932565782,15.284887165532,6.1820870309035));
#131695=CARTESIAN_POINT('Ctrl Pts',(15.3191495910078,15.282024776462,6.1832688099034));
#131696=CARTESIAN_POINT('Ctrl Pts',(15.3194056477232,15.2791546023593,6.18443255506905));
#131697=CARTESIAN_POINT('Ctrl Pts',(15.3221399290356,15.2485056760054,6.19685951545524));
#131698=CARTESIAN_POINT('Ctrl Pts',(15.3248433803914,15.2169634492227,6.20722956257817));
#131699=CARTESIAN_POINT('Ctrl Pts',(15.3275629769416,15.1848402558027,6.21544943543967));
#131700=CARTESIAN_POINT('Ctrl Pts',(15.330279770244,15.1527501736423,6.22366083559609));
#131701=CARTESIAN_POINT('Ctrl Pts',(15.3330131560189,15.1200806139098,6.2297269803529));
#131702=CARTESIAN_POINT('Ctrl Pts',(15.3357923491187,15.0871447382741,6.2335984180491));
#131703=CARTESIAN_POINT('Ctrl Pts',(15.3385702175381,15.0542245612634,6.2374680104551));
#131704=CARTESIAN_POINT('Ctrl Pts',(15.3413940744116,15.0210384430784,6.23914528121923));
#131705=CARTESIAN_POINT('Ctrl Pts',(15.3442702931754,14.9878979255697,6.23861849181247));
#131706=CARTESIAN_POINT('Ctrl Pts',(15.3471488638016,14.9547303093106,6.23809127165399));
#131707=CARTESIAN_POINT('Ctrl Pts',(15.350079923649,14.9216083960125,6.23535648147473));
#131708=CARTESIAN_POINT('Ctrl Pts',(15.3530450419179,14.8888422311719,6.23043713969165));
#131709=CARTESIAN_POINT('Ctrl Pts',(15.356011579446,14.8560603827466,6.22551544325663));
#131710=CARTESIAN_POINT('Ctrl Pts',(15.3590120451082,14.8236345843641,6.21840695804047));
#131711=CARTESIAN_POINT('Ctrl Pts',(15.3620039992297,14.7918731900644,6.20916981455404));
#131712=CARTESIAN_POINT('Ctrl Pts',(15.3650017553981,14.7600502035432,6.19991475824611));
#131713=CARTESIAN_POINT('Ctrl Pts',(15.3679904944384,14.7288942102524,6.18852226373755));
#131714=CARTESIAN_POINT('Ctrl Pts',(15.3709080726904,14.6987136396494,6.17509087119461));
#131715=CARTESIAN_POINT('Ctrl Pts',(15.3719407988323,14.6880307165027,6.17033660275556));
#131716=CARTESIAN_POINT('Ctrl Pts',(15.3729644690679,14.6774699890325,6.16532728193802));
#131717=CARTESIAN_POINT('Ctrl Pts',(15.3739759740021,14.6670450445103,6.16006871962322));
#131718=CARTESIAN_POINT('Ctrl Pts',(15.3739772330885,14.6670320679001,6.16006217394677));
#131719=CARTESIAN_POINT('Ctrl Pts',(15.373978492158,14.6670190914731,6.16005562787173));
#131720=CARTESIAN_POINT('Ctrl Pts',(15.3739797512106,14.6670061152295,6.16004908139809));
#131721=CARTESIAN_POINT('Ctrl Pts',(15.3765685213135,14.6403253309968,6.1465887105774));
#131722=CARTESIAN_POINT('Ctrl Pts',(15.3790860205765,14.6144177854373,6.13143927358467));
#131723=CARTESIAN_POINT('Ctrl Pts',(15.3815732127602,14.589497844783,6.11472815397399));
#131724=CARTESIAN_POINT('Ctrl Pts',(15.3818301718085,14.5869232933363,6.11300167967105));
#131725=CARTESIAN_POINT('Ctrl Pts',(15.3820868073725,14.5843593016485,6.11125857862862));
#131726=CARTESIAN_POINT('Ctrl Pts',(15.3823431646236,14.5818061179262,6.10949902060918));
#131727=CARTESIAN_POINT('Ctrl Pts',(15.3850775311863,14.5545732615545,6.09073116211081));
#131728=CARTESIAN_POINT('Ctrl Pts',(15.3877810720171,14.5285673908074,6.07008605612694));
#131729=CARTESIAN_POINT('Ctrl Pts',(15.3905007651949,14.5040381616394,6.04777332771944));
#131730=CARTESIAN_POINT('Ctrl Pts',(15.3932180794694,14.479530388077,6.02548011615447));
#131731=CARTESIAN_POINT('Ctrl Pts',(15.3959519991338,14.4564964272674,6.00152271037857));
#131732=CARTESIAN_POINT('Ctrl Pts',(15.398731750532,14.435149891367,5.97613562952543));
#131733=CARTESIAN_POINT('Ctrl Pts',(15.4015099804942,14.4138150390255,5.95076244373483));
#131734=CARTESIAN_POINT('Ctrl Pts',(15.4043342166437,14.3941655856131,5.92396141030448));
#131735=CARTESIAN_POINT('Ctrl Pts',(15.4072108249875,14.3763826913015,5.89598639120007));
#131736=CARTESIAN_POINT('Ctrl Pts',(15.4100893512336,14.358587940717,5.86799272049417));
#131737=CARTESIAN_POINT('Ctrl Pts',(15.4130203605021,14.3426621732482,5.83882357447615));
#131738=CARTESIAN_POINT('Ctrl Pts',(15.4159854127,14.3287566151184,5.80875056030614));
#131739=CARTESIAN_POINT('Ctrl Pts',(15.4179145687271,14.3197092225317,5.7891841133556));
#131740=CARTESIAN_POINT('Ctrl Pts',(15.4198576101616,14.311516429361,5.76923536980049));
#131741=CARTESIAN_POINT('Ctrl Pts',(15.4218039449478,14.3042130192439,5.74898305934474));
#131742=CARTESIAN_POINT('Origin',(13.2437274406976,15.,5.5));
#131743=CARTESIAN_POINT('',(15.901560926295,14.3042076642396,5.74898599458007));
#131744=CARTESIAN_POINT('',(15.8222092530609,14.3040405757782,5.74907393379149));
#131745=CARTESIAN_POINT('',(13.2437274406976,14.3042076641721,5.74898599439144));
#131746=CARTESIAN_POINT('Ctrl Pts',(15.901560926295,14.3042076642395,5.74898599457988));
#131747=CARTESIAN_POINT('Ctrl Pts',(15.9010190912704,14.306350730213,5.75497480082541));
#131748=CARTESIAN_POINT('Ctrl Pts',(15.9004756543572,14.3085674346765,5.76092615949075));
#131749=CARTESIAN_POINT('Ctrl Pts',(15.8993204802887,14.3134192632855,5.77345558730921));
#131750=CARTESIAN_POINT('Ctrl Pts',(15.8987090507264,14.3160688926906,5.78001660504494));
#131751=CARTESIAN_POINT('Ctrl Pts',(15.8969222802899,14.324044718264,5.79897754145352));
#131752=CARTESIAN_POINT('Ctrl Pts',(15.895738944638,14.3296165653406,5.81127015873152));
#131753=CARTESIAN_POINT('Ctrl Pts',(15.8899081820006,14.3584484064902,5.87050946718659));
#131754=CARTESIAN_POINT('Ctrl Pts',(15.8851092827127,14.3863156565981,5.91503639228237));
#131755=CARTESIAN_POINT('Ctrl Pts',(15.8773481532337,14.4384402854192,5.98145562301003));
#131756=CARTESIAN_POINT('Ctrl Pts',(15.8744072089615,14.4598552502085,6.00536411943401));
#131757=CARTESIAN_POINT('Ctrl Pts',(15.8707154059179,14.4893356864558,6.03425442147313));
#131758=CARTESIAN_POINT('Ctrl Pts',(15.8698980696092,14.4960342086426,6.04057777710842));
#131759=CARTESIAN_POINT('Ctrl Pts',(15.8686221836898,14.5067823201493,6.05035040832505));
#131760=CARTESIAN_POINT('Ctrl Pts',(15.8681581404396,14.5107536330575,6.05388378710459));
#131761=CARTESIAN_POINT('Ctrl Pts',(15.867245212566,14.5186953561192,6.06079766773829));
#131762=CARTESIAN_POINT('Ctrl Pts',(15.8667962564223,14.5226640760234,6.06417958535731));
#131763=CARTESIAN_POINT('Ctrl Pts',(15.8656048051966,14.5333567489225,6.07309765957925));
#131764=CARTESIAN_POINT('Ctrl Pts',(15.8648673489293,14.5401436239582,6.07855767678657));
#131765=CARTESIAN_POINT('Ctrl Pts',(15.8605185610571,14.5810764755566,6.11031246912124));
#131766=CARTESIAN_POINT('Ctrl Pts',(15.857060372767,14.6173778428562,6.13370312014058));
#131767=CARTESIAN_POINT('Ctrl Pts',(15.8511441067054,14.6824011018498,6.16796361242261));
#131768=CARTESIAN_POINT('Ctrl Pts',(15.8486984505258,14.710132281052,6.18045644194394));
#131769=CARTESIAN_POINT('Ctrl Pts',(15.8454071429745,14.7477255601951,6.19467603423283));
#131770=CARTESIAN_POINT('Ctrl Pts',(15.8446000858053,14.7569665060866,6.19796267237899));
#131771=CARTESIAN_POINT('Ctrl Pts',(15.842564223519,14.7802913079684,6.20573900734019));
#131772=CARTESIAN_POINT('Ctrl Pts',(15.841329533632,14.7944488959244,6.20999164788247));
#131773=CARTESIAN_POINT('Ctrl Pts',(15.8393035330068,14.8176218302293,6.21620113677814));
#131774=CARTESIAN_POINT('Ctrl Pts',(15.838520584489,14.8265634940413,6.21841883843111));
#131775=CARTESIAN_POINT('Ctrl Pts',(15.8369837408856,14.8440717595613,6.22241532247205));
#131776=CARTESIAN_POINT('Ctrl Pts',(15.8362304960068,14.852633132112,6.22421026383182));
#131777=CARTESIAN_POINT('Ctrl Pts',(15.8343761980905,14.8736469091048,6.22822789533029));
#131778=CARTESIAN_POINT('Ctrl Pts',(15.8332701611456,14.8861279062051,6.23028355744324));
#131779=CARTESIAN_POINT('Ctrl Pts',(15.8271812992151,14.9544922819002,6.23974836629611));
#131780=CARTESIAN_POINT('Ctrl Pts',(15.8220148474509,15.0110203090233,6.24106312870786));
#131781=CARTESIAN_POINT('Ctrl Pts',(15.8140122770399,15.0977367820379,6.23315265306898));
#131782=CARTESIAN_POINT('Ctrl Pts',(15.8111966503182,15.128138367114,6.22845469237488));
#131783=CARTESIAN_POINT('Ctrl Pts',(15.8076388507702,15.1670127164,6.21993739392308));
#131784=CARTESIAN_POINT('Ctrl Pts',(15.8068350942062,15.1758278124639,6.21783542815829));
#131785=CARTESIAN_POINT('Ctrl Pts',(15.8055753332943,15.1897200219132,6.21425152714977));
#131786=CARTESIAN_POINT('Ctrl Pts',(15.8051140520987,15.1948233720841,6.21287641978269));
#131787=CARTESIAN_POINT('Ctrl Pts',(15.8042570696595,15.204341415113,6.21020191288035));
#131788=CARTESIAN_POINT('Ctrl Pts',(15.8038606365126,15.2087595092214,6.20891582127889));
#131789=CARTESIAN_POINT('Ctrl Pts',(15.8027689692013,15.220959296157,6.20524055885781));
#131790=CARTESIAN_POINT('Ctrl Pts',(15.8020784453792,15.2287143004552,6.20276385968532));
#131791=CARTESIAN_POINT('Ctrl Pts',(15.7973192442402,15.282310802889,6.18466558542474));
#131792=CARTESIAN_POINT('Ctrl Pts',(15.7934517162254,15.3265679096676,6.1646963915172));
#131793=CARTESIAN_POINT('Ctrl Pts',(15.7867439009506,15.3987646129057,6.12315513103539));
#131794=CARTESIAN_POINT('Ctrl Pts',(15.7839294568019,15.427701106077,6.10366126042322));
#131795=CARTESIAN_POINT('Ctrl Pts',(15.7797768741851,15.4672646645769,6.07273126308239));
#131796=CARTESIAN_POINT('Ctrl Pts',(15.7784940641908,15.4790774543958,6.06288728274005));
#131797=CARTESIAN_POINT('Ctrl Pts',(15.7764102060157,15.4975455259033,6.04649459892924));
#131798=CARTESIAN_POINT('Ctrl Pts',(15.7756184840612,15.5043990884787,6.04017537883108));
#131799=CARTESIAN_POINT('Ctrl Pts',(15.7740696678275,15.5174783137206,6.02764991510521));
#131800=CARTESIAN_POINT('Ctrl Pts',(15.7733133078616,15.5237164035921,6.02145886911737));
#131801=CARTESIAN_POINT('Ctrl Pts',(15.7714817724414,15.5384553983814,6.0062997565654));
#131802=CARTESIAN_POINT('Ctrl Pts',(15.7704021037596,15.5468443575775,5.99722717935986));
#131803=CARTESIAN_POINT('Ctrl Pts',(15.7641627705108,15.5935830044438,5.9440658717889));
#131804=CARTESIAN_POINT('Ctrl Pts',(15.7588025787515,15.6268161495871,5.89577003024519));
#131805=CARTESIAN_POINT('Ctrl Pts',(15.7507180476973,15.6677859271082,5.81789665067658));
#131806=CARTESIAN_POINT('Ctrl Pts',(15.7480099981808,15.6799778555234,5.79090686942623));
#131807=CARTESIAN_POINT('Ctrl Pts',(15.7445678118916,15.6936997237978,5.75491447568632));
#131808=CARTESIAN_POINT('Ctrl Pts',(15.743776190196,15.6967287314128,5.74651530092497));
#131809=CARTESIAN_POINT('Ctrl Pts',(15.7425308521589,15.7012987426797,5.73308521615288));
#131810=CARTESIAN_POINT('Ctrl Pts',(15.742072049724,15.7029394151296,5.72808951879469));
#131811=CARTESIAN_POINT('Ctrl Pts',(15.7412160550945,15.7059210373339,5.71867287229715));
#131812=CARTESIAN_POINT('Ctrl Pts',(15.7408181712773,15.7072741113623,5.71425608763402));
#131813=CARTESIAN_POINT('Ctrl Pts',(15.7397162535129,15.7109266705092,5.7019213794533));
#131814=CARTESIAN_POINT('Ctrl Pts',(15.7390170834389,15.7131352992562,5.69397689857699));
#131815=CARTESIAN_POINT('Ctrl Pts',(15.73432834209,15.7271682758949,5.64001605048752));
#131816=CARTESIAN_POINT('Ctrl Pts',(15.7305310489525,15.7346659320182,5.5929818598551));
#131817=CARTESIAN_POINT('Ctrl Pts',(15.7235690116083,15.73999487045,5.50668397483167));
#131818=CARTESIAN_POINT('Ctrl Pts',(15.7204252805073,15.7393193074721,5.46769670588419));
#131819=CARTESIAN_POINT('Ctrl Pts',(15.7160592723548,15.734263861582,5.4153601122154));
#131820=CARTESIAN_POINT('Ctrl Pts',(15.7149162485942,15.7325753183973,5.40181301453608));
#131821=CARTESIAN_POINT('Ctrl Pts',(15.7129999858034,15.7291516524742,5.37941813497513));
#131822=CARTESIAN_POINT('Ctrl Pts',(15.7122333806722,15.7276279850374,5.37054105394538));
#131823=CARTESIAN_POINT('Ctrl Pts',(15.7106896388498,15.7242563918933,5.35284413076323));
#131824=CARTESIAN_POINT('Ctrl Pts',(15.7099126310405,15.7224086223868,5.34402584292082));
#131825=CARTESIAN_POINT('Ctrl Pts',(15.707943983482,15.7173532945442,5.32192128758176));
#131826=CARTESIAN_POINT('Ctrl Pts',(15.7067460308474,15.7139376416921,5.30868673148448));
#131827=CARTESIAN_POINT('Ctrl Pts',(15.7014591269118,15.6974073647799,5.25126728076949));
#131828=CARTESIAN_POINT('Ctrl Pts',(15.69725718942,15.6805447449814,5.20827688946693));
#131829=CARTESIAN_POINT('Ctrl Pts',(15.6894208780699,15.6421426175256,5.13215544570545));
#131830=CARTESIAN_POINT('Ctrl Pts',(15.6858099063898,15.6217346401265,5.09862314291903));
#131831=CARTESIAN_POINT('Ctrl Pts',(15.6815177101152,15.5935758700741,5.05969673935276));
#131832=CARTESIAN_POINT('Ctrl Pts',(15.6807333565859,15.5882617040098,5.05262156511884));
#131833=CARTESIAN_POINT('Ctrl Pts',(15.6794966561937,15.5795987355904,5.04150923696917));
#131834=CARTESIAN_POINT('Ctrl Pts',(15.6790393356279,15.5763320199259,5.0374095952544));
#131835=CARTESIAN_POINT('Ctrl Pts',(15.6781271835534,15.5696846613527,5.02924707667916));
#131836=CARTESIAN_POINT('Ctrl Pts',(15.6776724222115,15.5663035097473,5.02518501657882));
#131837=CARTESIAN_POINT('Ctrl Pts',(15.6764457854826,15.5570086501147,5.01425887489405));
#131838=CARTESIAN_POINT('Ctrl Pts',(15.6756794860002,15.5510115820901,5.00746641086904));
#131839=CARTESIAN_POINT('Ctrl Pts',(15.6716645065889,15.518660045634,4.97215483501962));
#131840=CARTESIAN_POINT('Ctrl Pts',(15.6685364360735,15.4902097312988,4.94563184997997));
#131841=CARTESIAN_POINT('Ctrl Pts',(15.6619999284044,15.4266539133024,4.89511954841005));
#131842=CARTESIAN_POINT('Ctrl Pts',(15.6586018071178,15.3913056073004,4.87167417419855));
#131843=CARTESIAN_POINT('Ctrl Pts',(15.6538154691473,15.3404796579314,4.84392296378181));
#131844=CARTESIAN_POINT('Ctrl Pts',(15.6525166773131,15.3265811729723,4.83689507318885));
#131845=CARTESIAN_POINT('Ctrl Pts',(15.6504135864206,15.3039914842732,4.82635487462265));
#131846=CARTESIAN_POINT('Ctrl Pts',(15.6496189427168,15.2954369557246,4.82255954814017));
#131847=CARTESIAN_POINT('Ctrl Pts',(15.6480687490371,15.2787290032232,4.81552349599436));
#131848=CARTESIAN_POINT('Ctrl Pts',(15.6473139943061,15.270585361286,4.8122635027787));
#131849=CARTESIAN_POINT('Ctrl Pts',(15.6454938928568,15.2509389101029,4.8048017541583));
#131850=CARTESIAN_POINT('Ctrl Pts',(15.6444241997129,15.2393863232312,4.80073961452834));
#131851=CARTESIAN_POINT('Ctrl Pts',(15.6381294417354,15.1714237059104,4.7787239738254));
#131852=CARTESIAN_POINT('Ctrl Pts',(15.6326973553008,15.1131315559367,4.76731763296795));
#131853=CARTESIAN_POINT('Ctrl Pts',(15.6245815824239,15.0250248309666,4.76084790327428));
#131854=CARTESIAN_POINT('Ctrl Pts',(15.621912349062,14.9958260197347,4.76043593965468));
#131855=CARTESIAN_POINT('Ctrl Pts',(15.6185120151877,14.9578077307438,4.76215202850299));
#131856=CARTESIAN_POINT('Ctrl Pts',(15.6177248847222,14.9489461998596,4.76271216757074));
#131857=CARTESIAN_POINT('Ctrl Pts',(15.616484884843,14.9348658291116,4.76385729725892));
#131858=CARTESIAN_POINT('Ctrl Pts',(15.6160269988506,14.9296397474941,4.76433840696036));
#131859=CARTESIAN_POINT('Ctrl Pts',(15.6151148265101,14.9191684264645,4.76541500398255));
#131860=CARTESIAN_POINT('Ctrl Pts',(15.6146605973175,14.9139235589778,4.76601109587703));
#131861=CARTESIAN_POINT('Ctrl Pts',(15.6134371707002,14.8997267705813,4.76777887313962));
#131862=CARTESIAN_POINT('Ctrl Pts',(15.6126734997449,14.8907888279233,4.76905852359377));
#131863=CARTESIAN_POINT('Ctrl Pts',(15.6087034449563,14.844048107674,4.77662701672887));
#131864=CARTESIAN_POINT('Ctrl Pts',(15.6056145689812,14.8067483662577,4.78568626445037));
#131865=CARTESIAN_POINT('Ctrl Pts',(15.5998676150899,14.738911608855,4.80786887622241));
#131866=CARTESIAN_POINT('Ctrl Pts',(15.5972155188678,14.7082337112476,4.82023173734152));
#131867=CARTESIAN_POINT('Ctrl Pts',(15.5932730728649,14.6648178000812,4.84120992372543));
#131868=CARTESIAN_POINT('Ctrl Pts',(15.5920227810439,14.6513562063296,4.84823399674612));
#131869=CARTESIAN_POINT('Ctrl Pts',(15.5896861642823,14.6268708246815,4.86198580402747));
#131870=CARTESIAN_POINT('Ctrl Pts',(15.5886038061238,14.6157885938362,4.86859755293151));
#131871=CARTESIAN_POINT('Ctrl Pts',(15.5867594510494,14.597384133368,4.88024176932054));
#131872=CARTESIAN_POINT('Ctrl Pts',(15.5860030170607,14.5899689897489,4.88512248649213));
#131873=CARTESIAN_POINT('Ctrl Pts',(15.5845485893017,14.5759765400734,4.89469811029625));
#131874=CARTESIAN_POINT('Ctrl Pts',(15.5838515498125,14.5693847607987,4.89936968382915));
#131875=CARTESIAN_POINT('Ctrl Pts',(15.5819814551295,14.5520117130343,4.9121148997504));
#131876=CARTESIAN_POINT('Ctrl Pts',(15.5808014029495,14.5413728983271,4.92037639269052));
#131877=CARTESIAN_POINT('Ctrl Pts',(15.5752414288283,14.4927873596902,4.96028040105452));
#131878=CARTESIAN_POINT('Ctrl Pts',(15.5707282547691,14.4578560089472,4.99538131067525));
#131879=CARTESIAN_POINT('Ctrl Pts',(15.5628121500631,14.4035241476881,5.06218069271082));
#131880=CARTESIAN_POINT('Ctrl Pts',(15.5594355344606,14.3825082743107,5.09235589864732));
#131881=CARTESIAN_POINT('Ctrl Pts',(15.5553877287887,14.3594366857689,5.13138924417488));
#131882=CARTESIAN_POINT('Ctrl Pts',(15.5546243149542,14.3551819463905,5.13888374911916));
#131883=CARTESIAN_POINT('Ctrl Pts',(15.5534124617848,14.3485734599106,5.15101367562257));
#131884=CARTESIAN_POINT('Ctrl Pts',(15.5529593695649,14.3461359610775,5.15560224076619));
#131885=CARTESIAN_POINT('Ctrl Pts',(15.5520470652589,14.3412931010373,5.16495566981849));
#131886=CARTESIAN_POINT('Ctrl Pts',(15.5515880253884,14.3388905716795,5.16972161546449));
#131887=CARTESIAN_POINT('Ctrl Pts',(15.5503355135044,14.332436059173,5.182878262787));
#131888=CARTESIAN_POINT('Ctrl Pts',(15.5495480222946,14.3284906143905,5.19132058498329));
#131889=CARTESIAN_POINT('Ctrl Pts',(15.5457817983754,14.310227132208,5.23240886148132));
#131890=CARTESIAN_POINT('Ctrl Pts',(15.5429020260804,14.2981223222434,5.26599135512854));
#131891=CARTESIAN_POINT('Ctrl Pts',(15.537254796242,14.2791807946754,5.33348518422662));
#131892=CARTESIAN_POINT('Ctrl Pts',(15.5344934406337,14.2722040533432,5.36725815972864));
#131893=CARTESIAN_POINT('Ctrl Pts',(15.5308147946604,14.2661962629926,5.41188048874733));
#131894=CARTESIAN_POINT('Ctrl Pts',(15.5299459220278,14.265009784337,5.42239627363822));
#131895=CARTESIAN_POINT('Ctrl Pts',(15.5277834975326,14.2626353941577,5.44845151526249));
#131896=CARTESIAN_POINT('Ctrl Pts',(15.5264838396102,14.261712521617,5.46400918246762));
#131897=CARTESIAN_POINT('Ctrl Pts',(15.5243797063117,14.2610234839208,5.48894002377559));
#131898=CARTESIAN_POINT('Ctrl Pts',(15.5235849042555,14.2609426892394,5.49830030569007));
#131899=CARTESIAN_POINT('Ctrl Pts',(15.5220346326109,14.2611305938584,5.51642945676641));
#131900=CARTESIAN_POINT('Ctrl Pts',(15.5212799615315,14.2613776184711,5.52519701311198));
#131901=CARTESIAN_POINT('Ctrl Pts',(15.5194604612362,14.2623430014501,5.5461838443705));
#131902=CARTESIAN_POINT('Ctrl Pts',(15.5183912932982,14.2632089988482,5.55839329141341));
#131903=CARTESIAN_POINT('Ctrl Pts',(15.5120936328619,14.2700347783098,5.62954040220463));
#131904=CARTESIAN_POINT('Ctrl Pts',(15.5066577747397,14.282760120173,5.68760036365243));
#131905=CARTESIAN_POINT('Ctrl Pts',(15.5010403239809,14.3029090446194,5.74533437517337));
#131906=CARTESIAN_POINT('Ctrl Pts',(15.5008623455759,14.3035547805997,5.74716150870291));
#131907=CARTESIAN_POINT('Ctrl Pts',(15.5006844331709,14.3042076645986,5.7489859955834));
#131908=CARTESIAN_POINT('',(15.4440687571878,14.2608033075753,5.50047868038583));
#131909=CARTESIAN_POINT('Ctrl Pts',(15.4218039449815,14.3042130191175,5.74898305899438));
#131910=CARTESIAN_POINT('Ctrl Pts',(15.424802386429,14.2929616929186,5.71778320195144));
#131911=CARTESIAN_POINT('Ctrl Pts',(15.4278094459352,14.2838229275677,5.68586179826189));
#131912=CARTESIAN_POINT('Ctrl Pts',(15.4307689392091,14.2768967474548,5.65352289190575));
#131913=CARTESIAN_POINT('Ctrl Pts',(15.4328487506394,14.2720293099464,5.63079642461635));
#131914=CARTESIAN_POINT('Ctrl Pts',(15.434904548357,14.2682540029085,5.6078641606579));
#131915=CARTESIAN_POINT('Ctrl Pts',(15.4369125409172,14.2655940059027,5.58483839126259));
#131916=CARTESIAN_POINT('Ctrl Pts',(15.4393520146978,14.2623624237341,5.55686480120453));
#131917=CARTESIAN_POINT('Ctrl Pts',(15.4417246722218,14.2607667042999,5.52869421490943));
#131918=CARTESIAN_POINT('Ctrl Pts',(15.4440687571363,14.2608033075744,5.5004786810059));
#131919=CARTESIAN_POINT('Ctrl Pts',(15.4440687571967,14.2608033075754,5.50047868027838));
#131920=CARTESIAN_POINT('Ctrl Pts',(15.4467761069373,14.2608455833229,5.46789056116125));
#131921=CARTESIAN_POINT('Ctrl Pts',(15.4494469348908,14.2630684344419,5.43522701256568));
#131922=CARTESIAN_POINT('Ctrl Pts',(15.4521278841484,14.2674494715339,5.40280611817825));
#131923=CARTESIAN_POINT('Ctrl Pts',(15.4548051655613,14.2718245148668,5.37042957927693));
#131924=CARTESIAN_POINT('Ctrl Pts',(15.4574930545461,14.2783512841037,5.33829519427106));
#131925=CARTESIAN_POINT('Ctrl Pts',(15.4602226997084,14.2869647716622,5.3067066159124));
#131926=CARTESIAN_POINT('Ctrl Pts',(15.4629502225471,14.2955715621569,5.27514259795625));
#131927=CARTESIAN_POINT('Ctrl Pts',(15.4657196952501,14.3062614877415,5.2441235989032));
#131928=CARTESIAN_POINT('Ctrl Pts',(15.4685412005376,14.3189337096865,5.21393790265118));
#131929=CARTESIAN_POINT('Ctrl Pts',(15.471364285272,14.3316130253987,5.18373530878646));
#131930=CARTESIAN_POINT('Ctrl Pts',(15.4742395361271,14.3462767111684,5.15436699216516));
#131931=CARTESIAN_POINT('Ctrl Pts',(15.4771535537219,14.3627913473154,5.12610630435767));
#131932=CARTESIAN_POINT('Ctrl Pts',(15.4800683726115,14.3793105246475,5.09783784544275));
#131933=CARTESIAN_POINT('Ctrl Pts',(15.4830218659706,14.3976817340025,5.07067768020242));
#131934=CARTESIAN_POINT('Ctrl Pts',(15.4859773680107,14.4177397040656,5.04488329105562));
#131935=CARTESIAN_POINT('Ctrl Pts',(15.4889386844745,14.4378371346109,5.01903815604416));
#131936=CARTESIAN_POINT('Ctrl Pts',(15.4919016374085,14.4596283158344,4.99456436472374));
#131937=CARTESIAN_POINT('Ctrl Pts',(15.4948095761129,14.4829120894533,4.97170310431067));
#131938=CARTESIAN_POINT('Ctrl Pts',(15.4965131315522,14.4965524042007,4.95831031014164));
#131939=CARTESIAN_POINT('Ctrl Pts',(15.4981974437974,14.5107042977867,4.94547060155898));
#131940=CARTESIAN_POINT('Ctrl Pts',(15.499849108333,14.5253208329636,4.93322896563607));
#131941=CARTESIAN_POINT('Ctrl Pts',(15.4998503674193,14.5253319753473,4.93321963367046));
#131942=CARTESIAN_POINT('Ctrl Pts',(15.4998516264888,14.5253431180245,4.93321030203082));
#131943=CARTESIAN_POINT('Ctrl Pts',(15.4998528855414,14.5253542609955,4.93320097071717));
#131944=CARTESIAN_POINT('Ctrl Pts',(15.5024416396342,14.5482654650402,4.91401473820545));
#131945=CARTESIAN_POINT('Ctrl Pts',(15.5049591237203,14.5724224611895,4.89620646031482));
#131946=CARTESIAN_POINT('Ctrl Pts',(15.50744630092,14.5976235007547,4.87992268447526));
#131947=CARTESIAN_POINT('Ctrl Pts',(15.5077029580282,14.6002240496569,4.8782423269934));
#131948=CARTESIAN_POINT('Ctrl Pts',(15.5079592924099,14.6028356704184,4.87657820375011));
#131949=CARTESIAN_POINT('Ctrl Pts',(15.5082153490777,14.6054581098794,4.8749304750595));
#131950=CARTESIAN_POINT('Ctrl Pts',(15.510949630506,14.6334616279128,4.85733533100091));
#131951=CARTESIAN_POINT('Ctrl Pts',(15.5136530819958,14.662704380166,4.84160919125144));
#131952=CARTESIAN_POINT('Ctrl Pts',(15.5163726786914,14.6928951544079,4.82789849849688));
#131953=CARTESIAN_POINT('Ctrl Pts',(15.5190894721413,14.7230548092714,4.81420193814694));
#131954=CARTESIAN_POINT('Ctrl Pts',(15.5218228580752,14.7541601598289,4.8025162421249));
#131955=CARTESIAN_POINT('Ctrl Pts',(15.5246020513376,14.78591151766,4.79294486361158));
#131956=CARTESIAN_POINT('Ctrl Pts',(15.5273799199213,14.8176477414778,4.78337804721402));
#131957=CARTESIAN_POINT('Ctrl Pts',(15.5302037769629,14.8500291864702,4.7759232651959));
#131958=CARTESIAN_POINT('Ctrl Pts',(15.5330799958899,14.8827511640677,4.77064655546633));
#131959=CARTESIAN_POINT('Ctrl Pts',(15.5359585666809,14.9154998981965,4.76536553100827));
#131960=CARTESIAN_POINT('Ctrl Pts',(15.5388896266881,14.9485896780001,4.76226605249483));
#131961=CARTESIAN_POINT('Ctrl Pts',(15.5418547451026,14.9817112101536,4.76137967478786));
#131962=CARTESIAN_POINT('Ctrl Pts',(15.5448212827776,15.0148485960011,4.76049287281426));
#131963=CARTESIAN_POINT('Ctrl Pts',(15.5478217485722,15.0480178284823,4.76182142709274));
#131964=CARTESIAN_POINT('Ctrl Pts',(15.5508137028031,15.0809051395052,4.76536202564308));
#131965=CARTESIAN_POINT('Ctrl Pts',(15.5538114590812,15.1138562261454,4.76890949018067));
#131966=CARTESIAN_POINT('Ctrl Pts',(15.5568001982077,15.1465243774485,4.77467809640339));
#131967=CARTESIAN_POINT('Ctrl Pts',(15.5597177765166,15.1785886845052,4.78262475853342));
#131968=CARTESIAN_POINT('Ctrl Pts',(15.5607505018425,15.1899383788234,4.78543761164969));
#131969=CARTESIAN_POINT('Ctrl Pts',(15.561774171273,15.2012123622676,4.78852295534572));
#131970=CARTESIAN_POINT('Ctrl Pts',(15.5627856754207,15.2123962407999,4.79187744433514));
#131971=CARTESIAN_POINT('Ctrl Pts',(15.5627869345069,15.2124101621135,4.79188161988956));
#131972=CARTESIAN_POINT('Ctrl Pts',(15.5627881935762,15.2124240833164,4.79188579586848));
#131973=CARTESIAN_POINT('Ctrl Pts',(15.5627894526286,15.2124380044084,4.79188997227193));
#131974=CARTESIAN_POINT('Ctrl Pts',(15.5653782067486,15.2410613434249,4.80047712991141));
#131975=CARTESIAN_POINT('Ctrl Pts',(15.5678956908651,15.2692187376239,4.81086252349366));
#131976=CARTESIAN_POINT('Ctrl Pts',(15.5703828680978,15.2966768492142,4.82295822031119));
#131977=CARTESIAN_POINT('Ctrl Pts',(15.570639525199,15.299510310068,4.82420640095606));
#131978=CARTESIAN_POINT('Ctrl Pts',(15.5708958595738,15.3023362990345,4.82547275596272));
#131979=CARTESIAN_POINT('Ctrl Pts',(15.5711519162349,15.3051545430087,4.82675716202661));
#131980=CARTESIAN_POINT('Ctrl Pts',(15.5738861976904,15.3352489455728,4.84047259386885));
#131981=CARTESIAN_POINT('Ctrl Pts',(15.5765896492107,15.3644636433141,4.8562507903979));
#131982=CARTESIAN_POINT('Ctrl Pts',(15.5793092459387,15.3925161939256,4.8739290360027));
#131983=CARTESIAN_POINT('Ctrl Pts',(15.5820260394214,15.4205398291541,4.8915890596195));
#131984=CARTESIAN_POINT('Ctrl Pts',(15.5847594253902,15.447403865845,4.91114466944784));
#131985=CARTESIAN_POINT('Ctrl Pts',(15.5875386186879,15.4728571084234,4.93240243204717));
#131986=CARTESIAN_POINT('Ctrl Pts',(15.5903164873072,15.498298218935,4.95365006231873));
#131987=CARTESIAN_POINT('Ctrl Pts',(15.5931403443849,15.5223300100993,4.97659793337382));
#131988=CARTESIAN_POINT('Ctrl Pts',(15.5960165633468,15.5447297884591,5.00102786236099));
#131989=CARTESIAN_POINT('Ctrl Pts',(15.598895134173,15.5671478829627,5.02547776753224));
#131990=CARTESIAN_POINT('Ctrl Pts',(15.6018261942143,15.5879313453698,5.05141206919082));
#131991=CARTESIAN_POINT('Ctrl Pts',(15.6047913126597,15.6068837525801,5.07858977762999));
#131992=CARTESIAN_POINT('Ctrl Pts',(15.6077578503658,15.6258452314031,5.1057804947409));
#131993=CARTESIAN_POINT('Ctrl Pts',(15.6107583161885,15.6429738229881,5.13421593755292));
#131994=CARTESIAN_POINT('Ctrl Pts',(15.6137502704426,15.6580997666351,5.16363220704589));
#131995=CARTESIAN_POINT('Ctrl Pts',(15.6167480267439,15.6732550427619,5.19310552105464));
#131996=CARTESIAN_POINT('Ctrl Pts',(15.6197367658887,15.6863995147595,5.22356381715342));
#131997=CARTESIAN_POINT('Ctrl Pts',(15.6226543442097,15.6973927169695,5.25471536204762));
#131998=CARTESIAN_POINT('Ctrl Pts',(15.6236870693484,15.7012839428522,5.26574196698586));
#131999=CARTESIAN_POINT('Ctrl Pts',(15.6247107385943,15.7049059383463,5.27685516403632));
#132000=CARTESIAN_POINT('Ctrl Pts',(15.6257222425617,15.7082535829996,5.28804109102039));
#132001=CARTESIAN_POINT('Ctrl Pts',(15.6257235016478,15.7082577500349,5.28805501488569));
#132002=CARTESIAN_POINT('Ctrl Pts',(15.625724760717,15.7082619166548,5.28806893889187));
#132003=CARTESIAN_POINT('Ctrl Pts',(15.6257260197694,15.7082660828591,5.2880828630389));
#132004=CARTESIAN_POINT('Ctrl Pts',(15.6283147738787,15.71683227034,5.31671248476454));
#132005=CARTESIAN_POINT('Ctrl Pts',(15.630832257985,15.7236402612103,5.34594169111475));
#132006=CARTESIAN_POINT('Ctrl Pts',(15.6333194352083,15.7286352001015,5.37552723412128));
#132007=CARTESIAN_POINT('Ctrl Pts',(15.6335760923015,15.7291506384404,5.37858022905785));
#132008=CARTESIAN_POINT('Ctrl Pts',(15.6338324266685,15.7296467880078,5.3816369762964));
#132009=CARTESIAN_POINT('Ctrl Pts',(15.6340884833215,15.7301236016266,5.38469717992357));
#132010=CARTESIAN_POINT('Ctrl Pts',(15.6368227647599,15.7352152194844,5.41737533092954));
#132011=CARTESIAN_POINT('Ctrl Pts',(15.6395262162643,15.7381001823414,5.45045292196372));
#132012=CARTESIAN_POINT('Ctrl Pts',(15.6422458129776,15.738759097609,5.48360457024803));
#132013=CARTESIAN_POINT('Ctrl Pts',(15.6449626064454,15.7394173336945,5.51672204721309));
#132014=CARTESIAN_POINT('Ctrl Pts',(15.6476959924004,15.7378546511993,5.54991325623536));
#132015=CARTESIAN_POINT('Ctrl Pts',(15.6504751856855,15.7340944960883,5.58286202331587));
#132016=CARTESIAN_POINT('Ctrl Pts',(15.653253054292,15.7303361332227,5.61579508565123));
#132017=CARTESIAN_POINT('Ctrl Pts',(15.6560769113579,15.7243827056555,5.64848588654057));
#132018=CARTESIAN_POINT('Ctrl Pts',(15.658953130309,15.7162940035838,5.68062845006448));
#132019=CARTESIAN_POINT('Ctrl Pts',(15.6618317011244,15.7081986874365,5.71279729633989));
#132020=CARTESIAN_POINT('Ctrl Pts',(15.6647627611558,15.6979647032516,5.74441700332746));
#132021=CARTESIAN_POINT('Ctrl Pts',(15.6677278795925,15.6856853357742,5.77519099721236));
#132022=CARTESIAN_POINT('Ctrl Pts',(15.6706944172898,15.67340009075,5.80597972113861));
#132023=CARTESIAN_POINT('Ctrl Pts',(15.6736948831047,15.6590673534345,5.83592192694714));
#132024=CARTESIAN_POINT('Ctrl Pts',(15.6766868373524,15.6428142042667,5.8647307140484));
#132025=CARTESIAN_POINT('Ctrl Pts',(15.6796845936473,15.6265295367228,5.89359536762682));
#132026=CARTESIAN_POINT('Ctrl Pts',(15.6826733327871,15.6083165017546,5.92132207483228));
#132027=CARTESIAN_POINT('Ctrl Pts',(15.6855909111045,15.5883415366898,5.94763309922456));
#132028=CARTESIAN_POINT('Ctrl Pts',(15.686623636346,15.5812710664653,5.95694632274894));
#132029=CARTESIAN_POINT('Ctrl Pts',(15.6876473056931,15.573980231511,5.96608228202831));
#132030=CARTESIAN_POINT('Ctrl Pts',(15.6886588097591,15.5664777948433,5.97502907795765));
#132031=CARTESIAN_POINT('Ctrl Pts',(15.6886600688453,15.566468456063,5.97504021462768));
#132032=CARTESIAN_POINT('Ctrl Pts',(15.6886613279146,15.5664591169365,5.97505135102813));
#132033=CARTESIAN_POINT('Ctrl Pts',(15.6886625869671,15.566449777464,5.97506248715896));
#132034=CARTESIAN_POINT('Ctrl Pts',(15.6912513410761,15.5472467664899,5.99795963052945));
#132035=CARTESIAN_POINT('Ctrl Pts',(15.6937688251809,15.526576192724,6.01971790758887));
#132036=CARTESIAN_POINT('Ctrl Pts',(15.6962560024016,15.5046110689217,6.04015774865318));
#132037=CARTESIAN_POINT('Ctrl Pts',(15.6965126595003,15.5023444411552,6.04226697925511));
#132038=CARTESIAN_POINT('Ctrl Pts',(15.6967689938728,15.5000640732066,6.04436216194234));
#132039=CARTESIAN_POINT('Ctrl Pts',(15.6970250505313,15.4977701863,6.04644309460028));
#132040=CARTESIAN_POINT('Ctrl Pts',(15.6997593319722,15.4732750904425,6.06866417480348));
#132041=CARTESIAN_POINT('Ctrl Pts',(15.7024627834775,15.4472330172999,6.08926175880403));
#132042=CARTESIAN_POINT('Ctrl Pts',(15.7051823801906,15.4199050829409,6.10804073529059));
#132043=CARTESIAN_POINT('Ctrl Pts',(15.7078991736582,15.392605317063,6.12680035520093));
#132044=CARTESIAN_POINT('Ctrl Pts',(15.7106325596118,15.3640227818022,6.14374547284348));
#132045=CARTESIAN_POINT('Ctrl Pts',(15.7134117528947,15.3344344565109,6.15872182172957));
#132046=CARTESIAN_POINT('Ctrl Pts',(15.7161896214991,15.3048602342394,6.17369103226823));
#132047=CARTESIAN_POINT('Ctrl Pts',(15.7190134785621,15.274281395181,6.18669358453111));
#132048=CARTESIAN_POINT('Ctrl Pts',(15.7218896975101,15.2429863847113,6.19761117637783));
#132049=CARTESIAN_POINT('Ctrl Pts',(15.7247682683224,15.211665784529,6.20853769546355));
#132050=CARTESIAN_POINT('Ctrl Pts',(15.7276993283503,15.1796279003228,6.21737592372426));
#132051=CARTESIAN_POINT('Ctrl Pts',(15.7306644467838,15.1471717414236,6.22404070546988));
#132052=CARTESIAN_POINT('Ctrl Pts',(15.7336309844779,15.1147000473112,6.23070867732821));
#132053=CARTESIAN_POINT('Ctrl Pts',(15.7366314502898,15.0818095912583,6.23520099846741));
#132054=CARTESIAN_POINT('Ctrl Pts',(15.739623404535,15.0488098856814,6.23746606025999));
#132055=CARTESIAN_POINT('Ctrl Pts',(15.7426211608274,15.0157461865294,6.23973551449787));
#132056=CARTESIAN_POINT('Ctrl Pts',(15.7456098999652,14.9825726452173,6.23976857485775));
#132057=CARTESIAN_POINT('Ctrl Pts',(15.7485274782814,14.9496127603104,6.23755154489927));
#132058=CARTESIAN_POINT('Ctrl Pts',(15.7495602035142,14.9379460624109,6.23676679037623));
#132059=CARTESIAN_POINT('Ctrl Pts',(15.7505838728528,14.9263062575021,6.23570050434283));
#132060=CARTESIAN_POINT('Ctrl Pts',(15.7515953769107,14.9147081028205,6.23435346340884));
#132061=CARTESIAN_POINT('Ctrl Pts',(15.7515966359968,14.9146936658287,6.23435178665771));
#132062=CARTESIAN_POINT('Ctrl Pts',(15.7515978950661,14.9146792288718,6.23435010946924));
#132063=CARTESIAN_POINT('Ctrl Pts',(15.7515991541185,14.9146647919497,6.23434843184341));
#132064=CARTESIAN_POINT('Ctrl Pts',(15.7541879082306,14.8849808480094,6.23089904346463));
#132065=CARTESIAN_POINT('Ctrl Pts',(15.756705392339,14.8554412061881,6.22559764700203));
#132066=CARTESIAN_POINT('Ctrl Pts',(15.7591925695637,14.8262909858308,6.21849001572236));
#132067=CARTESIAN_POINT('Ctrl Pts',(15.7594492266614,14.8232829127114,6.21775656416238));
#132068=CARTESIAN_POINT('Ctrl Pts',(15.7597055610327,14.8202790181393,6.21700391165846));
#132069=CARTESIAN_POINT('Ctrl Pts',(15.7599616176902,14.8172795925739,6.21623213185643));
#132070=CARTESIAN_POINT('Ctrl Pts',(15.7626958991342,14.7852504559489,6.20799074023513));
#132071=CARTESIAN_POINT('Ctrl Pts',(15.7653993506432,14.7537267468749,6.19756453245429));
#132072=CARTESIAN_POINT('Ctrl Pts',(15.7681189473603,14.7230150100721,6.18506432529857));
#132073=CARTESIAN_POINT('Ctrl Pts',(15.7708357408319,14.6923349296306,6.17257700282843));
#132074=CARTESIAN_POINT('Ctrl Pts',(15.7735691267899,14.662465092574,6.15802052075943));
#132075=CARTESIAN_POINT('Ctrl Pts',(15.7763483200773,14.6336866500919,6.14154140458493));
#132076=CARTESIAN_POINT('Ctrl Pts',(15.7791261886863,14.6049219246054,6.1250701430386));
#132077=CARTESIAN_POINT('Ctrl Pts',(15.7819500457541,14.5772474760076,6.10667838780921));
#132078=CARTESIAN_POINT('Ctrl Pts',(15.7848262647067,14.5509207205642,6.08654201668866));
#132079=CARTESIAN_POINT('Ctrl Pts',(15.7877048355236,14.5245724379154,6.06638918019703));
#132080=CARTESIAN_POINT('Ctrl Pts',(15.7906358955561,14.4995740184021,6.04448896725036));
#132081=CARTESIAN_POINT('Ctrl Pts',(15.7936010139937,14.4761610010362,6.02104430504163));
#132082=CARTESIAN_POINT('Ctrl Pts',(15.7965675516919,14.4527367769768,5.9975884209926));
#132083=CARTESIAN_POINT('Ctrl Pts',(15.7995680175075,14.4308995282325,5.97258646870972));
#132084=CARTESIAN_POINT('Ctrl Pts',(15.8025599717558,14.4108625484769,5.94626859422399));
#132085=CARTESIAN_POINT('Ctrl Pts',(15.8055577280513,14.3907867126787,5.91989968368066));
#132086=CARTESIAN_POINT('Ctrl Pts',(15.8085464671915,14.372518449713,5.89220933325829));
#132087=CARTESIAN_POINT('Ctrl Pts',(15.8114640455094,14.3562470770825,5.86346021727603));
#132088=CARTESIAN_POINT('Ctrl Pts',(15.81249677072,14.3504875550075,5.85328399109664));
#132089=CARTESIAN_POINT('Ctrl Pts',(15.8135204400367,14.3449779721579,5.84297542595422));
#132090=CARTESIAN_POINT('Ctrl Pts',(15.8145319440733,14.3397257942077,5.83254727499866));
#132091=CARTESIAN_POINT('Ctrl Pts',(15.8145332031598,14.3397192564715,5.83253429438356));
#132092=CARTESIAN_POINT('Ctrl Pts',(15.8145344622292,14.339712719122,5.83252131356128));
#132093=CARTESIAN_POINT('Ctrl Pts',(15.8145357212814,14.3397061821593,5.83250833253183));
#132094=CARTESIAN_POINT('Ctrl Pts',(15.8171533011343,14.3261157829449,5.80552066556783));
#132095=CARTESIAN_POINT('Ctrl Pts',(15.8196966394794,14.3141974283294,5.77763344311099));
#132096=CARTESIAN_POINT('Ctrl Pts',(15.8222092530609,14.3040405757782,5.7490739337915));
#132097=CARTESIAN_POINT('Origin',(13.2437274406976,15.,5.5));
#132098=CARTESIAN_POINT('',(16.3004622294836,14.3042076660467,5.7489859996302));
#132099=CARTESIAN_POINT('',(16.2213444347181,14.3044435251824,5.74885644548777));
#132100=CARTESIAN_POINT('',(13.2437274406976,14.3042076641721,5.74898599439144));
#132101=CARTESIAN_POINT('Ctrl Pts',(16.3004622294836,14.3042076679214,5.74898600486896));
#132102=CARTESIAN_POINT('Ctrl Pts',(16.2994517369524,14.3083860293658,5.76066245172471));
#132103=CARTESIAN_POINT('Ctrl Pts',(16.2984477733188,14.3128588604262,5.77223524884823));
#132104=CARTESIAN_POINT('Ctrl Pts',(16.2929454430558,14.3390315264409,5.83518931248759));
#132105=CARTESIAN_POINT('Ctrl Pts',(16.2885035166987,14.3661982337309,5.88409074977041));
#132106=CARTESIAN_POINT('Ctrl Pts',(16.2828018855551,14.4060020165941,5.93982887446734));
#132107=CARTESIAN_POINT('Ctrl Pts',(16.2817336435,14.4136657788038,5.94999464965032));
#132108=CARTESIAN_POINT('Ctrl Pts',(16.2799133217406,14.4270402699169,5.96681355123648));
#132109=CARTESIAN_POINT('Ctrl Pts',(16.2791666549248,14.4326139885565,5.97357242731626));
#132110=CARTESIAN_POINT('Ctrl Pts',(16.2776267006674,14.4442784741901,5.98721560616398));
#132111=CARTESIAN_POINT('Ctrl Pts',(16.2768330627778,14.450380141342,5.99408850973305));
#132112=CARTESIAN_POINT('Ctrl Pts',(16.274759435409,14.4665444102232,6.01162591928593));
#132113=CARTESIAN_POINT('Ctrl Pts',(16.2734716414276,14.476798521178,6.0221073584513));
#132114=CARTESIAN_POINT('Ctrl Pts',(16.2705622764027,14.5004203298335,6.04485787997494));
#132115=CARTESIAN_POINT('Ctrl Pts',(16.2689349142941,14.5139414905469,6.05695329495336));
#132116=CARTESIAN_POINT('Ctrl Pts',(16.2628065859188,14.5660075272807,6.10018830355885));
#132117=CARTESIAN_POINT('Ctrl Pts',(16.2582144284696,14.6072076165935,6.12792434102262));
#132118=CARTESIAN_POINT('Ctrl Pts',(16.2519397608728,14.6678688169862,6.16044075920834));
#132119=CARTESIAN_POINT('Ctrl Pts',(16.2501964108936,14.6852228537609,6.16888610813786));
#132120=CARTESIAN_POINT('Ctrl Pts',(16.2478605380079,14.709326048274,6.17946970058863));
#132121=CARTESIAN_POINT('Ctrl Pts',(16.2472410215083,14.7158032004805,6.1822042296793));
#132122=CARTESIAN_POINT('Ctrl Pts',(16.2461956952537,14.7268886467197,6.18669899219772));
#132123=CARTESIAN_POINT('Ctrl Pts',(16.2457673575847,14.7314771119835,6.18850619614771));
#132124=CARTESIAN_POINT('Ctrl Pts',(16.2448285044712,14.7416385581513,6.19239131391346));
#132125=CARTESIAN_POINT('Ctrl Pts',(16.2443191647446,14.7472190691158,6.19444810793961));
#132126=CARTESIAN_POINT('Ctrl Pts',(16.2427430721005,14.764679699825,6.20064514321187));
#132127=CARTESIAN_POINT('Ctrl Pts',(16.2416884022442,14.776641869792,6.20454982914273));
#132128=CARTESIAN_POINT('Ctrl Pts',(16.2398172509503,14.7982559150491,6.21099915045727));
#132129=CARTESIAN_POINT('Ctrl Pts',(16.2389969332587,14.807870113797,6.21365719647443));
#132130=CARTESIAN_POINT('Ctrl Pts',(16.234677573181,14.859063361113,6.22670102230444));
#132131=CARTESIAN_POINT('Ctrl Pts',(16.2312668776027,14.9014345153497,6.23365027564152));
#132132=CARTESIAN_POINT('Ctrl Pts',(16.227513995898,14.947678265039,6.23715385661125));
#132133=CARTESIAN_POINT('Ctrl Pts',(16.2272290538534,14.951187461355,6.23739454022586));
#132134=CARTESIAN_POINT('Ctrl Pts',(16.2246841239846,14.9825029434427,6.23931784241169));
#132135=CARTESIAN_POINT('Ctrl Pts',(16.2224024202493,15.0103788541925,6.23945182248278));
#132136=CARTESIAN_POINT('Ctrl Pts',(16.2191280149388,15.0495016434262,6.23742715382624));
#132137=CARTESIAN_POINT('Ctrl Pts',(16.2181745354255,15.0607943267638,6.23658213477939));
#132138=CARTESIAN_POINT('Ctrl Pts',(16.2164765984805,15.0806948903967,6.23463226694157));
#132139=CARTESIAN_POINT('Ctrl Pts',(16.2157355645625,15.0893112778201,6.23363459222357));
#132140=CARTESIAN_POINT('Ctrl Pts',(16.2141596971666,15.1074759079027,6.23120661578024));
#132141=CARTESIAN_POINT('Ctrl Pts',(16.213323881398,15.1170175919536,6.22974039876132));
#132142=CARTESIAN_POINT('Ctrl Pts',(16.2109833356914,15.1434632639723,6.22514466104485));
#132143=CARTESIAN_POINT('Ctrl Pts',(16.2094665257275,15.1602897243496,6.22161179777485));
#132144=CARTESIAN_POINT('Ctrl Pts',(16.2043397419378,15.21607839776,6.20785105990925));
#132145=CARTESIAN_POINT('Ctrl Pts',(16.2006587937955,15.2543211754153,6.19502723309645));
#132146=CARTESIAN_POINT('Ctrl Pts',(16.1934521527081,15.3263731291505,6.16412052970031));
#132147=CARTESIAN_POINT('Ctrl Pts',(16.1899398749359,15.3602094609348,6.14639399538106));
#132148=CARTESIAN_POINT('Ctrl Pts',(16.1857252512568,15.4001595372095,6.12134890298495));
#132149=CARTESIAN_POINT('Ctrl Pts',(16.1849264454501,15.4077028061472,6.11642563128004));
#132150=CARTESIAN_POINT('Ctrl Pts',(16.1836725673053,15.4195177080691,6.10840258587782));
#132151=CARTESIAN_POINT('Ctrl Pts',(16.1832122963809,15.4238491016908,6.10539306098997));
#132152=CARTESIAN_POINT('Ctrl Pts',(16.1822999433935,15.4324288427241,6.09929448456349));
#132153=CARTESIAN_POINT('Ctrl Pts',(16.1818478664713,15.4366772160495,6.09620600248864));
#132154=CARTESIAN_POINT('Ctrl Pts',(16.1806374201285,15.4480338803516,6.08776341003342));
#132155=CARTESIAN_POINT('Ctrl Pts',(16.1798843782696,15.4550792880145,6.08232555133863));
#132156=CARTESIAN_POINT('Ctrl Pts',(16.1766762745876,15.4849273452204,6.05841522031983));
#132157=CARTESIAN_POINT('Ctrl Pts',(16.1742877709097,15.5067194532521,6.03871878431391));
#132158=CARTESIAN_POINT('Ctrl Pts',(16.1671599541238,15.5685312217722,5.9757718637109));
#132159=CARTESIAN_POINT('Ctrl Pts',(16.1624818325113,15.6046066430114,5.92899486387698));
#132160=CARTESIAN_POINT('Ctrl Pts',(16.1565508664372,15.6410437584492,5.86787901320984));
#132161=CARTESIAN_POINT('Ctrl Pts',(16.1555182781162,15.6470731304854,5.85716718298428));
#132162=CARTESIAN_POINT('Ctrl Pts',(16.153732120129,15.6569461091196,5.83855557014548));
#132163=CARTESIAN_POINT('Ctrl Pts',(16.1529832734326,15.6609212494549,5.83072821505775));
#132164=CARTESIAN_POINT('Ctrl Pts',(16.151427344782,15.6688372745419,5.81442803510577));
#132165=CARTESIAN_POINT('Ctrl Pts',(16.1506197592493,15.6727587485998,5.80594760621321));
#132166=CARTESIAN_POINT('Ctrl Pts',(16.1484586982169,15.6827510787009,5.78321695762616));
#132167=CARTESIAN_POINT('Ctrl Pts',(16.1470960980081,15.6885361283502,5.76884717349373));
#132168=CARTESIAN_POINT('Ctrl Pts',(16.1431974357493,15.7036294570319,5.72766577761879));
#132169=CARTESIAN_POINT('Ctrl Pts',(16.14063083312,15.7118501264622,5.70048726058336));
#132170=CARTESIAN_POINT('Ctrl Pts',(16.1333611922224,15.7304593445063,5.62315946724311));
#132171=CARTESIAN_POINT('Ctrl Pts',(16.1286091628451,15.7372325108256,5.57230276390171));
#132172=CARTESIAN_POINT('Ctrl Pts',(16.1231163930742,15.7389859294872,5.51106993450556));
#132173=CARTESIAN_POINT('Ctrl Pts',(16.1222192695503,15.7390682070861,5.50098144736492));
#132174=CARTESIAN_POINT('Ctrl Pts',(16.1208490323358,15.7388762434804,5.48540427117969));
#132175=CARTESIAN_POINT('Ctrl Pts',(16.1203690880374,15.7387474241494,5.47991548355235));
#132176=CARTESIAN_POINT('Ctrl Pts',(16.1194506682585,15.7383813262252,5.46934187656149));
#132177=CARTESIAN_POINT('Ctrl Pts',(16.1190118194879,15.7381526675241,5.46425722848243));
#132178=CARTESIAN_POINT('Ctrl Pts',(16.1178846774055,15.7374260515046,5.45112430516183));
#132179=CARTESIAN_POINT('Ctrl Pts',(16.1172004730792,15.7368488511159,5.44308073742272));
#132180=CARTESIAN_POINT('Ctrl Pts',(16.1156800591803,15.7352609399702,5.42508406500585));
#132181=CARTESIAN_POINT('Ctrl Pts',(16.114847005266,15.7341795590782,5.41513865776079));
#132182=CARTESIAN_POINT('Ctrl Pts',(16.1121475273747,15.7299897172839,5.38274105617902));
#132183=CARTESIAN_POINT('Ctrl Pts',(16.1103088907729,15.7260502379792,5.36040823020972));
#132184=CARTESIAN_POINT('Ctrl Pts',(16.1039354346095,15.7087724728781,5.28336388715953));
#132185=CARTESIAN_POINT('Ctrl Pts',(16.099453702746,15.6902213510403,5.23003094407816));
#132186=CARTESIAN_POINT('Ctrl Pts',(16.0937134464031,15.6603054969069,5.16791887995087));
#132187=CARTESIAN_POINT('Ctrl Pts',(16.0926510421927,15.654521121012,5.1566586496617));
#132188=CARTESIAN_POINT('Ctrl Pts',(16.0908375506354,15.6442545999071,5.13787633009199));
#132189=CARTESIAN_POINT('Ctrl Pts',(16.0900917768073,15.6399226061558,5.13027498600969));
#132190=CARTESIAN_POINT('Ctrl Pts',(16.0885509856233,15.6307555689497,5.11483350634812));
#132191=CARTESIAN_POINT('Ctrl Pts',(16.087755583233,15.6259068700205,5.1070033220359));
#132192=CARTESIAN_POINT('Ctrl Pts',(16.085670895987,15.612906428095,5.0868599069873));
#132193=CARTESIAN_POINT('Ctrl Pts',(16.0843736437006,15.6045301393251,5.07469743833649));
#132194=CARTESIAN_POINT('Ctrl Pts',(16.0821946018103,15.5900018051966,5.05489913060011));
#132195=CARTESIAN_POINT('Ctrl Pts',(16.0813202022419,15.5840516577785,5.04711970995621));
#132196=CARTESIAN_POINT('Ctrl Pts',(16.0777183412289,15.5590533148954,5.01574826955821));
#132197=CARTESIAN_POINT('Ctrl Pts',(16.0749504526078,15.5387181570825,4.99322319274776));
#132198=CARTESIAN_POINT('Ctrl Pts',(16.0681965799785,15.4861752831793,4.94176780959381));
#132199=CARTESIAN_POINT('Ctrl Pts',(16.0642034676475,15.4526944752259,4.91428851100823));
#132200=CARTESIAN_POINT('Ctrl Pts',(16.0595658526669,15.4098179824205,4.8849829995674));
#132201=CARTESIAN_POINT('Ctrl Pts',(16.0587948830366,15.402548780796,4.88020068635026));
#132202=CARTESIAN_POINT('Ctrl Pts',(16.0575740714618,15.3907922703712,4.87276036027724));
#132203=CARTESIAN_POINT('Ctrl Pts',(16.0571194613647,15.3863585996155,4.87001968065359));
#132204=CARTESIAN_POINT('Ctrl Pts',(16.0562072769506,15.3773437510821,4.86457811825307));
#132205=CARTESIAN_POINT('Ctrl Pts',(16.0557498371956,15.3727616985852,4.86187932498903));
#132206=CARTESIAN_POINT('Ctrl Pts',(16.0545070172728,15.3601556106697,4.85463656913661));
#132207=CARTESIAN_POINT('Ctrl Pts',(16.0537274648998,15.3520746871094,4.8501927511099));
#132208=CARTESIAN_POINT('Ctrl Pts',(16.050260591106,15.3154516944331,4.83093711483149));
#132209=CARTESIAN_POINT('Ctrl Pts',(16.0476529092147,15.2860410521651,4.81784460919582));
#132210=CARTESIAN_POINT('Ctrl Pts',(16.0407098498805,15.2052851296335,4.7880406812357));
#132211=CARTESIAN_POINT('Ctrl Pts',(16.0364095748317,15.1528177150459,4.77496620498191));
#132212=CARTESIAN_POINT('Ctrl Pts',(16.0308455963803,15.0865407429377,4.76596999310194));
#132213=CARTESIAN_POINT('Ctrl Pts',(16.0297574123535,15.0736407351407,4.76456383569484));
#132214=CARTESIAN_POINT('Ctrl Pts',(16.0279136768122,15.0519402937685,4.76277502968693));
#132215=CARTESIAN_POINT('Ctrl Pts',(16.0271638811653,15.0431576224315,4.76220879891137));
#132216=CARTESIAN_POINT('Ctrl Pts',(16.0256262978969,15.0252481221696,4.76137501229877));
#132217=CARTESIAN_POINT('Ctrl Pts',(16.024838273481,15.0161222994786,4.76111949865441));
#132218=CARTESIAN_POINT('Ctrl Pts',(16.022799887066,14.9926675338573,4.76089749298013));
#132219=CARTESIAN_POINT('Ctrl Pts',(16.0215422321533,14.9783407858983,4.76117857548268));
#132220=CARTESIAN_POINT('Ctrl Pts',(16.0187160992876,14.9464939424655,4.7627304250224));
#132221=CARTESIAN_POINT('Ctrl Pts',(16.0171423687037,14.9289931362629,4.76420977877831));
#132222=CARTESIAN_POINT('Ctrl Pts',(16.0114400193112,14.8663993992292,4.77175466705736));
#132223=CARTESIAN_POINT('Ctrl Pts',(16.0072344764716,14.821837352697,4.78135695623573));
#132224=CARTESIAN_POINT('Ctrl Pts',(16.0009225239235,14.7560490643651,4.80203144599196));
#132225=CARTESIAN_POINT('Ctrl Pts',(15.9987900437993,14.7339976332204,4.81013396169094));
#132226=CARTESIAN_POINT('Ctrl Pts',(15.9960328669673,14.705435186727,4.82220268317415));
#132227=CARTESIAN_POINT('Ctrl Pts',(15.9953684601801,14.6985478953803,4.82523761627725));
#132228=CARTESIAN_POINT('Ctrl Pts',(15.9942767683819,14.6872102779137,4.83044187776041));
#132229=CARTESIAN_POINT('Ctrl Pts',(15.993846248157,14.682733403364,4.83255157290317));
#132230=CARTESIAN_POINT('Ctrl Pts',(15.9929285476355,14.6731743377037,4.83717413978791));
#132231=CARTESIAN_POINT('Ctrl Pts',(15.992442180808,14.6680992999583,4.83970077514199));
#132232=CARTESIAN_POINT('Ctrl Pts',(15.991019488024,14.6532437048725,4.84731128239167));
#132233=CARTESIAN_POINT('Ctrl Pts',(15.9900921046246,14.6435466937445,4.85255612606353));
#132234=CARTESIAN_POINT('Ctrl Pts',(15.9878880628603,14.6205635310667,4.86566008880557));
#132235=CARTESIAN_POINT('Ctrl Pts',(15.9866205851412,14.6073988567092,4.87372244904268));
#132236=CARTESIAN_POINT('Ctrl Pts',(15.9805803177298,14.5454225966811,4.91440118590786));
#132237=CARTESIAN_POINT('Ctrl Pts',(15.9759465432297,14.500363227696,4.95234149642313));
#132238=CARTESIAN_POINT('Ctrl Pts',(15.9696755283331,14.4483120568325,5.00799621496053));
#132239=CARTESIAN_POINT('Ctrl Pts',(15.9682213917082,14.4368160487304,5.02119831351721));
#132240=CARTESIAN_POINT('Ctrl Pts',(15.965923971035,14.4196306026858,5.04241020722167));
#132241=CARTESIAN_POINT('Ctrl Pts',(15.9650936615076,14.4136133593676,5.05014697471417));
#132242=CARTESIAN_POINT('Ctrl Pts',(15.9635196870945,14.4025821906683,5.06492796583384));
#132243=CARTESIAN_POINT('Ctrl Pts',(15.9627774851918,14.3975345266656,5.07194503447357));
#132244=CARTESIAN_POINT('Ctrl Pts',(15.9610585369559,14.3862043860028,5.08829324205044));
#132245=CARTESIAN_POINT('Ctrl Pts',(15.9600787316703,14.3800097453002,5.09768226004053));
#132246=CARTESIAN_POINT('Ctrl Pts',(15.9566108560075,14.3590194791475,5.1311331617797));
#132247=CARTESIAN_POINT('Ctrl Pts',(15.9540831653982,14.345392974958,5.1558953796543));
#132248=CARTESIAN_POINT('Ctrl Pts',(15.945984206961,14.306918924882,5.23640900976162));
#132249=CARTESIAN_POINT('Ctrl Pts',(15.9402934057937,14.287535892335,5.29448554910314));
#132250=CARTESIAN_POINT('Ctrl Pts',(15.933952087427,14.2735792845062,5.36387612304762));
#132251=CARTESIAN_POINT('Ctrl Pts',(15.9330823703939,14.271840270461,5.37350809422712));
#132252=CARTESIAN_POINT('Ctrl Pts',(15.9317444608854,14.2694344745218,5.38853474024009));
#132253=CARTESIAN_POINT('Ctrl Pts',(15.9312699092587,14.2686350526367,5.39390659417686));
#132254=CARTESIAN_POINT('Ctrl Pts',(15.9303538317602,14.2671962967282,5.40436523333159));
#132255=CARTESIAN_POINT('Ctrl Pts',(15.9299120316084,14.2665505446367,5.40945069976812));
#132256=CARTESIAN_POINT('Ctrl Pts',(15.9287655007803,14.2650026661564,5.42274631658249));
#132257=CARTESIAN_POINT('Ctrl Pts',(15.9280651414896,14.2641851237619,5.43096596306673));
#132258=CARTESIAN_POINT('Ctrl Pts',(15.9265017110519,14.262655414056,5.44949537110412));
#132259=CARTESIAN_POINT('Ctrl Pts',(15.9256420786784,14.2620213108645,5.45980998031163));
#132260=CARTESIAN_POINT('Ctrl Pts',(15.921511900116,14.2599991945482,5.50980596743498));
#132261=CARTESIAN_POINT('Ctrl Pts',(15.9183376690916,14.2615941501501,5.54954520300804));
#132262=CARTESIAN_POINT('Ctrl Pts',(15.9120257110401,14.2710262189477,5.62732246567828));
#132263=CARTESIAN_POINT('Ctrl Pts',(15.9088985736854,14.2786777125098,5.66524936995509));
#132264=CARTESIAN_POINT('Ctrl Pts',(15.9049235216853,14.2917510482803,5.71115705945049));
#132265=CARTESIAN_POINT('Ctrl Pts',(15.904160970047,14.2944059507075,5.71986565153891));
#132266=CARTESIAN_POINT('Ctrl Pts',(15.9027854288629,14.2994510306775,5.73538086262834));
#132267=CARTESIAN_POINT('Ctrl Pts',(15.9021752100555,14.3017780490148,5.74219642533103));
#132268=CARTESIAN_POINT('Ctrl Pts',(15.901560926295,14.3042076642396,5.74898599458032));
#132269=CARTESIAN_POINT('',(15.8432246779788,14.2612681978804,5.50006554428406));
#132270=CARTESIAN_POINT('Ctrl Pts',(15.822316354248,14.3042195800731,5.74901929091195));
#132271=CARTESIAN_POINT('Ctrl Pts',(15.8257720408061,14.2899780123663,5.70922717712378));
#132272=CARTESIAN_POINT('Ctrl Pts',(15.8291379930438,14.2791756081813,5.668284904552));
#132273=CARTESIAN_POINT('Ctrl Pts',(15.8348254834206,14.2671320011413,5.59904583292395));
#132274=CARTESIAN_POINT('Ctrl Pts',(15.8371105551477,14.2639051901807,5.57120207702545));
#132275=CARTESIAN_POINT('Ctrl Pts',(15.8401059855828,14.2617981889574,5.53525759524664));
#132276=CARTESIAN_POINT('Ctrl Pts',(15.8407749389911,14.2614597588463,5.52726379577456));
#132277=CARTESIAN_POINT('Ctrl Pts',(15.8419862648768,14.2610841869658,5.51286288273956));
#132278=CARTESIAN_POINT('Ctrl Pts',(15.8425272369543,14.2610004566375,5.50645771277246));
#132279=CARTESIAN_POINT('Ctrl Pts',(15.8430707068965,14.2610000018627,5.50005246929806));
#132280=CARTESIAN_POINT('Ctrl Pts',(15.8432343872441,14.261285110058,5.50006636877984));
#132281=CARTESIAN_POINT('Ctrl Pts',(15.8461654839889,14.2612946478705,5.46562025595231));
#132282=CARTESIAN_POINT('Ctrl Pts',(15.8491505168945,14.2636863127109,5.43121385975223));
#132283=CARTESIAN_POINT('Ctrl Pts',(15.852183835402,14.2684229126413,5.39717845675775));
#132284=CARTESIAN_POINT('Ctrl Pts',(15.8552208664968,14.2731653098663,5.3631013966129));
#132285=CARTESIAN_POINT('Ctrl Pts',(15.8583062235405,14.2802583961928,5.32939603907854));
#132286=CARTESIAN_POINT('Ctrl Pts',(15.8614058499154,14.2896334199308,5.29638824388491));
#132287=CARTESIAN_POINT('Ctrl Pts',(15.8645149786118,14.2990371840649,5.26327925885615));
#132288=CARTESIAN_POINT('Ctrl Pts',(15.8676381130064,14.3107373316171,5.23087191259096));
#132289=CARTESIAN_POINT('Ctrl Pts',(15.8707154043018,14.3246296874959,5.19949159250958));
#132290=CARTESIAN_POINT('Ctrl Pts',(15.8730027357389,14.3349557890202,5.17616679620788));
#132291=CARTESIAN_POINT('Ctrl Pts',(15.8752640840529,14.3464924798322,5.15340938928462));
#132292=CARTESIAN_POINT('Ctrl Pts',(15.8774685112417,14.3591812956108,5.13135232938189));
#132293=CARTESIAN_POINT('Ctrl Pts',(15.8774697703278,14.3591885429865,5.1313397312164));
#132294=CARTESIAN_POINT('Ctrl Pts',(15.8774710293971,14.3591957907502,5.13132713325581));
#132295=CARTESIAN_POINT('Ctrl Pts',(15.8774722884495,14.3592030389018,5.13131453550017));
#132296=CARTESIAN_POINT('Ctrl Pts',(15.88006104256,14.3741060580229,5.10541212580785));
#132297=CARTESIAN_POINT('Ctrl Pts',(15.8825785266667,14.3906531832454,5.08037439649702));
#132298=CARTESIAN_POINT('Ctrl Pts',(15.8850657038896,14.4087054696607,5.0564084055246));
#132299=CARTESIAN_POINT('Ctrl Pts',(15.8853223609872,14.4105683234191,5.05393530403883));
#132300=CARTESIAN_POINT('Ctrl Pts',(15.8855786953586,14.4124471622381,5.05147363121617));
#132301=CARTESIAN_POINT('Ctrl Pts',(15.8858347520161,14.4143418036469,5.04902362474293));
#132302=CARTESIAN_POINT('Ctrl Pts',(15.8885690334582,14.4345735870917,5.02286141791415));
#132303=CARTESIAN_POINT('Ctrl Pts',(15.8912724849652,14.4566124161231,4.99802716624137));
#132304=CARTESIAN_POINT('Ctrl Pts',(15.8939920816802,14.4802353179151,4.97475863671982));
#132305=CARTESIAN_POINT('Ctrl Pts',(15.8967088751499,14.5038338702174,4.95151409141598));
#132306=CARTESIAN_POINT('Ctrl Pts',(15.8994422611057,14.5290127331921,4.92983176695324));
#132307=CARTESIAN_POINT('Ctrl Pts',(15.9022214543911,14.5555261725094,4.90991198894262));
#132308=CARTESIAN_POINT('Ctrl Pts',(15.904999322998,14.582026974425,4.89000170552201));
#132309=CARTESIAN_POINT('Ctrl Pts',(15.9078231800637,14.6098608284518,4.87185209576196));
#132310=CARTESIAN_POINT('Ctrl Pts',(15.9106993990143,14.6387644217228,4.85563008019805));
#132311=CARTESIAN_POINT('Ctrl Pts',(15.9135779698292,14.6676916492615,4.83939480000458));
#132312=CARTESIAN_POINT('Ctrl Pts',(15.9165090298598,14.6976902939112,4.82509019853197));
#132313=CARTESIAN_POINT('Ctrl Pts',(15.9194741482956,14.7284808452098,4.81285240797014));
#132314=CARTESIAN_POINT('Ctrl Pts',(15.9224406859921,14.759286134475,4.80060875976236));
#132315=CARTESIAN_POINT('Ctrl Pts',(15.9254411518062,14.7908841955844,4.79043400749844));
#132316=CARTESIAN_POINT('Ctrl Pts',(15.9284331060532,14.8229793103559,4.78243308993879));
#132317=CARTESIAN_POINT('Ctrl Pts',(15.9314308623474,14.8551366645051,4.77441665686743));
#132318=CARTESIAN_POINT('Ctrl Pts',(15.9344196014866,14.887793253204,4.76858294864165));
#132319=CARTESIAN_POINT('Ctrl Pts',(15.9373371798038,14.9206329578154,4.76500202182394));
#132320=CARTESIAN_POINT('Ctrl Pts',(15.9383699050267,14.9322571157913,4.7637344934));
#132321=CARTESIAN_POINT('Ctrl Pts',(15.9393935743555,14.9439040274351,4.76274886121914));
#132322=CARTESIAN_POINT('Ctrl Pts',(15.9404050784039,14.9555590270972,4.76204694128078));
#132323=CARTESIAN_POINT('Ctrl Pts',(15.94040633749,14.9555735348478,4.76204606755451));
#132324=CARTESIAN_POINT('Ctrl Pts',(15.9404075965593,14.9555880426407,4.76204519426493));
#132325=CARTESIAN_POINT('Ctrl Pts',(15.9404088556117,14.9556025504756,4.76204432141208));
#132326=CARTESIAN_POINT('Ctrl Pts',(15.9429976097227,14.9854322993204,4.76024963727026));
#132327=CARTESIAN_POINT('Ctrl Pts',(15.94551509383,15.0154438358427,4.76030365815609));
#132328=CARTESIAN_POINT('Ctrl Pts',(15.9480022710536,15.0453878132334,4.76220418088315));
#132329=CARTESIAN_POINT('Ctrl Pts',(15.9482589281508,15.0484777958231,4.76240029985764));
#132330=CARTESIAN_POINT('Ctrl Pts',(15.9485152625218,15.0515670219798,4.76261605462374));
#132331=CARTESIAN_POINT('Ctrl Pts',(15.9487713191789,15.0546551928411,4.76285142346396));
#132332=CARTESIAN_POINT('Ctrl Pts',(15.9515056006213,15.0876319893532,4.76536479163489));
#132333=CARTESIAN_POINT('Ctrl Pts',(15.9542090521288,15.1204932118478,4.77011769576169));
#132334=CARTESIAN_POINT('Ctrl Pts',(15.9569286488443,15.152917660288,4.77705463303679));
#132335=CARTESIAN_POINT('Ctrl Pts',(15.9596454423144,15.185308686976,4.78398442000988));
#132336=CARTESIAN_POINT('Ctrl Pts',(15.9623788282709,15.2172637955092,4.7930931725959));
#132337=CARTESIAN_POINT('Ctrl Pts',(15.9651580215568,15.2484805436034,4.8042857888708));
#132338=CARTESIAN_POINT('Ctrl Pts',(15.9679358901642,15.2796824125045,4.81547307028191));
#132339=CARTESIAN_POINT('Ctrl Pts',(15.9707597472306,15.3101466471275,4.82874191248828));
#132340=CARTESIAN_POINT('Ctrl Pts',(15.9736359661817,15.3395890414552,4.8439641629593));
#132341=CARTESIAN_POINT('Ctrl Pts',(15.9765145369972,15.3690555106246,4.85919886055894));
#132342=CARTESIAN_POINT('Ctrl Pts',(15.9794455970283,15.3974984857032,4.87639006392071));
#132343=CARTESIAN_POINT('Ctrl Pts',(15.9824107154647,15.42465057061,4.89537916217598));
#132344=CARTESIAN_POINT('Ctrl Pts',(15.9853772531617,15.4518156519232,4.91437734960579));
#132345=CARTESIAN_POINT('Ctrl Pts',(15.9883777189763,15.4776885772525,4.93517530105871));
#132346=CARTESIAN_POINT('Ctrl Pts',(15.9913696732237,15.5020190932365,4.95758371613387));
#132347=CARTESIAN_POINT('Ctrl Pts',(15.9943674295183,15.5263967913596,4.98003558597831));
#132348=CARTESIAN_POINT('Ctrl Pts',(15.9973561686579,15.5492258537316,5.00410462934443));
#132349=CARTESIAN_POINT('Ctrl Pts',(16.0002737469752,15.5702739453929,5.02956532598645));
#132350=CARTESIAN_POINT('Ctrl Pts',(16.0013064721957,15.5777242664251,5.03857756171499));
#132351=CARTESIAN_POINT('Ctrl Pts',(16.0023301415221,15.5849516420565,5.04776380482493));
#132352=CARTESIAN_POINT('Ctrl Pts',(16.003341645568,15.5919464914698,5.05711280422425));
#132353=CARTESIAN_POINT('Ctrl Pts',(16.0033429046542,15.5919551984226,5.05712444154354));
#132354=CARTESIAN_POINT('Ctrl Pts',(16.0033441637235,15.5919639050338,5.05713607913817));
#132355=CARTESIAN_POINT('Ctrl Pts',(16.0033454227759,15.5919726113034,5.05714771700814));
#132356=CARTESIAN_POINT('Ctrl Pts',(16.0059341768868,15.6098736858217,5.08107649337375));
#132357=CARTESIAN_POINT('Ctrl Pts',(16.008451660994,15.6263305680899,5.10617363003627));
#132358=CARTESIAN_POINT('Ctrl Pts',(16.0109388382175,15.6412079936657,5.13222964617114));
#132359=CARTESIAN_POINT('Ctrl Pts',(16.0111954953145,15.6427432267902,5.1349184217834));
#132360=CARTESIAN_POINT('Ctrl Pts',(16.0114518296852,15.6442616429966,5.13761736242249));
#132361=CARTESIAN_POINT('Ctrl Pts',(16.0117078863421,15.6457630960937,5.14032620651912));
#132362=CARTESIAN_POINT('Ctrl Pts',(16.0144421677842,15.6617962482467,5.16925239118957));
#132363=CARTESIAN_POINT('Ctrl Pts',(16.0171456192913,15.6758952568307,5.19931346233171));
#132364=CARTESIAN_POINT('Ctrl Pts',(16.0198652160065,15.6879298675583,5.23021061591972));
#132365=CARTESIAN_POINT('Ctrl Pts',(16.0225820094763,15.6999520735174,5.26107592202646));
#132366=CARTESIAN_POINT('Ctrl Pts',(16.0253153954325,15.7099145849502,5.29277523906632));
#132367=CARTESIAN_POINT('Ctrl Pts',(16.0280945887181,15.7177305371739,5.32500365682599));
#132368=CARTESIAN_POINT('Ctrl Pts',(16.0308724573252,15.7255427639915,5.35721671318894));
#132369=CARTESIAN_POINT('Ctrl Pts',(16.0336963143912,15.7312107543982,5.3899582105465));
#132370=CARTESIAN_POINT('Ctrl Pts',(16.0365725333421,15.7346852768664,5.42292029765544));
#132371=CARTESIAN_POINT('Ctrl Pts',(16.0394511041573,15.7381626404275,5.45590933763434));
#132372=CARTESIAN_POINT('Ctrl Pts',(16.0423821641882,15.7394430394864,5.48911928919101));
#132373=CARTESIAN_POINT('Ctrl Pts',(16.0453472826244,15.7385119261771,5.52223959406798));
#132374=CARTESIAN_POINT('Ctrl Pts',(16.0483138203211,15.7375803671882,5.55537575205327));
#132375=CARTESIAN_POINT('Ctrl Pts',(16.0513142861355,15.7344350386086,5.58842223382762));
#132376=CARTESIAN_POINT('Ctrl Pts',(16.0543062403828,15.729096452324,5.62106592495639));
#132377=CARTESIAN_POINT('Ctrl Pts',(16.0573039966772,15.7237475133645,5.65377291927117));
#132378=CARTESIAN_POINT('Ctrl Pts',(16.0602927358166,15.7161962885673,5.68607561174723));
#132379=CARTESIAN_POINT('Ctrl Pts',(16.0632103141338,15.7065033953313,5.71765593879732));
#132380=CARTESIAN_POINT('Ctrl Pts',(16.0642430393564,15.70307243505,5.7288343191983));
#132381=CARTESIAN_POINT('Ctrl Pts',(16.0652667086848,15.6993735456597,5.7399221611344));
#132382=CARTESIAN_POINT('Ctrl Pts',(16.0662782127328,15.6954108566826,5.75090527566));
#132383=CARTESIAN_POINT('Ctrl Pts',(16.0662794718189,15.6954059240609,5.75091894707072));
#132384=CARTESIAN_POINT('Ctrl Pts',(16.0662807308882,15.6954009910215,5.75093261834753));
#132385=CARTESIAN_POINT('Ctrl Pts',(16.0662819899406,15.6953960575642,5.75094628949041));
#132386=CARTESIAN_POINT('Ctrl Pts',(16.0688707440513,15.6852523117074,5.77905570476472));
#132387=CARTESIAN_POINT('Ctrl Pts',(16.0713882281583,15.6733385845194,5.80660127331832));
#132388=CARTESIAN_POINT('Ctrl Pts',(16.0738754053815,15.6597554710563,5.83335483003574));
#132389=CARTESIAN_POINT('Ctrl Pts',(16.0741320624789,15.658353800744,5.83611558634535));
#132390=CARTESIAN_POINT('Ctrl Pts',(16.07438839685,15.6569343931202,5.838867885452));
#132391=CARTESIAN_POINT('Ctrl Pts',(16.0746444535072,15.6554973862791,5.84161146142266));
#132392=CARTESIAN_POINT('Ctrl Pts',(16.0773787349494,15.640152418565,5.87090852771709));
#132393=CARTESIAN_POINT('Ctrl Pts',(16.0800821864566,15.6227960265121,5.89921410483932));
#132394=CARTESIAN_POINT('Ctrl Pts',(16.0828017831719,15.6036061681248,5.92625509761583));
#132395=CARTESIAN_POINT('Ctrl Pts',(16.0855185766417,15.5844360898333,5.95326821767887));
#132396=CARTESIAN_POINT('Ctrl Pts',(16.0882519625979,15.5634368616103,5.97901954286687));
#132397=CARTESIAN_POINT('Ctrl Pts',(16.0910311558835,15.54081539972,6.00326886208316));
#132398=CARTESIAN_POINT('Ctrl Pts',(16.0938090244907,15.5182047201539,6.02750662307106));
#132399=CARTESIAN_POINT('Ctrl Pts',(16.0966328815568,15.4939736351654,6.05024395547408));
#132400=CARTESIAN_POINT('Ctrl Pts',(16.0995091005077,15.4683522103346,6.07127046451998));
#132401=CARTESIAN_POINT('Ctrl Pts',(16.1023876713229,15.4427098350425,6.09231416679644));
#132402=CARTESIAN_POINT('Ctrl Pts',(16.1053187313538,15.4156749284953,6.11164430213428));
#132403=CARTESIAN_POINT('Ctrl Pts',(16.1082838497899,15.38749888833,6.12907795716688));
#132404=CARTESIAN_POINT('Ctrl Pts',(16.1112503874867,15.3593093616398,6.14651995685763));
#132405=CARTESIAN_POINT('Ctrl Pts',(16.1142508533011,15.3299774848519,6.16206357463772));
#132406=CARTESIAN_POINT('Ctrl Pts',(16.1172428075483,15.2997760684677,6.17555377561747));
#132407=CARTESIAN_POINT('Ctrl Pts',(16.1202405638427,15.2695160849972,6.18907013701815));
#132408=CARTESIAN_POINT('Ctrl Pts',(16.1232293029821,15.2383828600024,6.2005247098438));
#132409=CARTESIAN_POINT('Ctrl Pts',(16.1261468812994,15.206675390044,6.2097932364135));
#132410=CARTESIAN_POINT('Ctrl Pts',(16.1271796065214,15.1954520053085,6.21307398507493));
#132411=CARTESIAN_POINT('Ctrl Pts',(16.1282032758492,15.1841569214697,6.21608116023705));
#132412=CARTESIAN_POINT('Ctrl Pts',(16.1292147798966,15.1728042606247,6.21881040925667));
#132413=CARTESIAN_POINT('Ctrl Pts',(16.1292160389828,15.1727901292151,6.21881380653385));
#132414=CARTESIAN_POINT('Ctrl Pts',(16.1292172980521,15.1727759976877,6.21881720338843));
#132415=CARTESIAN_POINT('Ctrl Pts',(16.1292185571045,15.1727618660425,6.21882059982039));
#132416=CARTESIAN_POINT('Ctrl Pts',(16.1318073112161,15.1437056057739,6.22580404788869));
#132417=CARTESIAN_POINT('Ctrl Pts',(16.1343247953239,15.1141470703662,6.2309990673935));
#132418=CARTESIAN_POINT('Ctrl Pts',(16.136811972548,15.0843321497203,6.23436422354309));
#132419=CARTESIAN_POINT('Ctrl Pts',(16.1370686296446,15.0812554847797,6.23471148114836));
#132420=CARTESIAN_POINT('Ctrl Pts',(16.1373249640148,15.0781761308462,6.23503927325043));
#132421=CARTESIAN_POINT('Ctrl Pts',(16.1375810206711,15.0750943859746,6.23534756896916));
#132422=CARTESIAN_POINT('Ctrl Pts',(16.1403153021134,15.0421862088087,6.23863968124789));
#132423=CARTESIAN_POINT('Ctrl Pts',(16.1430187536206,15.0090001903672,6.23970655581451));
#132424=CARTESIAN_POINT('Ctrl Pts',(16.1457383503359,14.9758622872572,6.2385466710135));
#132425=CARTESIAN_POINT('Ctrl Pts',(16.1484551438058,14.9427585412983,6.23738798177278));
#132426=CARTESIAN_POINT('Ctrl Pts',(16.1511885297621,14.9097029541351,6.23400767228793));
#132427=CARTESIAN_POINT('Ctrl Pts',(16.1539677230478,14.8770099384777,6.22844649006174));
#132428=CARTESIAN_POINT('Ctrl Pts',(16.156745591655,14.8443325056635,6.22288795852497));
#132429=CARTESIAN_POINT('Ctrl Pts',(16.1595694487211,14.8120173320975,6.2151509486412));
#132430=CARTESIAN_POINT('Ctrl Pts',(16.1624456676721,14.7803666548847,6.20531193827383));
#132431=CARTESIAN_POINT('Ctrl Pts',(16.1653242384874,14.7486900971328,6.19546488261594));
#132432=CARTESIAN_POINT('Ctrl Pts',(16.1682552985183,14.7176791223776,6.18351248750219));
#132433=CARTESIAN_POINT('Ctrl Pts',(16.1712204169545,14.6876247431539,6.16956415940564));
#132434=CARTESIAN_POINT('Ctrl Pts',(16.1741869546514,14.657555978334,6.1556091549105));
#132435=CARTESIAN_POINT('Ctrl Pts',(16.1771874204658,14.6284447284925,6.13965615574805));
#132436=CARTESIAN_POINT('Ctrl Pts',(16.1801793747131,14.6005704943679,6.12184778282757));
#132437=CARTESIAN_POINT('Ctrl Pts',(16.1831771310075,14.5726422060673,6.10400487561566));
#132438=CARTESIAN_POINT('Ctrl Pts',(16.1861658701469,14.5459558905665,6.08429889930881));
#132439=CARTESIAN_POINT('Ctrl Pts',(16.1890834484642,14.5207797401804,6.06291126999443));
#132440=CARTESIAN_POINT('Ctrl Pts',(16.190116173686,14.5118682243058,6.05534076397057));
#132441=CARTESIAN_POINT('Ctrl Pts',(16.1911398430137,14.5031457892696,6.04755994471023));
#132442=CARTESIAN_POINT('Ctrl Pts',(16.1921513470609,14.4946238357708,6.03957821451086));
#132443=CARTESIAN_POINT('Ctrl Pts',(16.1921526061468,14.4946132279322,6.03956827912393));
#132444=CARTESIAN_POINT('Ctrl Pts',(16.192153865216,14.4946026203798,6.0395583434045));
#132445=CARTESIAN_POINT('Ctrl Pts',(16.1921551242685,14.4945920131137,6.03954840735257));
#132446=CARTESIAN_POINT('Ctrl Pts',(16.1947166929634,14.4730113081658,6.01933330168643));
#132447=CARTESIAN_POINT('Ctrl Pts',(16.1972091345585,14.452614857626,5.99773757154862));
#132448=CARTESIAN_POINT('Ctrl Pts',(16.1996718468606,14.43357266356,5.9749388885128));
#132449=CARTESIAN_POINT('Ctrl Pts',(16.1999144880521,14.4316965123535,5.97269262547517));
#132450=CARTESIAN_POINT('Ctrl Pts',(16.2001568406503,14.4298335115516,5.97043472646499));
#132451=CARTESIAN_POINT('Ctrl Pts',(16.2003989423363,14.4279838256286,5.96816538861521));
#132452=CARTESIAN_POINT('Ctrl Pts',(16.2030952611575,14.4073836263946,5.94289146980893));
#132453=CARTESIAN_POINT('Ctrl Pts',(16.2057612561779,14.3884341056361,5.91619331180146));
#132454=CARTESIAN_POINT('Ctrl Pts',(16.2084419210787,14.3713139137559,5.88833392594945));
#132455=CARTESIAN_POINT('Ctrl Pts',(16.2111203234904,14.354208171369,5.86049805350281));
#132456=CARTESIAN_POINT('Ctrl Pts',(16.2138138376184,14.3389283469309,5.83150336784397));
#132457=CARTESIAN_POINT('Ctrl Pts',(16.2165508775019,14.3256113643662,5.80162775802377));
#132458=CARTESIAN_POINT('Ctrl Pts',(16.2181370964783,14.317893665191,5.78431370297036));
#132459=CARTESIAN_POINT('Ctrl Pts',(16.219737581817,14.3108344778435,5.76670402266428));
#132460=CARTESIAN_POINT('Ctrl Pts',(16.2213546080976,14.30445467332,5.74885446889987));
#132461=CARTESIAN_POINT('Origin',(13.2437274406976,15.,5.5));
#132462=CARTESIAN_POINT('',(16.700862083818,14.3042076661182,5.74898599983006));
#132463=CARTESIAN_POINT('',(16.6220124733702,14.3041067945379,5.74904127694233));
#132464=CARTESIAN_POINT('',(13.2437274406976,14.3042076641721,5.74898599439144));
#132465=CARTESIAN_POINT('Ctrl Pts',(16.700862083818,14.3042076680644,5.74898600526868));
#132466=CARTESIAN_POINT('Ctrl Pts',(16.697396127047,14.3169106070095,5.78448441611916));
#132467=CARTESIAN_POINT('Ctrl Pts',(16.6939254027009,14.3323145057219,5.81896699613406));
#132468=CARTESIAN_POINT('Ctrl Pts',(16.6897732313851,14.3544659205637,5.85983832197784));
#132469=CARTESIAN_POINT('Ctrl Pts',(16.688996145643,14.3587806335753,5.86747191840067));
#132470=CARTESIAN_POINT('Ctrl Pts',(16.6877680762403,14.3658822725913,5.87952998952657));
#132471=CARTESIAN_POINT('Ctrl Pts',(16.6873122307183,14.3685818987329,5.88400454741232));
#132472=CARTESIAN_POINT('Ctrl Pts',(16.6864000885435,14.3741159482379,5.89296089698515));
#132473=CARTESIAN_POINT('Ctrl Pts',(16.6859438966717,14.3769515865792,5.89744155900922));
#132474=CARTESIAN_POINT('Ctrl Pts',(16.6847086223169,14.3848090117365,5.90956646588726));
#132475=CARTESIAN_POINT('Ctrl Pts',(16.6839352496254,14.389925076977,5.91714895901912));
#132476=CARTESIAN_POINT('Ctrl Pts',(16.6805305820722,14.4132676031344,5.95039634309607));
#132477=CARTESIAN_POINT('Ctrl Pts',(16.6779756732664,14.4329841427522,5.97497927212336));
#132478=CARTESIAN_POINT('Ctrl Pts',(16.6709924275226,14.491334276544,6.0388989526216));
#132479=CARTESIAN_POINT('Ctrl Pts',(16.6666044889277,14.532881654663,6.07528474817825));
#132480=CARTESIAN_POINT('Ctrl Pts',(16.6609552702171,14.5886114384769,6.11403984977518));
#132481=CARTESIAN_POINT('Ctrl Pts',(16.6598792605772,14.5993290448737,6.1210863314509));
#132482=CARTESIAN_POINT('Ctrl Pts',(16.6580498333824,14.6176798711039,6.13247872328531));
#132483=CARTESIAN_POINT('Ctrl Pts',(16.657301961652,14.6252173257953,6.13697405708416));
#132484=CARTESIAN_POINT('Ctrl Pts',(16.6557630176664,14.6407869965908,6.14588778183389));
#132485=CARTESIAN_POINT('Ctrl Pts',(16.6549716400314,14.6488249119773,6.1502930489956));
#132486=CARTESIAN_POINT('Ctrl Pts',(16.6529121896104,14.6698091237733,6.16129117495463));
#132487=CARTESIAN_POINT('Ctrl Pts',(16.6516365194986,14.6828709577164,6.16765345707789));
#132488=CARTESIAN_POINT('Ctrl Pts',(16.6487607324478,14.7124306441505,6.18098855034726));
#132489=CARTESIAN_POINT('Ctrl Pts',(16.6471550449522,14.7290112016229,6.18775468449328));
#132490=CARTESIAN_POINT('Ctrl Pts',(16.6412055574989,14.7907332606746,6.21036351310312));
#132491=CARTESIAN_POINT('Ctrl Pts',(16.6367767559302,14.8371363246202,6.22241516764773));
#132492=CARTESIAN_POINT('Ctrl Pts',(16.6304810244729,14.9052189388955,6.2332005389251));
#132493=CARTESIAN_POINT('Ctrl Pts',(16.6285694675975,14.9261996763351,6.23560871969796));
#132494=CARTESIAN_POINT('Ctrl Pts',(16.626055319452,14.9544398303568,6.23762939867577));
#132495=CARTESIAN_POINT('Ctrl Pts',(16.6254202808825,14.961630338924,6.23803837322562));
#132496=CARTESIAN_POINT('Ctrl Pts',(16.6243576536445,14.9737733086633,6.23855106742231));
#132497=CARTESIAN_POINT('Ctrl Pts',(16.6239273106088,14.9787227017123,6.23871022856819));
#132498=CARTESIAN_POINT('Ctrl Pts',(16.6229947321607,14.9895208619953,6.23894884305295));
#132499=CARTESIAN_POINT('Ctrl Pts',(16.6224935252894,14.9953695683326,6.23900864080523));
#132500=CARTESIAN_POINT('Ctrl Pts',(16.6209730864128,15.013231077231,6.23897918571332));
#132501=CARTESIAN_POINT('Ctrl Pts',(16.6199647447072,15.0252422497625,6.23866648522819));
#132502=CARTESIAN_POINT('Ctrl Pts',(16.6181927584174,15.0465439788686,6.23759163177315));
#132503=CARTESIAN_POINT('Ctrl Pts',(16.6174252207451,15.0558372439007,6.23694638609425));
#132504=CARTESIAN_POINT('Ctrl Pts',(16.6135991214926,15.1023627928273,6.23283082534517));
#132505=CARTESIAN_POINT('Ctrl Pts',(16.6106116320748,15.1393077540344,6.2267137368902));
#132506=CARTESIAN_POINT('Ctrl Pts',(16.6046124570518,15.2115688710089,6.20903336982803));
#132507=CARTESIAN_POINT('Ctrl Pts',(16.6016095028439,15.2467892629939,6.1975558763184));
#132508=CARTESIAN_POINT('Ctrl Pts',(16.5975229952409,15.2920899763909,6.17893168891085));
#132509=CARTESIAN_POINT('Ctrl Pts',(16.5965147704517,15.303067313797,6.1741030799319));
#132510=CARTESIAN_POINT('Ctrl Pts',(16.5947567091956,15.3218290512853,6.16529944744243));
#132511=CARTESIAN_POINT('Ctrl Pts',(16.5940111956343,15.3296696118895,6.16144933747986));
#132512=CARTESIAN_POINT('Ctrl Pts',(16.5924490395351,15.3458467900563,6.15314645713499));
#132513=CARTESIAN_POINT('Ctrl Pts',(16.5916317210831,15.3541698543324,6.14867094340432));
#132514=CARTESIAN_POINT('Ctrl Pts',(16.5894093478587,15.3764080282279,6.13615736343223));
#132515=CARTESIAN_POINT('Ctrl Pts',(16.5879941970488,15.3901496615505,6.12782350210994));
#132516=CARTESIAN_POINT('Ctrl Pts',(16.5847236518551,15.4209303547678,6.10775510370916));
#132517=CARTESIAN_POINT('Ctrl Pts',(16.5828598036385,15.4377696776775,6.09574003307194));
#132518=CARTESIAN_POINT('Ctrl Pts',(16.5764441604068,15.4934134864181,6.05240335973789));
#132519=CARTESIAN_POINT('Ctrl Pts',(16.5718167743148,15.529542652497,6.01787128497162));
#132520=CARTESIAN_POINT('Ctrl Pts',(16.5659423369917,15.5716277765433,5.9686001628841));
#132521=CARTESIAN_POINT('Ctrl Pts',(16.5645991596043,15.5809897409556,5.95694138781113));
#132522=CARTESIAN_POINT('Ctrl Pts',(16.5627011205613,15.5938991736403,5.93982594648477));
#132523=CARTESIAN_POINT('Ctrl Pts',(16.5621304802254,15.5977377943766,5.93459478845771));
#132524=CARTESIAN_POINT('Ctrl Pts',(16.5611368577866,15.6043525755692,5.92532687817746));
#132525=CARTESIAN_POINT('Ctrl Pts',(16.560712074633,15.6071582351041,5.92131208336096));
#132526=CARTESIAN_POINT('Ctrl Pts',(16.5597509218269,15.6134555281901,5.91210730662903));
#132527=CARTESIAN_POINT('Ctrl Pts',(16.5592161696538,15.6169215213975,5.90690043275396));
#132528=CARTESIAN_POINT('Ctrl Pts',(16.5574544292141,15.628199438263,5.88948245097071));
#132529=CARTESIAN_POINT('Ctrl Pts',(16.5562439569937,15.6357187740616,5.87708465255163));
#132530=CARTESIAN_POINT('Ctrl Pts',(16.5531138415788,15.6544122566918,5.8441124417685));
#132531=CARTESIAN_POINT('Ctrl Pts',(16.551217036634,15.6649825220733,5.82321385037684));
#132532=CARTESIAN_POINT('Ctrl Pts',(16.5449197963812,15.6968646566975,5.75196624729619));
#132533=CARTESIAN_POINT('Ctrl Pts',(16.5405636196362,15.7135816886529,5.6997691359747));
#132534=CARTESIAN_POINT('Ctrl Pts',(16.5349452604301,15.7269404095369,5.63358346970776));
#132535=CARTESIAN_POINT('Ctrl Pts',(16.5338647721879,15.7291580570579,5.62089412508123));
#132536=CARTESIAN_POINT('Ctrl Pts',(16.5320300864344,15.7323285768023,5.59946371602465));
#132537=CARTESIAN_POINT('Ctrl Pts',(16.5312815117741,15.7334591455888,5.5907515445291));
#132538=CARTESIAN_POINT('Ctrl Pts',(16.5297430990076,15.7354498665781,5.57292633795143));
#132539=CARTESIAN_POINT('Ctrl Pts',(16.5289529810346,15.7362965390031,5.56381337809065));
#132540=CARTESIAN_POINT('Ctrl Pts',(16.526901438242,15.7380432181176,5.54027496343849));
#132541=CARTESIAN_POINT('Ctrl Pts',(16.5256325308499,15.7386896072786,5.52583534290751));
#132542=CARTESIAN_POINT('Ctrl Pts',(16.5227754168504,15.7391861397318,5.49361525066842));
#132543=CARTESIAN_POINT('Ctrl Pts',(16.5211817603835,15.738818750493,5.47584084334564));
#132544=CARTESIAN_POINT('Ctrl Pts',(16.5153274600387,15.7351503425984,5.41124689602264));
#132545=CARTESIAN_POINT('Ctrl Pts',(16.5109849894262,15.7280329359563,5.36475745325885));
#132546=CARTESIAN_POINT('Ctrl Pts',(16.5046705211652,15.7111389927466,5.29777930728284));
#132547=CARTESIAN_POINT('Ctrl Pts',(16.5026617415075,15.7047563474995,5.27654846837885));
#132548=CARTESIAN_POINT('Ctrl Pts',(16.5000485123283,15.6950277626955,5.24878272790917));
#132549=CARTESIAN_POINT('Ctrl Pts',(16.4994081496334,15.6925260842247,5.24196638968495));
#132550=CARTESIAN_POINT('Ctrl Pts',(16.4983395300471,15.6881470916671,5.23055765927861));
#132551=CARTESIAN_POINT('Ctrl Pts',(16.4979084411969,15.6863233397076,5.22594548918882));
#132552=CARTESIAN_POINT('Ctrl Pts',(16.4969777369728,15.6822596192105,5.2159636404118));
#132553=CARTESIAN_POINT('Ctrl Pts',(16.4964791027891,15.6800024631341,5.21060148807503));
#132554=CARTESIAN_POINT('Ctrl Pts',(16.4949759442973,15.6729612828783,5.19441168204379));
#132555=CARTESIAN_POINT('Ctrl Pts',(16.4939819524131,15.6679799518022,5.18367115264801));
#132556=CARTESIAN_POINT('Ctrl Pts',(16.4915748546421,15.6551676489959,5.15769971834669));
#132557=CARTESIAN_POINT('Ctrl Pts',(16.490173371231,15.647061095932,5.14261203177783));
#132558=CARTESIAN_POINT('Ctrl Pts',(16.4858317139062,15.6201453132324,5.09644091755839));
#132559=CARTESIAN_POINT('Ctrl Pts',(16.482932120987,15.59956492672,5.06645396042234));
#132560=CARTESIAN_POINT('Ctrl Pts',(16.479600182799,15.5738216035869,5.03430327486165));
#132561=CARTESIAN_POINT('Ctrl Pts',(16.479206018556,15.5707431444231,5.03053548097517));
#132562=CARTESIAN_POINT('Ctrl Pts',(16.4766041782743,15.5502167787151,5.00591313281881));
#132563=CARTESIAN_POINT('Ctrl Pts',(16.474375420893,15.5316683697906,4.98600700717737));
#132564=CARTESIAN_POINT('Ctrl Pts',(16.4711614918809,15.5039506608614,4.95936939270322));
#132565=CARTESIAN_POINT('Ctrl Pts',(16.4702134048853,15.4956574270842,4.95175606788137));
#132566=CARTESIAN_POINT('Ctrl Pts',(16.4685215121982,15.4806781161585,4.93862254815849));
#132567=CARTESIAN_POINT('Ctrl Pts',(16.4677810460902,15.4740625612184,4.93302489546963));
#132568=CARTESIAN_POINT('Ctrl Pts',(16.4662026513189,15.4598457832204,4.92141836183003));
#132569=CARTESIAN_POINT('Ctrl Pts',(16.4653636903635,15.4522218190262,4.91544011151077));
#132570=CARTESIAN_POINT('Ctrl Pts',(16.4630027609883,15.4305951544256,4.89915808710946));
#132571=CARTESIAN_POINT('Ctrl Pts',(16.4614683549362,15.4163441192289,4.88919671160989));
#132572=CARTESIAN_POINT('Ctrl Pts',(16.4588081736029,15.3913298926544,4.87299422773725));
#132573=CARTESIAN_POINT('Ctrl Pts',(16.4576911601493,15.3807353319335,4.86650501463834));
#132574=CARTESIAN_POINT('Ctrl Pts',(16.4523334905467,15.3294785882724,4.83686032626347));
#132575=CARTESIAN_POINT('Ctrl Pts',(16.448004017321,15.2868427769925,4.81733540362058));
#132576=CARTESIAN_POINT('Ctrl Pts',(16.4416874909688,15.2215838565512,4.79464963332036));
#132577=CARTESIAN_POINT('Ctrl Pts',(16.4396647726037,15.2001915974189,4.78828229344947));
#132578=CARTESIAN_POINT('Ctrl Pts',(16.4370369193232,15.1714841896348,4.78113487363869));
#132579=CARTESIAN_POINT('Ctrl Pts',(16.4363953816452,15.1644006132314,4.77948188899048));
#132580=CARTESIAN_POINT('Ctrl Pts',(16.4353254359835,15.1524459984151,4.7768777215563));
#132581=CARTESIAN_POINT('Ctrl Pts',(16.4348941789191,15.1475878987098,4.77587057029255));
#132582=CARTESIAN_POINT('Ctrl Pts',(16.433963870749,15.1370183212739,4.7737901520935));
#132583=CARTESIAN_POINT('Ctrl Pts',(16.4334657905818,15.1313037382141,4.77273519343357));
#132584=CARTESIAN_POINT('Ctrl Pts',(16.4319663339226,15.1139494771497,4.76974269173346));
#132585=CARTESIAN_POINT('Ctrl Pts',(16.4309754139526,15.1022746024243,4.7680162759527));
#132586=CARTESIAN_POINT('Ctrl Pts',(16.4285778563981,15.0736499010753,4.76448175641307));
#132587=CARTESIAN_POINT('Ctrl Pts',(16.4271827196844,15.0566688658583,4.76297888505902));
#132588=CARTESIAN_POINT('Ctrl Pts',(16.4228864016805,15.003866178877,4.76014175807839));
#132589=CARTESIAN_POINT('Ctrl Pts',(16.4200248331092,14.9679894091775,4.76082436630523));
#132590=CARTESIAN_POINT('Ctrl Pts',(16.416338688891,14.9225986707608,4.76499999611553));
#132591=CARTESIAN_POINT('Ctrl Pts',(16.4155484592389,14.9129131602611,4.7660845791198));
#132592=CARTESIAN_POINT('Ctrl Pts',(16.4127980377695,14.8794349905929,4.77050549853386));
#132593=CARTESIAN_POINT('Ctrl Pts',(16.4108213625446,14.8557878135062,4.77480982872409));
#132594=CARTESIAN_POINT('Ctrl Pts',(16.4078915331915,14.8217068295919,4.78274623831879));
#132595=CARTESIAN_POINT('Ctrl Pts',(16.4069660897088,14.8110768529963,4.78547258161488));
#132596=CARTESIAN_POINT('Ctrl Pts',(16.4053002469293,14.792212183767,4.79076130537416));
#132597=CARTESIAN_POINT('Ctrl Pts',(16.4045628499817,14.7839540346447,4.79323311490274));
#132598=CARTESIAN_POINT('Ctrl Pts',(16.4029620675492,14.7662382783447,4.79887524195338));
#132599=CARTESIAN_POINT('Ctrl Pts',(16.4020972545112,14.7567979574469,4.80209369250876));
#132600=CARTESIAN_POINT('Ctrl Pts',(16.3995645114551,14.7295466866203,4.81200438870312));
#132601=CARTESIAN_POINT('Ctrl Pts',(16.3978809421187,14.7119268698687,4.81919409007022));
#132602=CARTESIAN_POINT('Ctrl Pts',(16.3937876159225,14.6703002890944,4.83808496325697));
#132603=CARTESIAN_POINT('Ctrl Pts',(16.3913611777954,14.6466128856851,4.85042268709786));
#132604=CARTESIAN_POINT('Ctrl Pts',(16.3847133964604,14.5841709859134,4.88737345685745));
#132605=CARTESIAN_POINT('Ctrl Pts',(16.3804642203436,14.5469542834794,4.91435928191798));
#132606=CARTESIAN_POINT('Ctrl Pts',(16.3753883718121,14.5044745958915,4.95164883622007));
#132607=CARTESIAN_POINT('Ctrl Pts',(16.3744399295171,14.4966229480837,4.95884752259677));
#132608=CARTESIAN_POINT('Ctrl Pts',(16.3730094108972,14.4848851923959,4.97008578154907));
#132609=CARTESIAN_POINT('Ctrl Pts',(16.3725195867291,14.4808852239365,4.97400361262789));
#132610=CARTESIAN_POINT('Ctrl Pts',(16.3715958623317,14.4733734307764,4.98153032409678));
#132611=CARTESIAN_POINT('Ctrl Pts',(16.3711614344424,14.4698535181646,4.98513005670938));
#132612=CARTESIAN_POINT('Ctrl Pts',(16.3700648563114,14.4610079819816,4.99436308511563));
#132613=CARTESIAN_POINT('Ctrl Pts',(16.3694063748255,14.4557336417689,5.00004477037013));
#132614=CARTESIAN_POINT('Ctrl Pts',(16.3660162860778,14.4288302185592,5.02995647632269));
#132615=CARTESIAN_POINT('Ctrl Pts',(16.3633741567363,14.4087232839458,5.05551344210995));
#132616=CARTESIAN_POINT('Ctrl Pts',(16.3561068289732,14.3578586366054,5.12975363443086));
#132617=CARTESIAN_POINT('Ctrl Pts',(16.3515324557921,14.3310078152352,5.18081896613052));
#132618=CARTESIAN_POINT('Ctrl Pts',(16.3457023003394,14.3058621021702,5.24613093422921));
#132619=CARTESIAN_POINT('Ctrl Pts',(16.3446537826047,14.3016719122226,5.25789512980407));
#132620=CARTESIAN_POINT('Ctrl Pts',(16.3428564887666,14.2950646186758,5.27804689881088));
#132621=CARTESIAN_POINT('Ctrl Pts',(16.3421127916269,14.2924943198568,5.28638171969691));
#132622=CARTESIAN_POINT('Ctrl Pts',(16.340569722473,14.2875010275874,5.30365355611688));
#132623=CARTESIAN_POINT('Ctrl Pts',(16.339769880511,14.2850973039703,5.3125944774282));
#132624=CARTESIAN_POINT('Ctrl Pts',(16.3376573781823,14.2792337748496,5.3361619311406));
#132625=CARTESIAN_POINT('Ctrl Pts',(16.3363363354901,14.276051302438,5.35085216691753));
#132626=CARTESIAN_POINT('Ctrl Pts',(16.3341102538847,14.2714926668311,5.37550518710915));
#132627=CARTESIAN_POINT('Ctrl Pts',(16.3332127604705,14.2698679289812,5.38541800972001));
#132628=CARTESIAN_POINT('Ctrl Pts',(16.329471934667,14.263973833022,5.42662469209067));
#132629=CARTESIAN_POINT('Ctrl Pts',(16.3265850864333,14.2615111181704,5.45814030991767));
#132630=CARTESIAN_POINT('Ctrl Pts',(16.3199160195203,14.2605008124614,5.53071569711654));
#132631=CARTESIAN_POINT('Ctrl Pts',(16.3161331652276,14.2633436787261,5.57169786656442));
#132632=CARTESIAN_POINT('Ctrl Pts',(16.3116824894046,14.270910620945,5.62094333208096));
#132633=CARTESIAN_POINT('Ctrl Pts',(16.3109015453472,14.2724043019312,5.62962690176481));
#132634=CARTESIAN_POINT('Ctrl Pts',(16.3096688947638,14.2750324092338,5.64342380203196));
#132635=CARTESIAN_POINT('Ctrl Pts',(16.3092122670681,14.2760664444781,5.64855506591789));
#132636=CARTESIAN_POINT('Ctrl Pts',(16.308300127549,14.278255609077,5.65885228363348));
#132637=CARTESIAN_POINT('Ctrl Pts',(16.3078447020281,14.2794118903938,5.66401766855364));
#132638=CARTESIAN_POINT('Ctrl Pts',(16.3066140564873,14.2827066742947,5.67802833003765));
#132639=CARTESIAN_POINT('Ctrl Pts',(16.305844474352,14.2849532951371,5.68684762410514));
#132640=CARTESIAN_POINT('Ctrl Pts',(16.3035172559882,14.2923025791173,5.71362032009262));
#132641=CARTESIAN_POINT('Ctrl Pts',(16.3019823719936,14.2979219165104,5.73142044878301));
#132642=CARTESIAN_POINT('Ctrl Pts',(16.3004622294836,14.3042076679214,5.74898600486896));
#132643=CARTESIAN_POINT('',(16.2439139857417,14.2608925795155,5.49943231825045));
#132644=CARTESIAN_POINT('Ctrl Pts',(16.2211956582352,14.3041893991231,5.74893494673765));
#132645=CARTESIAN_POINT('Ctrl Pts',(16.2216107958238,14.3025459439714,5.74434124251259));
#132646=CARTESIAN_POINT('Ctrl Pts',(16.2220273713241,14.3009480621918,5.73973149340631));
#132647=CARTESIAN_POINT('Ctrl Pts',(16.2228901658018,14.2977448441053,5.73018608030003));
#132648=CARTESIAN_POINT('Ctrl Pts',(16.2233365551274,14.2961456329688,5.72524866831267));
#132649=CARTESIAN_POINT('Ctrl Pts',(16.2246645325414,14.291560634912,5.71056715181112));
#132650=CARTESIAN_POINT('Ctrl Pts',(16.2255508068294,14.2887243917547,5.70077810113298));
#132651=CARTESIAN_POINT('Ctrl Pts',(16.2283906682725,14.2803487823945,5.6694614364029));
#132652=CARTESIAN_POINT('Ctrl Pts',(16.2303672975008,14.2755783160696,5.64774322464492));
#132653=CARTESIAN_POINT('Ctrl Pts',(16.2361851377203,14.2645785358762,5.58409284640734));
#132654=CARTESIAN_POINT('Ctrl Pts',(16.2400864757065,14.2609679963021,5.54180086186545));
#132655=CARTESIAN_POINT('Ctrl Pts',(16.2439755819599,14.2610002137098,5.49943798301597));
#132656=CARTESIAN_POINT('Ctrl Pts',(16.2439139857417,14.2608925795155,5.49943231825045));
#132657=CARTESIAN_POINT('Ctrl Pts',(16.2468365782592,14.2608415859776,5.46711637395115));
#132658=CARTESIAN_POINT('Ctrl Pts',(16.2497445498771,14.2629206022102,5.43486649125833));
#132659=CARTESIAN_POINT('Ctrl Pts',(16.2525823523489,14.2671249071872,5.40291827216697));
#132660=CARTESIAN_POINT('Ctrl Pts',(16.2534241981765,14.2683721316287,5.39344070098001));
#132661=CARTESIAN_POINT('Ctrl Pts',(16.2542598688615,14.2698064864784,5.38398934254864));
#132662=CARTESIAN_POINT('Ctrl Pts',(16.2550879142251,14.2714281697843,5.37456952060223));
#132663=CARTESIAN_POINT('Ctrl Pts',(16.2550891733112,14.2714306356384,5.37455519727192));
#132664=CARTESIAN_POINT('Ctrl Pts',(16.2550904323805,14.2714331019271,5.37454087400039));
#132665=CARTESIAN_POINT('Ctrl Pts',(16.2550916914329,14.2714355686507,5.37452655078767));
#132666=CARTESIAN_POINT('Ctrl Pts',(16.2576804455433,14.2765074311787,5.34507640618042));
#132667=CARTESIAN_POINT('Ctrl Pts',(16.26019792965,14.2834206029643,5.3158718979988));
#132668=CARTESIAN_POINT('Ctrl Pts',(16.262685106873,14.2921159389437,5.28715526692191));
#132669=CARTESIAN_POINT('Ctrl Pts',(16.2629417639707,14.2930132291228,5.28419193679843));
#132670=CARTESIAN_POINT('Ctrl Pts',(16.2631980983421,14.2939294622358,5.28123383178361));
#132671=CARTESIAN_POINT('Ctrl Pts',(16.2634541549996,14.2948645488209,5.27828123786169));
#132672=CARTESIAN_POINT('Ctrl Pts',(16.2661884364418,14.3048497994343,5.24675218938546));
#132673=CARTESIAN_POINT('Ctrl Pts',(16.268891887949,14.3169888650432,5.21584760837416));
#132674=CARTESIAN_POINT('Ctrl Pts',(16.2716114846644,14.3311542867762,5.18586750192992));
#132675=CARTESIAN_POINT('Ctrl Pts',(16.2743282781342,14.3453051073906,5.15591829771342));
#132676=CARTESIAN_POINT('Ctrl Pts',(16.2770616640904,14.3614775464346,5.12689157639859));
#132677=CARTESIAN_POINT('Ctrl Pts',(16.2798408573761,14.3795098824573,5.09906003173981));
#132678=CARTESIAN_POINT('Ctrl Pts',(16.2826187259834,14.397533623523,5.07124175274624));
#132679=CARTESIAN_POINT('Ctrl Pts',(16.2854425830495,14.4174151856514,5.04461741703861));
#132680=CARTESIAN_POINT('Ctrl Pts',(16.2883188020004,14.4389648407132,5.01943440967743));
#132681=CARTESIAN_POINT('Ctrl Pts',(16.2911973728157,14.4605321167784,4.9942308103458));
#132682=CARTESIAN_POINT('Ctrl Pts',(16.2941284328466,14.4837701232007,4.97047085744732));
#132683=CARTESIAN_POINT('Ctrl Pts',(16.2970935512828,14.5084633227428,4.94837860849926));
#132684=CARTESIAN_POINT('Ctrl Pts',(16.3000600889796,14.5331683417405,4.92627578504663));
#132685=CARTESIAN_POINT('Ctrl Pts',(16.3030605547941,14.5593300841324,4.90584232511856));
#132686=CARTESIAN_POINT('Ctrl Pts',(16.3060525090414,14.5867070545747,4.88727858186716));
#132687=CARTESIAN_POINT('Ctrl Pts',(16.3090502653358,14.6141371148912,4.86867883949768));
#132688=CARTESIAN_POINT('Ctrl Pts',(16.3120390044752,14.6427875121405,4.85195640921161));
#132689=CARTESIAN_POINT('Ctrl Pts',(16.3149565827925,14.6723855863172,4.83728592043362));
#132690=CARTESIAN_POINT('Ctrl Pts',(16.3159893080143,14.6828623154375,4.8320930576794));
#132691=CARTESIAN_POINT('Ctrl Pts',(16.317012977342,14.6934574794728,4.82715701469034));
#132692=CARTESIAN_POINT('Ctrl Pts',(16.3180244813892,14.7041579350933,4.82248454661349));
#132693=CARTESIAN_POINT('Ctrl Pts',(16.3180257404753,14.7041712546597,4.82247873048274));
#132694=CARTESIAN_POINT('Ctrl Pts',(16.3180269995446,14.7041845744162,4.82247291474745));
#132695=CARTESIAN_POINT('Ctrl Pts',(16.318028258597,14.7041978943625,4.82246709940767));
#132696=CARTESIAN_POINT('Ctrl Pts',(16.3206170127076,14.7315852099172,4.81051010339048));
#132697=CARTESIAN_POINT('Ctrl Pts',(16.3231344968146,14.7597798089517,4.8002261436611));
#132698=CARTESIAN_POINT('Ctrl Pts',(16.3256216740378,14.788546836311,4.79169901605146));
#132699=CARTESIAN_POINT('Ctrl Pts',(16.3258783311352,14.7915153669307,4.79081908365207));
#132700=CARTESIAN_POINT('Ctrl Pts',(16.3261346655063,14.7944899491001,4.78995784657965));
#132701=CARTESIAN_POINT('Ctrl Pts',(16.3263907221636,14.797470294757,4.78911538736027));
#132702=CARTESIAN_POINT('Ctrl Pts',(16.3291250036058,14.8292956880439,4.78011925098165));
#132703=CARTESIAN_POINT('Ctrl Pts',(16.331828455113,14.8617837753845,4.77326547667347));
#132704=CARTESIAN_POINT('Ctrl Pts',(16.3345480518283,14.8946138889352,4.76861256365983));
#132705=CARTESIAN_POINT('Ctrl Pts',(16.3372648452982,14.9274101625911,4.76396444667244));
#132706=CARTESIAN_POINT('Ctrl Pts',(16.3399982312544,14.9605475209686,4.76151213864556));
#132707=CARTESIAN_POINT('Ctrl Pts',(16.3427774245401,14.9937092705058,4.76127050225467));
#132708=CARTESIAN_POINT('Ctrl Pts',(16.3455552931473,15.0268552137816,4.76102898103767));
#132709=CARTESIAN_POINT('Ctrl Pts',(16.3483791502134,15.0600254369483,4.76299571935205));
#132710=CARTESIAN_POINT('Ctrl Pts',(16.3512553691644,15.0929089861587,4.76714827089704));
#132711=CARTESIAN_POINT('Ctrl Pts',(16.3541339399797,15.1258194240193,4.77130421795463));
#132712=CARTESIAN_POINT('Ctrl Pts',(16.3570650000106,15.1584427019205,4.77764945578953));
#132713=CARTESIAN_POINT('Ctrl Pts',(16.3600301184468,15.1904731593011,4.7861271540139));
#132714=CARTESIAN_POINT('Ctrl Pts',(16.3629966561436,15.222518948132,4.79460891010755));
#132715=CARTESIAN_POINT('Ctrl Pts',(16.365997121958,15.2539713716961,4.80522531729318));
#132716=CARTESIAN_POINT('Ctrl Pts',(16.3689890762053,15.2845302955342,4.8178848294456));
#132717=CARTESIAN_POINT('Ctrl Pts',(16.3719868324997,15.3151484797431,4.83056889113345));
#132718=CARTESIAN_POINT('Ctrl Pts',(16.3749755716391,15.3448696292337,4.84530450140765));
#132719=CARTESIAN_POINT('Ctrl Pts',(16.3778931499564,15.3733979594889,4.86195993922172));
#132720=CARTESIAN_POINT('Ctrl Pts',(16.3789258751784,15.383496035013,4.86785540760101));
#132721=CARTESIAN_POINT('Ctrl Pts',(16.3799495445063,15.3934447213567,4.87399101363608));
#132722=CARTESIAN_POINT('Ctrl Pts',(16.3809610485537,15.4032311492864,4.88035949358426));
#132723=CARTESIAN_POINT('Ctrl Pts',(16.3809623076398,15.403243331102,4.88036742085342));
#132724=CARTESIAN_POINT('Ctrl Pts',(16.3809635667091,15.4032555126918,4.88037534849871));
#132725=CARTESIAN_POINT('Ctrl Pts',(16.3809648257615,15.4032676940556,4.88038327652013));
#132726=CARTESIAN_POINT('Ctrl Pts',(16.3835535798724,15.4283139551783,4.89668418480728));
#132727=CARTESIAN_POINT('Ctrl Pts',(16.3860710639795,15.4524066853143,4.91457931255719));
#132728=CARTESIAN_POINT('Ctrl Pts',(16.3885582412028,15.4753467568033,4.93391857026285));
#132729=CARTESIAN_POINT('Ctrl Pts',(16.3888148983,15.4777139914744,4.93591422931627));
#132730=CARTESIAN_POINT('Ctrl Pts',(16.3890712326708,15.4800689381655,4.9379252227119));
#132731=CARTESIAN_POINT('Ctrl Pts',(16.3893272893277,15.4824113695533,4.93995135522031));
#132732=CARTESIAN_POINT('Ctrl Pts',(16.3920615707698,15.5074248441075,4.96158725636354));
#132733=CARTESIAN_POINT('Ctrl Pts',(16.3947650222769,15.5310132754005,4.9849546685096));
#132734=CARTESIAN_POINT('Ctrl Pts',(16.397484618992,15.5529514804485,5.00981791677843));
#132735=CARTESIAN_POINT('Ctrl Pts',(16.4002014124618,15.5748670725211,5.03465553706087));
#132736=CARTESIAN_POINT('Ctrl Pts',(16.4029347984178,15.5951361406784,5.06098542902574));
#132737=CARTESIAN_POINT('Ctrl Pts',(16.4057139917034,15.613572135076,5.08855124356168));
#132738=CARTESIAN_POINT('Ctrl Pts',(16.4084918603105,15.6319993421162,5.11610391909035));
#132739=CARTESIAN_POINT('Ctrl Pts',(16.4113157173763,15.6485954289492,5.1448910979431));
#132740=CARTESIAN_POINT('Ctrl Pts',(16.4141919363272,15.6632081644352,5.17464071062246));
#132741=CARTESIAN_POINT('Ctrl Pts',(16.4170705071423,15.6778328486537,5.20441464935378));
#132742=CARTESIAN_POINT('Ctrl Pts',(16.4200015671731,15.6904710096386,5.23515252812032));
#132743=CARTESIAN_POINT('Ctrl Pts',(16.4229666856092,15.7010020464407,5.26656779241988));
#132744=CARTESIAN_POINT('Ctrl Pts',(16.4259332233059,15.7115381239473,5.29799809370624));
#132745=CARTESIAN_POINT('Ctrl Pts',(16.4289336891202,15.7199649479335,5.33010653009044));
#132746=CARTESIAN_POINT('Ctrl Pts',(16.4319256433674,15.7261939526705,5.36259207416802));
#132747=CARTESIAN_POINT('Ctrl Pts',(16.4349233996618,15.7324350367965,5.39514061475019));
#132748=CARTESIAN_POINT('Ctrl Pts',(16.4379121388011,15.7364693053219,5.42806795315767));
#132749=CARTESIAN_POINT('Ctrl Pts',(16.4408297171184,15.7382441408574,5.46105460492308));
#132750=CARTESIAN_POINT('Ctrl Pts',(16.441862442341,15.7388723733242,5.47273077727572));
#132751=CARTESIAN_POINT('Ctrl Pts',(16.4428861116694,15.7392178859971,5.48441421180992));
#132752=CARTESIAN_POINT('Ctrl Pts',(16.4438976157173,15.7392796697724,5.49609016536313));
#132753=CARTESIAN_POINT('Ctrl Pts',(16.4438988748035,15.7392797466787,5.49610469919649));
#132754=CARTESIAN_POINT('Ctrl Pts',(16.4439001338727,15.7392798231467,5.49611923304801));
#132755=CARTESIAN_POINT('Ctrl Pts',(16.4439013929252,15.7392798991764,5.49613376691765));
#132756=CARTESIAN_POINT('Ctrl Pts',(16.4464901470361,15.7394362246864,5.52601704601413));
#132757=CARTESIAN_POINT('Ctrl Pts',(16.4490076311434,15.7377366584986,5.55598046900575));
#132758=CARTESIAN_POINT('Ctrl Pts',(16.4514948083669,15.7341970729513,5.5857751850253));
#132759=CARTESIAN_POINT('Ctrl Pts',(16.4517514654643,15.733831815605,5.58884976501857));
#132760=CARTESIAN_POINT('Ctrl Pts',(16.4520077998353,15.7334469934861,5.59192251302494));
#132761=CARTESIAN_POINT('Ctrl Pts',(16.4522638564925,15.7330426446669,5.59499313182244));
#132762=CARTESIAN_POINT('Ctrl Pts',(16.454998137935,15.7287248367074,5.62778249994964));
#132763=CARTESIAN_POINT('Ctrl Pts',(16.4577015894424,15.7221771993878,5.66033366716369));
#132764=CARTESIAN_POINT('Ctrl Pts',(16.460421186158,15.7134727644175,5.69232896005582));
#132765=CARTESIAN_POINT('Ctrl Pts',(16.463137979628,15.7047773016111,5.7242912735511));
#132766=CARTESIAN_POINT('Ctrl Pts',(16.4658713655845,15.693930054134,5.7556988452053));
#132767=CARTESIAN_POINT('Ctrl Pts',(16.4686505588704,15.6810425646902,5.78625490248517));
#132768=CARTESIAN_POINT('Ctrl Pts',(16.4714284274778,15.6681612179569,5.81679639548447));
#132769=CARTESIAN_POINT('Ctrl Pts',(16.4742522845441,15.6532418888684,5.84648722545286));
#132770=CARTESIAN_POINT('Ctrl Pts',(16.4771285034953,15.6364281210601,5.87505064095674));
#132771=CARTESIAN_POINT('Ctrl Pts',(16.4800070743107,15.6196006047506,5.9036374125673));
#132772=CARTESIAN_POINT('Ctrl Pts',(16.4829381343418,15.6008756475668,5.93109494856035));
#132773=CARTESIAN_POINT('Ctrl Pts',(16.4859032527782,15.5804262839172,5.95716495227471));
#132774=CARTESIAN_POINT('Ctrl Pts',(16.4888697904752,15.5599671321338,5.98324743445488));
#132775=CARTESIAN_POINT('Ctrl Pts',(16.4918702562898,15.5377817769755,6.00794101795833));
#132776=CARTESIAN_POINT('Ctrl Pts',(16.4948622105372,15.5140729562227,6.03100620585586));
#132777=CARTESIAN_POINT('Ctrl Pts',(16.4978599668317,15.4903181589325,6.05411612214736));
#132778=CARTESIAN_POINT('Ctrl Pts',(16.5008487059713,15.4650335376564,6.07559105786966));
#132779=CARTESIAN_POINT('Ctrl Pts',(16.5037662842887,15.4384570130061,6.09521139358542));
#132780=CARTESIAN_POINT('Ctrl Pts',(16.5047990095091,15.429049811453,6.10215633672778));
#132781=CARTESIAN_POINT('Ctrl Pts',(16.5058226788356,15.4194810891018,6.10886912851364));
#132782=CARTESIAN_POINT('Ctrl Pts',(16.5068341828815,15.4097626054639,6.1153408194724));
#132783=CARTESIAN_POINT('Ctrl Pts',(16.5068354419677,15.4097505082231,6.11534887521515));
#132784=CARTESIAN_POINT('Ctrl Pts',(16.506836701037,15.4097384107261,6.11535693060174));
#132785=CARTESIAN_POINT('Ctrl Pts',(16.5068379600894,15.4097263129728,6.11536498563214));
#132786=CARTESIAN_POINT('Ctrl Pts',(16.5094267142004,15.3848519646828,6.13192703878028));
#132787=CARTESIAN_POINT('Ctrl Pts',(16.5119441983077,15.3588902034422,6.14698300756358));
#132788=CARTESIAN_POINT('Ctrl Pts',(16.5144313755313,15.3320576118916,6.16040931753061));
#132789=CARTESIAN_POINT('Ctrl Pts',(16.5146880326282,15.3292886998153,6.16179480695444));
#132790=CARTESIAN_POINT('Ctrl Pts',(16.5149443669988,15.3265105601295,6.16316294738053));
#132791=CARTESIAN_POINT('Ctrl Pts',(16.5152004236556,15.323723462026,6.16451360718012));
#132792=CARTESIAN_POINT('Ctrl Pts',(16.5179347050977,15.2939616479088,6.17893652463707));
#132793=CARTESIAN_POINT('Ctrl Pts',(16.5206381566049,15.2631727098718,6.1913659790012));
#132794=CARTESIAN_POINT('Ctrl Pts',(16.5233577533202,15.2316621446506,6.20168829630943));
#132795=CARTESIAN_POINT('Ctrl Pts',(16.52607454679,15.2001840591894,6.21199997380887));
#132796=CARTESIAN_POINT('Ctrl Pts',(16.5288079327462,15.1679861570418,6.22020932409411));
#132797=CARTESIAN_POINT('Ctrl Pts',(16.5315871260319,15.1353776527562,6.22624633234962));
#132798=CARTESIAN_POINT('Ctrl Pts',(16.5343649946392,15.1027846910322,6.23228046311734));
#132799=CARTESIAN_POINT('Ctrl Pts',(16.5371888517053,15.0697816585366,6.23614460733382));
#132800=CARTESIAN_POINT('Ctrl Pts',(16.5400650706562,15.0366786428791,6.2378064879869));
#132801=CARTESIAN_POINT('Ctrl Pts',(16.5429436414715,15.0035485591153,6.23946972754826));
#132802=CARTESIAN_POINT('Ctrl Pts',(16.5458747015025,14.9703183625751,6.23892719459613));
#132803=CARTESIAN_POINT('Ctrl Pts',(16.5488398199387,14.9372989419958,6.23618139203368));
#132804=CARTESIAN_POINT('Ctrl Pts',(16.5518063576355,14.9042637165967,6.23343427518667));
#132805=CARTESIAN_POINT('Ctrl Pts',(16.5548068234498,14.871439420416,6.22848163652201));
#132806=CARTESIAN_POINT('Ctrl Pts',(16.557798777697,14.8391375720869,6.22136112611124));
#132807=CARTESIAN_POINT('Ctrl Pts',(16.5607965339914,14.8067730834789,6.21422680748886));
#132808=CARTESIAN_POINT('Ctrl Pts',(16.5637852731306,14.7749330466829,6.20491568543388));
#132809=CARTESIAN_POINT('Ctrl Pts',(16.5667028514477,14.7439317229275,6.19350572657112));
#132810=CARTESIAN_POINT('Ctrl Pts',(16.5677355766706,14.7329582903388,6.1894669824385));
#132811=CARTESIAN_POINT('Ctrl Pts',(16.5687592459994,14.7220899513954,6.18516567679505));
#132812=CARTESIAN_POINT('Ctrl Pts',(16.5697707500476,14.7113406472614,6.1806067109747));
#132813=CARTESIAN_POINT('Ctrl Pts',(16.5697720091338,14.7113272668899,6.18060103612772));
#132814=CARTESIAN_POINT('Ctrl Pts',(16.5697732682031,14.7113138866751,6.18059536087092));
#132815=CARTESIAN_POINT('Ctrl Pts',(16.5697745272555,14.7113005066169,6.18058968520427));
#132816=CARTESIAN_POINT('Ctrl Pts',(16.5723632911273,14.6837894906899,6.16891982897771));
#132817=CARTESIAN_POINT('Ctrl Pts',(16.5748807844833,14.6569385324742,6.15551355888183));
#132818=CARTESIAN_POINT('Ctrl Pts',(16.5773679708376,14.6309699385419,6.14048383039845));
#132819=CARTESIAN_POINT('Ctrl Pts',(16.5776248130349,14.6282882614275,6.13893176797203));
#132820=CARTESIAN_POINT('Ctrl Pts',(16.5778813320413,14.6256160149713,6.13736243376493));
#132821=CARTESIAN_POINT('Ctrl Pts',(16.5781375729667,14.6229534576917,6.13577598057665));
#132822=CARTESIAN_POINT('Ctrl Pts',(16.5808718844585,14.5945416770366,6.11884715791783));
#132823=CARTESIAN_POINT('Ctrl Pts',(16.5835753690728,14.5672302344032,6.09996426653787));
#132824=CARTESIAN_POINT('Ctrl Pts',(16.586295002674,14.5412820633584,6.0793199811601));
#132825=CARTESIAN_POINT('Ctrl Pts',(16.5891089842951,14.5144337127617,6.05795951568898));
#132826=CARTESIAN_POINT('Ctrl Pts',(16.5919409097406,14.4890448400346,6.03471373893295));
#132827=CARTESIAN_POINT('Ctrl Pts',(16.5948228149276,14.4653687253073,6.00982733631907));
#132828=CARTESIAN_POINT('Ctrl Pts',(16.5976046135951,14.4425150295311,5.98580539349394));
#132829=CARTESIAN_POINT('Ctrl Pts',(16.6004330743049,14.4212568161143,5.96025523821325));
#132830=CARTESIAN_POINT('Ctrl Pts',(16.6033137008858,14.401790641754,5.93341904099662));
#132831=CARTESIAN_POINT('Ctrl Pts',(16.6061942600457,14.3823249229993,5.90658347188088));
#132832=CARTESIAN_POINT('Ctrl Pts',(16.6091270143045,14.3646510995958,5.87846199693993));
#132833=CARTESIAN_POINT('Ctrl Pts',(16.612092674658,14.3489367067677,5.84931589224036));
#132834=CARTESIAN_POINT('Ctrl Pts',(16.6150613409843,14.3332063859398,5.82014024525074));
#132835=CARTESIAN_POINT('Ctrl Pts',(16.6180628108254,14.3194395724126,5.78993776234784));
#132836=CARTESIAN_POINT('Ctrl Pts',(16.6210538554812,14.3077750183842,5.75899004845362));
#132837=CARTESIAN_POINT('Ctrl Pts',(16.6213735567761,14.3065282389286,5.75568216597613));
#132838=CARTESIAN_POINT('Ctrl Pts',(16.6216931184145,14.3053054482088,5.75236578931324));
#132839=CARTESIAN_POINT('Ctrl Pts',(16.6220124733702,14.3041067945379,5.74904127694233));
#132840=CARTESIAN_POINT('Origin',(13.2437274406976,15.,5.5));
#132841=CARTESIAN_POINT('',(17.1015120386236,14.3042076643465,5.74898599487892));
#132842=CARTESIAN_POINT('',(17.0220282051085,14.3041366315448,5.74902320646588));
#132843=CARTESIAN_POINT('',(13.2437274406976,14.3042076641721,5.74898599439144));
#132844=CARTESIAN_POINT('Ctrl Pts',(17.1015120386236,14.3042076645209,5.7489859953664));
#132845=CARTESIAN_POINT('Ctrl Pts',(17.1010629887414,14.306009822866,5.75402213389287));
#132846=CARTESIAN_POINT('Ctrl Pts',(17.1006122891737,14.3078666430159,5.7590386633245));
#132847=CARTESIAN_POINT('Ctrl Pts',(17.0993979148554,14.312996258662,5.77244816797651));
#132848=CARTESIAN_POINT('Ctrl Pts',(17.0986311940599,14.3163681184237,5.78080167409815));
#132849=CARTESIAN_POINT('Ctrl Pts',(17.0970874669747,14.3234155464965,5.79738127426927));
#132850=CARTESIAN_POINT('Ctrl Pts',(17.0963105928316,14.3270905347949,5.80560592432059));
#132851=CARTESIAN_POINT('Ctrl Pts',(17.0943428025253,14.3367138154367,5.82612726321211));
#132852=CARTESIAN_POINT('Ctrl Pts',(17.0931455852938,14.3428541473218,5.83832946778211));
#132853=CARTESIAN_POINT('Ctrl Pts',(17.0878380526966,14.3712930007245,5.89114566203298));
#132854=CARTESIAN_POINT('Ctrl Pts',(17.0836133526042,14.3970407641257,5.9297744573182));
#132855=CARTESIAN_POINT('Ctrl Pts',(17.0767942921161,14.4437964901717,5.98737637993273));
#132856=CARTESIAN_POINT('Ctrl Pts',(17.0742280057754,14.4625759471951,6.00800945654015));
#132857=CARTESIAN_POINT('Ctrl Pts',(17.0706800586025,14.4904828425965,6.03538681560242));
#132858=CARTESIAN_POINT('Ctrl Pts',(17.0696686565435,14.4986669011208,6.04305794538599));
#132859=CARTESIAN_POINT('Ctrl Pts',(17.067883286662,14.5135582107111,6.05639225507572));
#132860=CARTESIAN_POINT('Ctrl Pts',(17.0671057338256,14.5201976486511,6.06212781514659));
#132861=CARTESIAN_POINT('Ctrl Pts',(17.0658771095241,14.5309533831471,6.07108982414434));
#132862=CARTESIAN_POINT('Ctrl Pts',(17.0654211690367,14.5350042696298,6.07439297751985));
#132863=CARTESIAN_POINT('Ctrl Pts',(17.0645661448299,14.5427183944272,6.08054808511209));
#132864=CARTESIAN_POINT('Ctrl Pts',(17.064166421157,14.5463740626173,6.08340899767106));
#132865=CARTESIAN_POINT('Ctrl Pts',(17.0630517243684,14.5567003592184,6.09133456648626));
#132866=CARTESIAN_POINT('Ctrl Pts',(17.0623418065563,14.5634307619532,6.09632076947767));
#132867=CARTESIAN_POINT('Ctrl Pts',(17.0577403497939,14.6079677298945,6.12815751129518));
#132868=CARTESIAN_POINT('Ctrl Pts',(17.0540303975087,14.6481510188862,6.15151732457892));
#132869=CARTESIAN_POINT('Ctrl Pts',(17.0469629073583,14.7278513642259,6.18830946972849));
#132870=CARTESIAN_POINT('Ctrl Pts',(17.0436224891662,14.7668246479606,6.20246951165992));
#132871=CARTESIAN_POINT('Ctrl Pts',(17.0391043645555,14.8192384898768,6.21666799252661));
#132872=CARTESIAN_POINT('Ctrl Pts',(17.0380212531432,14.8317874139924,6.21971676368964));
#132873=CARTESIAN_POINT('Ctrl Pts',(17.0361760108917,14.8530885201933,6.22430438714678));
#132874=CARTESIAN_POINT('Ctrl Pts',(17.0354194559501,14.8618005907772,6.22601703619758));
#132875=CARTESIAN_POINT('Ctrl Pts',(17.0339650543251,14.8784936012233,6.22898727087771));
#132876=CARTESIAN_POINT('Ctrl Pts',(17.0332681652654,14.8864685026522,6.23027175342549));
#132877=CARTESIAN_POINT('Ctrl Pts',(17.0313991246292,14.9077827406307,6.23334718886206));
#132878=CARTESIAN_POINT('Ctrl Pts',(17.0302199909763,14.9211519719025,6.23490479594459));
#132879=CARTESIAN_POINT('Ctrl Pts',(17.0246506061707,14.9838846854003,6.24048221769656));
#132880=CARTESIAN_POINT('Ctrl Pts',(17.0201263347773,15.0335209023497,6.23989740917214));
#132881=CARTESIAN_POINT('Ctrl Pts',(17.0131866491669,15.108530822838,6.23144852099819));
#132882=CARTESIAN_POINT('Ctrl Pts',(17.0107980610273,15.1341760510584,6.22718141130333));
#132883=CARTESIAN_POINT('Ctrl Pts',(17.0070430561451,15.174615643203,6.21823994784909));
#132884=CARTESIAN_POINT('Ctrl Pts',(17.0056563068226,15.1895802475821,6.21443590866868));
#132885=CARTESIAN_POINT('Ctrl Pts',(17.0037252111576,15.2105584999238,6.20839746862312));
#132886=CARTESIAN_POINT('Ctrl Pts',(17.0031634824079,15.2166780735814,6.20654969879856));
#132887=CARTESIAN_POINT('Ctrl Pts',(17.0021793433855,15.227439621733,6.20314733182012));
#132888=CARTESIAN_POINT('Ctrl Pts',(17.0017552602062,15.232091188662,6.2016257095619));
#132889=CARTESIAN_POINT('Ctrl Pts',(17.0007876390334,15.2427358597911,6.19802616507192));
#132890=CARTESIAN_POINT('Ctrl Pts',(17.000245841114,15.2487178710238,6.19591713168326));
#132891=CARTESIAN_POINT('Ctrl Pts',(16.9985159888412,15.2678619419067,6.18888924453129));
#132892=CARTESIAN_POINT('Ctrl Pts',(16.997342980813,15.2809120440398,6.18367163761283));
#132893=CARTESIAN_POINT('Ctrl Pts',(16.9916447820021,15.3442202180977,6.15624090201944));
#132894=CARTESIAN_POINT('Ctrl Pts',(16.9873047325161,15.3920444802288,6.12884170678909));
#132895=CARTESIAN_POINT('Ctrl Pts',(16.981318040755,15.4515491397386,6.08530086199236));
#132896=CARTESIAN_POINT('Ctrl Pts',(16.9797825423878,15.4662765191978,6.07363738065959));
#132897=CARTESIAN_POINT('Ctrl Pts',(16.976984981612,15.4919588065323,6.05165508682364));
#132898=CARTESIAN_POINT('Ctrl Pts',(16.9757303191036,15.5030732358454,6.04153860379621));
#132899=CARTESIAN_POINT('Ctrl Pts',(16.973680316267,15.5205240239193,6.02465364322095));
#132900=CARTESIAN_POINT('Ctrl Pts',(16.9728937334068,15.5270552882818,6.01809208793202));
#132901=CARTESIAN_POINT('Ctrl Pts',(16.9713555527193,15.5394971974875,6.0051136983365));
#132902=CARTESIAN_POINT('Ctrl Pts',(16.9706046849001,15.5454208898163,5.99871145275268));
#132903=CARTESIAN_POINT('Ctrl Pts',(16.9687669541212,15.5595473143835,5.98289104202235));
#132904=CARTESIAN_POINT('Ctrl Pts',(16.9676753233456,15.567626966765,5.97336723648909));
#132905=CARTESIAN_POINT('Ctrl Pts',(16.961503387527,15.611539664855,5.91886411174524));
#132906=CARTESIAN_POINT('Ctrl Pts',(16.9562302586365,15.6422611978186,5.87003474592157));
#132907=CARTESIAN_POINT('Ctrl Pts',(16.9481829916127,15.6799640864898,5.79099051701522));
#132908=CARTESIAN_POINT('Ctrl Pts',(16.9454271662665,15.6912501490172,5.76305939908778));
#132909=CARTESIAN_POINT('Ctrl Pts',(16.9419335674514,15.7036541653223,5.72599244626899));
#132910=CARTESIAN_POINT('Ctrl Pts',(16.9411365006676,15.7063506742697,5.71741784093578));
#132911=CARTESIAN_POINT('Ctrl Pts',(16.9398846894468,15.7103792329684,5.70374032055653));
#132912=CARTESIAN_POINT('Ctrl Pts',(16.9394247738157,15.7118141618425,5.69866901433246));
#132913=CARTESIAN_POINT('Ctrl Pts',(16.93856834987,15.7144026134699,5.68913266812467));
#132914=CARTESIAN_POINT('Ctrl Pts',(16.9381711314264,15.7155688222134,5.68467139604451));
#132915=CARTESIAN_POINT('Ctrl Pts',(16.9370738941703,15.7186919723345,5.67224992483934));
#132916=CARTESIAN_POINT('Ctrl Pts',(16.9363786691551,15.7205584339007,5.66426730857187));
#132917=CARTESIAN_POINT('Ctrl Pts',(16.931657781287,15.73242601812,5.60940908720544));
#132918=CARTESIAN_POINT('Ctrl Pts',(16.9278284164877,15.7379804895321,5.56168074581195));
#132919=CARTESIAN_POINT('Ctrl Pts',(16.9217092438539,15.7393937807021,5.48570329407221));
#132920=CARTESIAN_POINT('Ctrl Pts',(16.9194463639833,15.7383186904235,5.45765739397033));
#132921=CARTESIAN_POINT('Ctrl Pts',(16.9155369902868,15.7337870368565,5.41020776228871));
#132922=CARTESIAN_POINT('Ctrl Pts',(16.9139113140119,15.731144315119,5.3907574938111));
#132923=CARTESIAN_POINT('Ctrl Pts',(16.9114158379383,15.7259786288951,5.36151713602058));
#132924=CARTESIAN_POINT('Ctrl Pts',(16.9105634616441,15.7240236218185,5.35163474920394));
#132925=CARTESIAN_POINT('Ctrl Pts',(16.9089706594558,15.7200240015546,5.33338493673109));
#132926=CARTESIAN_POINT('Ctrl Pts',(16.9082320696553,15.7180338863259,5.32500723829367));
#132927=CARTESIAN_POINT('Ctrl Pts',(16.9065535349365,15.7132102905085,5.3061715964801));
#132928=CARTESIAN_POINT('Ctrl Pts',(16.9056110541433,15.7102923453717,5.29573760669279));
#132929=CARTESIAN_POINT('Ctrl Pts',(16.9024902911401,15.6999545920789,5.26167724369267));
#132930=CARTESIAN_POINT('Ctrl Pts',(16.9002826684072,15.6915774701594,5.23836194032731));
#132931=CARTESIAN_POINT('Ctrl Pts',(16.8941641740181,15.6655130597364,5.17587332999429));
#132932=CARTESIAN_POINT('Ctrl Pts',(16.8902004338957,15.6455555552518,5.13775264625651));
#132933=CARTESIAN_POINT('Ctrl Pts',(16.8838122837411,15.6079988528801,5.07908161270821));
#132934=CARTESIAN_POINT('Ctrl Pts',(16.8813782184418,15.5923824361585,5.05737343289217));
#132935=CARTESIAN_POINT('Ctrl Pts',(16.8783242124831,15.5708506426264,5.03062973650073));
#132936=CARTESIAN_POINT('Ctrl Pts',(16.8776522086612,15.5659871648315,5.02477642728545));
#132937=CARTESIAN_POINT('Ctrl Pts',(16.8765517994293,15.5578043703098,5.01523211441731));
#132938=CARTESIAN_POINT('Ctrl Pts',(16.8761200477903,15.5545368592671,5.01149770005004));
#132939=CARTESIAN_POINT('Ctrl Pts',(16.8752040842733,15.5474796194494,5.00359411594678));
#132940=CARTESIAN_POINT('Ctrl Pts',(16.8747206298936,15.5436794176455,4.99943488666151));
#132941=CARTESIAN_POINT('Ctrl Pts',(16.8733166114837,15.5324329879911,4.98740514017314));
#132942=CARTESIAN_POINT('Ctrl Pts',(16.8724046388137,15.5248604090546,4.97965399453943));
#132943=CARTESIAN_POINT('Ctrl Pts',(16.870246488778,15.5063641917029,4.96153647205967));
#132944=CARTESIAN_POINT('Ctrl Pts',(16.8690089825265,15.4952886193859,4.95133168784819));
#132945=CARTESIAN_POINT('Ctrl Pts',(16.8633519836663,15.4428528917104,4.90590144068372));
#132946=CARTESIAN_POINT('Ctrl Pts',(16.8590557435465,15.3980011826466,4.87496631705344));
#132947=CARTESIAN_POINT('Ctrl Pts',(16.8528986192143,15.3317577763217,4.8393226121397));
#132948=CARTESIAN_POINT('Ctrl Pts',(16.8511703161143,15.3129423560662,4.83020543042086));
#132949=CARTESIAN_POINT('Ctrl Pts',(16.848552660313,15.2843353138525,4.81781227586705));
#132950=CARTESIAN_POINT('Ctrl Pts',(16.8476835965648,15.2748194829559,4.81392355263777));
#132951=CARTESIAN_POINT('Ctrl Pts',(16.846148564366,15.2580021904839,4.80745702613958));
#132952=CARTESIAN_POINT('Ctrl Pts',(16.8454855530226,15.2507353738999,4.80479307872245));
#132953=CARTESIAN_POINT('Ctrl Pts',(16.8439416446739,15.2338164194497,4.79889051058087));
#132954=CARTESIAN_POINT('Ctrl Pts',(16.843058147837,15.2241367733724,4.795736328985));
#132955=CARTESIAN_POINT('Ctrl Pts',(16.8403953716461,15.1949905876826,4.7869005464086));
#132956=CARTESIAN_POINT('Ctrl Pts',(16.8385977990153,15.1753538551609,4.78181964873577));
#132957=CARTESIAN_POINT('Ctrl Pts',(16.8341223707168,15.1266032869994,4.77132418064754));
#132958=CARTESIAN_POINT('Ctrl Pts',(16.8314228819217,15.0973265194249,4.76683968628251));
#132959=CARTESIAN_POINT('Ctrl Pts',(16.8246068168924,15.0233946123894,4.76002167337448));
#132960=CARTESIAN_POINT('Ctrl Pts',(16.8204783210415,14.9786428171387,4.75995961023736));
#132961=CARTESIAN_POINT('Ctrl Pts',(16.8157269978302,14.9256231363466,4.76470245771879));
#132962=CARTESIAN_POINT('Ctrl Pts',(16.8149681038898,14.9171035406863,4.76561414071456));
#132963=CARTESIAN_POINT('Ctrl Pts',(16.813761605079,14.9034554770302,4.76731518062048));
#132964=CARTESIAN_POINT('Ctrl Pts',(16.8133094160191,14.8983163777741,4.76801069900851));
#132965=CARTESIAN_POINT('Ctrl Pts',(16.8123970024063,14.8878919974392,4.7695334323692));
#132966=CARTESIAN_POINT('Ctrl Pts',(16.8119369730679,14.8826075634945,4.77036404136967));
#132967=CARTESIAN_POINT('Ctrl Pts',(16.8106784576917,14.8680853668081,4.77280851276459));
#132968=CARTESIAN_POINT('Ctrl Pts',(16.8098860480527,14.8588681707807,4.77454099930935));
#132969=CARTESIAN_POINT('Ctrl Pts',(16.8080714743497,14.8376527085884,4.77894840597014));
#132970=CARTESIAN_POINT('Ctrl Pts',(16.807054653506,14.8256830067229,4.78174818343004));
#132971=CARTESIAN_POINT('Ctrl Pts',(16.8033101110349,14.7815245768757,4.79324616393884));
#132972=CARTESIAN_POINT('Ctrl Pts',(16.8006374344958,14.7498644725895,4.80382112921949));
#132973=CARTESIAN_POINT('Ctrl Pts',(16.794830142338,14.6831619885609,4.83124132498402));
#132974=CARTESIAN_POINT('Ctrl Pts',(16.7916988447189,14.6485191436547,4.8487817891561));
#132975=CARTESIAN_POINT('Ctrl Pts',(16.7873489532573,14.6037902530223,4.8760415459075));
#132976=CARTESIAN_POINT('Ctrl Pts',(16.7862089460339,14.5923646076857,4.8834453345144));
#132977=CARTESIAN_POINT('Ctrl Pts',(16.7843722103877,14.5744753983555,4.89575215313949));
#132978=CARTESIAN_POINT('Ctrl Pts',(16.7836829649347,14.5678764309258,4.90045362391436));
#132979=CARTESIAN_POINT('Ctrl Pts',(16.7822317113484,14.5542294688992,4.91051882492109));
#132980=CARTESIAN_POINT('Ctrl Pts',(16.7814690203417,14.5471979840458,4.91590262656079));
#132981=CARTESIAN_POINT('Ctrl Pts',(16.779593885952,14.5302631960329,4.92935866077688));
#132982=CARTESIAN_POINT('Ctrl Pts',(16.7784763837562,14.5204696121644,4.93756354510834));
#132983=CARTESIAN_POINT('Ctrl Pts',(16.7735779817468,14.4788635628557,4.97429712734431));
#132984=CARTESIAN_POINT('Ctrl Pts',(16.7696992591317,14.4493517391013,5.00529611961691));
#132985=CARTESIAN_POINT('Ctrl Pts',(16.7616414124294,14.3945523610328,5.07387174876006));
#132986=CARTESIAN_POINT('Ctrl Pts',(16.7574739573392,14.3696951817944,5.11158186296606));
#132987=CARTESIAN_POINT('Ctrl Pts',(16.7526905897982,14.344406392462,5.15883924840147));
#132988=CARTESIAN_POINT('Ctrl Pts',(16.7519357170864,14.3405152226653,5.16642319531918));
#132989=CARTESIAN_POINT('Ctrl Pts',(16.750778616955,14.3346971724314,5.17826262774972));
#132990=CARTESIAN_POINT('Ctrl Pts',(16.750371365387,14.3326781132605,5.1824715881774));
#132991=CARTESIAN_POINT('Ctrl Pts',(16.7495161272941,14.328496886686,5.19140390675305));
#132992=CARTESIAN_POINT('Ctrl Pts',(16.7490687759639,14.3263443621103,5.19613149938571));
#132993=CARTESIAN_POINT('Ctrl Pts',(16.74788720829,14.3207565631175,5.20875526596189));
#132994=CARTESIAN_POINT('Ctrl Pts',(16.747157882137,14.3174089866019,5.21668979860382));
#132995=CARTESIAN_POINT('Ctrl Pts',(16.7433826877292,14.3006602953589,5.25840964077225));
#132996=CARTESIAN_POINT('Ctrl Pts',(16.7404445143384,14.2896245216491,5.29309574667645));
#132997=CARTESIAN_POINT('Ctrl Pts',(16.7334970652377,14.2696087221208,5.37696808254232));
#132998=CARTESIAN_POINT('Ctrl Pts',(16.7295073315853,14.2629733896052,5.42652006416303));
#132999=CARTESIAN_POINT('Ctrl Pts',(16.7242487805051,14.2609487094766,5.48977930657587));
#133000=CARTESIAN_POINT('Ctrl Pts',(16.7231239182279,14.2608850291573,5.50320730468455));
#133001=CARTESIAN_POINT('Ctrl Pts',(16.721304951729,14.2613687563276,5.52469920782863));
#133002=CARTESIAN_POINT('Ctrl Pts',(16.7206180532956,14.2616826171588,5.53276577919979));
#133003=CARTESIAN_POINT('Ctrl Pts',(16.7191666066163,14.2626192895688,5.54969509756409));
#133004=CARTESIAN_POINT('Ctrl Pts',(16.7184013146512,14.2632699133235,5.55855492479974));
#133005=CARTESIAN_POINT('Ctrl Pts',(16.716508785168,14.265260388448,5.58028816418176));
#133006=CARTESIAN_POINT('Ctrl Pts',(16.7153762601525,14.266778980117,5.59314169845822));
#133007=CARTESIAN_POINT('Ctrl Pts',(16.7102443827919,14.2751111994405,5.65065960781032));
#133008=CARTESIAN_POINT('Ctrl Pts',(16.7061345551986,14.2856735042036,5.69467485559293));
#133009=CARTESIAN_POINT('Ctrl Pts',(16.7016111543801,14.3014937675516,5.74130199537794));
#133010=CARTESIAN_POINT('Ctrl Pts',(16.7012366265413,14.3028349465736,5.74514992987891));
#133011=CARTESIAN_POINT('Ctrl Pts',(16.700862083818,14.3042076680644,5.74898600526868));
#133012=CARTESIAN_POINT('',(16.6438825647488,14.2609107381065,5.50061424492574));
#133013=CARTESIAN_POINT('Ctrl Pts',(16.6220124734468,14.3041067942504,5.74904127614493));
#133014=CARTESIAN_POINT('Ctrl Pts',(16.6250063842204,14.2928695735229,5.71787440921185));
#133015=CARTESIAN_POINT('Ctrl Pts',(16.6279833582934,14.283756768005,5.68599041700478));
#133016=CARTESIAN_POINT('Ctrl Pts',(16.6308791641049,14.2768707640213,5.65369834793092));
#133017=CARTESIAN_POINT('Ctrl Pts',(16.6314924590787,14.2754123956401,5.64685929692086));
#133018=CARTESIAN_POINT('Ctrl Pts',(16.6321020669945,14.2740537690431,5.64000203572447));
#133019=CARTESIAN_POINT('Ctrl Pts',(16.6327073172076,14.2727956189547,5.63312965534444));
#133020=CARTESIAN_POINT('Ctrl Pts',(16.632708576295,14.2727930016555,5.63311535889766));
#133021=CARTESIAN_POINT('Ctrl Pts',(16.6327098353647,14.2727903847881,5.63310106237043));
#133022=CARTESIAN_POINT('Ctrl Pts',(16.6327110944169,14.2727877683526,5.63308676576276));
#133023=CARTESIAN_POINT('Ctrl Pts',(16.6355088912899,14.2669736682273,5.60131762472554));
#133024=CARTESIAN_POINT('Ctrl Pts',(16.6382196158601,14.2632907979205,5.56914710280213));
#133025=CARTESIAN_POINT('Ctrl Pts',(16.6408988670525,14.2617459925759,5.53680734929748));
#133026=CARTESIAN_POINT('Ctrl Pts',(16.6418968418795,14.2611705792474,5.52476134928105));
#133027=CARTESIAN_POINT('Ctrl Pts',(16.6428904499833,14.2608919445406,5.51269237424421));
#133028=CARTESIAN_POINT('Ctrl Pts',(16.6438825646895,14.2609107381054,5.50061424564688));
#133029=CARTESIAN_POINT('Ctrl Pts',(16.643882564756,14.2609107381066,5.50061424483712));
#133030=CARTESIAN_POINT('Ctrl Pts',(16.6465594256901,14.2609614457461,5.46802580481307));
#133031=CARTESIAN_POINT('Ctrl Pts',(16.6492248243156,14.2631785677597,5.43537629957805));
#133032=CARTESIAN_POINT('Ctrl Pts',(16.6519184636661,14.2675388665903,5.40297839022479));
#133033=CARTESIAN_POINT('Ctrl Pts',(16.6546091468162,14.2718943801043,5.37061603674961));
#133034=CARTESIAN_POINT('Ctrl Pts',(16.6573283838935,14.2783879342007,5.33850485702922));
#133035=CARTESIAN_POINT('Ctrl Pts',(16.6600972580023,14.2869564952498,5.30694519284429));
#133036=CARTESIAN_POINT('Ctrl Pts',(16.6629358361132,14.2957407623855,5.27459104150862));
#133037=CARTESIAN_POINT('Ctrl Pts',(16.6658268589015,14.3067057226881,5.24281665383555));
#133038=CARTESIAN_POINT('Ctrl Pts',(16.6687685064462,14.3197454173502,5.21193175497587));
#133039=CARTESIAN_POINT('Ctrl Pts',(16.6716387263794,14.3324684886811,5.18179678775293));
#133040=CARTESIAN_POINT('Ctrl Pts',(16.6745570252431,14.3471665761053,5.15250863134965));
#133041=CARTESIAN_POINT('Ctrl Pts',(16.6774978093645,14.3637081100762,5.12434123441606));
#133042=CARTESIAN_POINT('Ctrl Pts',(16.6805483689687,14.3808671170754,5.0951223867577));
#133043=CARTESIAN_POINT('Ctrl Pts',(16.6836229974486,14.400010227424,5.06710973508013));
#133044=CARTESIAN_POINT('Ctrl Pts',(16.6866684347531,14.4209520888332,5.04059252345234));
#133045=CARTESIAN_POINT('Ctrl Pts',(16.689419504486,14.4398697401633,5.01663842720363));
#133046=CARTESIAN_POINT('Ctrl Pts',(16.6921461764301,14.4602558442988,4.99390399701323));
#133047=CARTESIAN_POINT('Ctrl Pts',(16.6947959895646,14.4819398756577,4.97259029927949));
#133048=CARTESIAN_POINT('Ctrl Pts',(16.6950795225656,14.4842600915272,4.97030970952653));
#133049=CARTESIAN_POINT('Ctrl Pts',(16.6953621755916,14.4865951746014,4.96804533731648));
#133050=CARTESIAN_POINT('Ctrl Pts',(16.6956438843734,14.4889449220592,4.96579739400117));
#133051=CARTESIAN_POINT('Ctrl Pts',(16.6956451434595,14.4889554241615,4.96578734690839));
#133052=CARTESIAN_POINT('Ctrl Pts',(16.6956464025288,14.4889659265784,4.96577730012147));
#133053=CARTESIAN_POINT('Ctrl Pts',(16.6956476615812,14.4889764293097,4.96576725364046));
#133054=CARTESIAN_POINT('Ctrl Pts',(16.698236415692,14.5105712324155,4.94511055288288));
#133055=CARTESIAN_POINT('Ctrl Pts',(16.7007538997991,14.5335000660394,4.92574657004337));
#133056=CARTESIAN_POINT('Ctrl Pts',(16.7032410770228,14.5575712947012,4.90783484987428));
#133057=CARTESIAN_POINT('Ctrl Pts',(16.7034977341184,14.5600552558676,4.90598650146011));
#133058=CARTESIAN_POINT('Ctrl Pts',(16.7037540684878,14.5625513363268,4.9041536210528));
#133059=CARTESIAN_POINT('Ctrl Pts',(16.7040101251433,14.5650592940532,4.90233638532723));
#133060=CARTESIAN_POINT('Ctrl Pts',(16.7067444065843,14.5918403291031,4.882931172413));
#133061=CARTESIAN_POINT('Ctrl Pts',(16.7094478580905,14.6199812640224,4.86530908904674));
#133062=CARTESIAN_POINT('Ctrl Pts',(16.712167454805,14.6492011879857,4.84963548072506));
#133063=CARTESIAN_POINT('Ctrl Pts',(16.714884248274,14.6783909932855,4.8339780280969));
#133064=CARTESIAN_POINT('Ctrl Pts',(16.7176176342296,14.7086571639179,4.82026463139376));
#133065=CARTESIAN_POINT('Ctrl Pts',(16.7203968275148,14.7397074937255,4.80861829985391));
#133066=CARTESIAN_POINT('Ctrl Pts',(16.7231746961215,14.770743023662,4.79697751943725));
#133067=CARTESIAN_POINT('Ctrl Pts',(16.7259985531871,14.8025617776855,4.78740157792263));
#133068=CARTESIAN_POINT('Ctrl Pts',(16.7288747721376,14.8348640907066,4.7799764809219));
#133069=CARTESIAN_POINT('Ctrl Pts',(16.7317533429524,14.8671928171055,4.77254531247075));
#133070=CARTESIAN_POINT('Ctrl Pts',(16.7346844029829,14.9000058437402,4.76726842074805));
#133071=CARTESIAN_POINT('Ctrl Pts',(16.7376495214185,14.932996634669,4.76419770746982));
#133072=CARTESIAN_POINT('Ctrl Pts',(16.7406160591147,14.9660032167143,4.76112552438776));
#133073=CARTESIAN_POINT('Ctrl Pts',(16.7436165249284,14.9991878060083,4.76026176405387));
#133074=CARTESIAN_POINT('Ctrl Pts',(16.7466084791747,15.0322371001287,4.76162383275038));
#133075=CARTESIAN_POINT('Ctrl Pts',(16.7496062354682,15.0653504839878,4.76298854279306));
#133076=CARTESIAN_POINT('Ctrl Pts',(16.7525949746064,15.0983281615029,4.76658822636295));
#133077=CARTESIAN_POINT('Ctrl Pts',(16.7555125529221,15.1308470796392,4.77240107403294));
#133078=CARTESIAN_POINT('Ctrl Pts',(16.7565452781547,15.1423576900358,4.77445862787109));
#133079=CARTESIAN_POINT('Ctrl Pts',(16.7575689474929,15.1538107410985,4.77679307545662));
#133080=CARTESIAN_POINT('Ctrl Pts',(16.7585804515502,15.1651916493713,4.77940202891363));
#133081=CARTESIAN_POINT('Ctrl Pts',(16.7585817106364,15.1652058159424,4.77940527645099));
#133082=CARTESIAN_POINT('Ctrl Pts',(16.7585829697057,15.165219982431,4.77940852441924));
#133083=CARTESIAN_POINT('Ctrl Pts',(16.7585842287581,15.1652341488371,4.77941177281841));
#133084=CARTESIAN_POINT('Ctrl Pts',(16.7611729828629,15.1943618804791,4.78609084857802));
#133085=CARTESIAN_POINT('Ctrl Pts',(16.7636904669635,15.2231433804942,4.79459499438346));
#133086=CARTESIAN_POINT('Ctrl Pts',(16.7661776441801,15.2513400157569,4.80485187133802));
#133087=CARTESIAN_POINT('Ctrl Pts',(16.7664343012795,15.2542496864349,4.80591030025496));
#133088=CARTESIAN_POINT('Ctrl Pts',(16.7666906356525,15.2571531011647,4.80698735709798));
#133089=CARTESIAN_POINT('Ctrl Pts',(16.7669466923117,15.2600499792979,4.80808293685841));
#133090=CARTESIAN_POINT('Ctrl Pts',(16.7696809737491,15.2909840707281,4.81978200147913));
#133091=CARTESIAN_POINT('Ctrl Pts',(16.7723844252509,15.3211765337626,4.8335973992389));
#133092=CARTESIAN_POINT('Ctrl Pts',(16.7751040219605,15.3503348016202,4.84938541269512));
#133093=CARTESIAN_POINT('Ctrl Pts',(16.7778208154246,15.3794630143664,4.86515715253361));
#133094=CARTESIAN_POINT('Ctrl Pts',(16.7805542013748,15.407559280387,4.88289688671094));
#133095=CARTESIAN_POINT('Ctrl Pts',(16.7833333946544,15.4343601838811,4.90242818442848));
#133096=CARTESIAN_POINT('Ctrl Pts',(16.7861112632556,15.461148312956,4.92195017272166));
#133097=CARTESIAN_POINT('Ctrl Pts',(16.7889351203156,15.4866424248478,4.94326171939172));
#133098=CARTESIAN_POINT('Ctrl Pts',(16.7918113392609,15.5106059100672,4.96615981685137));
#133099=CARTESIAN_POINT('Ctrl Pts',(16.7946899100705,15.5345889900622,4.9890766379265));
#133100=CARTESIAN_POINT('Ctrl Pts',(16.7976209700962,15.5570389841673,5.01358251613917));
#133101=CARTESIAN_POINT('Ctrl Pts',(16.8005860885279,15.5777439905351,5.03944995274565));
#133102=CARTESIAN_POINT('Ctrl Pts',(16.8035526262203,15.5984589074007,5.06532977085873));
#133103=CARTESIAN_POINT('Ctrl Pts',(16.8065530920311,15.617427095542,5.0925725843381));
#133104=CARTESIAN_POINT('Ctrl Pts',(16.8095450462761,15.6344617451785,5.12092627517138));
#133105=CARTESIAN_POINT('Ctrl Pts',(16.8125428025684,15.6515294286896,5.1493349499514));
#133106=CARTESIAN_POINT('Ctrl Pts',(16.8155315417069,15.6666557095804,5.1788591868016));
#133107=CARTESIAN_POINT('Ctrl Pts',(16.818449120025,15.6796811719533,5.20921716044695));
#133108=CARTESIAN_POINT('Ctrl Pts',(16.8194818452668,15.6842917504234,5.21996286878954));
#133109=CARTESIAN_POINT('Ctrl Pts',(16.8205055146144,15.6886394013387,5.23081275163717));
#133110=CARTESIAN_POINT('Ctrl Pts',(16.8215170186811,15.6927181004045,5.24175331502708));
#133111=CARTESIAN_POINT('Ctrl Pts',(16.8215182777672,15.6927231774313,5.24176693347078));
#133112=CARTESIAN_POINT('Ctrl Pts',(16.8215195368365,15.6927282540528,5.24178055208245));
#133113=CARTESIAN_POINT('Ctrl Pts',(16.8215207958888,15.692733330269,5.24179417086212));
#133114=CARTESIAN_POINT('Ctrl Pts',(16.8241095500145,15.7031706050995,5.26979592275927));
#133115=CARTESIAN_POINT('Ctrl Pts',(16.8266270341365,15.7118930947728,5.29851200578593));
#133116=CARTESIAN_POINT('Ctrl Pts',(16.8291142113749,15.7188300073692,5.32770332332898));
#133117=CARTESIAN_POINT('Ctrl Pts',(16.8293708684722,15.7195458421008,5.3307156373331));
#133118=CARTESIAN_POINT('Ctrl Pts',(16.8296272028431,15.7202426778066,5.33373296865914));
#133119=CARTESIAN_POINT('Ctrl Pts',(16.8298832595002,15.7209204478801,5.3367550251531));
#133120=CARTESIAN_POINT('Ctrl Pts',(16.8326175409575,15.7281579638471,5.36902582462275));
#133121=CARTESIAN_POINT('Ctrl Pts',(16.83532099248,15.7332200032505,5.40184084872015));
#133122=CARTESIAN_POINT('Ctrl Pts',(16.8380405892106,15.7360657380996,5.43487670433805));
#133123=CARTESIAN_POINT('Ctrl Pts',(16.8407573826957,15.7389085396853,5.467878507991));
#133124=CARTESIAN_POINT('Ctrl Pts',(16.8434907686671,15.7395401330745,5.50110048012781));
#133125=CARTESIAN_POINT('Ctrl Pts',(16.8462699619677,15.7379630432526,5.53422558867269));
#133126=CARTESIAN_POINT('Ctrl Pts',(16.8490478305899,15.7363867051369,5.56733490842048));
#133127=CARTESIAN_POINT('Ctrl Pts',(16.8518716876706,15.732604098387,5.60034738573811));
#133128=CARTESIAN_POINT('Ctrl Pts',(16.8547479066354,15.726654686108,5.63295376539774));
#133129=CARTESIAN_POINT('Ctrl Pts',(16.8576264774643,15.7207004090362,5.66558680706586));
#133130=CARTESIAN_POINT('Ctrl Pts',(16.8605575375082,15.7125758807696,5.69781307511916));
#133131=CARTESIAN_POINT('Ctrl Pts',(16.8635226559561,15.7023546065231,5.72933048503895));
#133132=CARTESIAN_POINT('Ctrl Pts',(16.8664891936645,15.692128439841,5.76086298083677));
#133133=CARTESIAN_POINT('Ctrl Pts',(16.8694896594893,15.6798033696425,5.79168595445143));
#133134=CARTESIAN_POINT('Ctrl Pts',(16.872481613745,15.6654872616378,5.82150474272471));
#133135=CARTESIAN_POINT('Ctrl Pts',(16.8754793700477,15.651143391601,5.85138135608267));
#133136=CARTESIAN_POINT('Ctrl Pts',(16.8784681091935,15.6348002466764,5.88024979143524));
#133137=CARTESIAN_POINT('Ctrl Pts',(16.8813856875151,15.6166055685332,5.90782193193857));
#133138=CARTESIAN_POINT('Ctrl Pts',(16.8824184126543,15.6101652610429,5.9175815474487));
#133139=CARTESIAN_POINT('Ctrl Pts',(16.8834420819007,15.6034933686891,5.92717883105449));
#133140=CARTESIAN_POINT('Ctrl Pts',(16.8844535858685,15.5965978499449,5.93660133118031));
#133141=CARTESIAN_POINT('Ctrl Pts',(16.8844548449546,15.5965892666349,5.93661305999177));
#133142=CARTESIAN_POINT('Ctrl Pts',(16.8844561040239,15.5965806829618,5.93662478855707));
#133143=CARTESIAN_POINT('Ctrl Pts',(16.8844573630763,15.5965720989255,5.93663651687619));
#133144=CARTESIAN_POINT('Ctrl Pts',(16.8870461171823,15.5789223498776,5.96075126681616));
#133145=CARTESIAN_POINT('Ctrl Pts',(16.8895636012852,15.5597330649106,5.9838265042824));
#133146=CARTESIAN_POINT('Ctrl Pts',(16.8920507785056,15.5391650265205,6.00567163107275));
#133147=CARTESIAN_POINT('Ctrl Pts',(16.8923074355913,15.5370425670722,6.00792587597812));
#133148=CARTESIAN_POINT('Ctrl Pts',(16.8925637699507,15.5349054701415,6.01016701056156));
#133149=CARTESIAN_POINT('Ctrl Pts',(16.8928198265962,15.5327539431289,6.01239481854684));
#133150=CARTESIAN_POINT('Ctrl Pts',(16.8955541080245,15.5097790254493,6.03618429679496));
#133151=CARTESIAN_POINT('Ctrl Pts',(16.8982575595193,15.4851533413693,6.05845593155753));
#133152=CARTESIAN_POINT('Ctrl Pts',(16.9009771562235,15.4591245586892,6.0789978014248));
#133153=CARTESIAN_POINT('Ctrl Pts',(16.9036939496823,15.4331226053783,6.09951849760078));
#133154=CARTESIAN_POINT('Ctrl Pts',(16.9064273356287,15.4057209095348,6.11831332109029));
#133155=CARTESIAN_POINT('Ctrl Pts',(16.9092065289052,15.3771856637107,6.13521005913319));
#133156=CARTESIAN_POINT('Ctrl Pts',(16.9119843975034,15.3486640189634,6.1520987434928));
#133157=CARTESIAN_POINT('Ctrl Pts',(16.9148082545612,15.3190101342279,6.16709137084068));
#133158=CARTESIAN_POINT('Ctrl Pts',(16.9176844735039,15.2885040169897,6.18005085748797));
#133159=CARTESIAN_POINT('Ctrl Pts',(16.9205630443112,15.2579729551071,6.19302094101928));
#133160=CARTESIAN_POINT('Ctrl Pts',(16.9234941043344,15.2265883307033,6.20395463414458));
#133161=CARTESIAN_POINT('Ctrl Pts',(16.9264592227623,15.1946428800942,6.21274723003703));
#133162=CARTESIAN_POINT('Ctrl Pts',(16.9294257604509,15.1626821387212,6.22154403452584));
#133163=CARTESIAN_POINT('Ctrl Pts',(16.9324262262567,15.1301599394637,6.22819757454658));
#133164=CARTESIAN_POINT('Ctrl Pts',(16.9354181804942,15.0973817131741,6.23263592389099));
#133165=CARTESIAN_POINT('Ctrl Pts',(16.9384159367794,15.0645399228002,6.23708288015662));
#133166=CARTESIAN_POINT('Ctrl Pts',(16.9414046759084,15.0314409111029,6.23930557025361));
#133167=CARTESIAN_POINT('Ctrl Pts',(16.9443222542134,14.9984065670693,6.23926897428871));
#133168=CARTESIAN_POINT('Ctrl Pts',(16.9453549795373,14.9867135120508,6.2392560205388));
#133169=CARTESIAN_POINT('Ctrl Pts',(16.946378648965,14.9750287081898,6.23896037407447));
#133170=CARTESIAN_POINT('Ctrl Pts',(16.9473901531091,14.963366931805,6.23838183572383));
#133171=CARTESIAN_POINT('Ctrl Pts',(16.9473914121955,14.9633524156181,6.23838111557875));
#133172=CARTESIAN_POINT('Ctrl Pts',(16.9473926712649,14.9633378994371,6.23838039499499));
#133173=CARTESIAN_POINT('Ctrl Pts',(16.9473939303175,14.963323383262,6.23837967397251));
#133174=CARTESIAN_POINT('Ctrl Pts',(16.949982684385,14.9334764912267,6.23689717049036));
#133175=CARTESIAN_POINT('Ctrl Pts',(16.9525001684468,14.9036513402204,6.23355717295173));
#133176=CARTESIAN_POINT('Ctrl Pts',(16.9549873456218,14.8740955363832,6.22838917508527));
#133177=CARTESIAN_POINT('Ctrl Pts',(16.9552440027414,14.8710456099215,6.22785587835838));
#133178=CARTESIAN_POINT('Ctrl Pts',(16.9555003371347,14.8679985854887,6.22730314674342));
#133179=CARTESIAN_POINT('Ctrl Pts',(16.9557563938139,14.8649547577722,6.22673103455314));
#133180=CARTESIAN_POINT('Ctrl Pts',(16.9584906752287,14.8324514792832,6.22062177884627));
#133181=CARTESIAN_POINT('Ctrl Pts',(16.9611941267044,14.8003083118629,6.21229910980488));
#133182=CARTESIAN_POINT('Ctrl Pts',(16.9639137233856,14.7688384464318,6.20185336829151));
#133183=CARTESIAN_POINT('Ctrl Pts',(16.9666305168212,14.7374010188114,6.19141839380819));
#133184=CARTESIAN_POINT('Ctrl Pts',(16.9693639027405,14.7066354875256,6.17886529019366));
#133185=CARTESIAN_POINT('Ctrl Pts',(16.972143095989,14.6768320623852,6.16432170530663));
#133186=CARTESIAN_POINT('Ctrl Pts',(16.9749209645589,14.6470428427916,6.14978505249452));
#133187=CARTESIAN_POINT('Ctrl Pts',(16.9777448215873,14.6182147553789,6.13326012794015));
#133188=CARTESIAN_POINT('Ctrl Pts',(16.9806210405032,14.5906162642677,6.11490543446986));
#133189=CARTESIAN_POINT('Ctrl Pts',(16.9834996112832,14.5629952060628,6.09653573249482));
#133190=CARTESIAN_POINT('Ctrl Pts',(16.9864306712816,14.53660572719,6.07633336382567));
#133191=CARTESIAN_POINT('Ctrl Pts',(16.9893957896912,14.5116962476894,6.05448526576069));
#133192=CARTESIAN_POINT('Ctrl Pts',(16.9923623273612,14.4867748452112,6.03262671005515));
#133193=CARTESIAN_POINT('Ctrl Pts',(16.9953627931549,14.4633349049778,6.00912070567207));
#133194=CARTESIAN_POINT('Ctrl Pts',(16.9983547473907,14.4416044468513,5.98418281774479));
#133195=CARTESIAN_POINT('Ctrl Pts',(17.0013525036737,14.4198318486605,5.95919656985214));
#133196=CARTESIAN_POINT('Ctrl Pts',(17.0043412428111,14.3997756562837,5.93277245066423));
#133197=CARTESIAN_POINT('Ctrl Pts',(17.0072588211384,14.381642112811,5.90516006526719));
#133198=CARTESIAN_POINT('Ctrl Pts',(17.008291546456,14.3752234438528,5.89538620274128));
#133199=CARTESIAN_POINT('Ctrl Pts',(17.0093152158794,14.3690454337186,5.88546379198059));
#133200=CARTESIAN_POINT('Ctrl Pts',(17.0103267200215,14.3631163736062,5.87540506553523));
#133201=CARTESIAN_POINT('Ctrl Pts',(17.0103279791075,14.3631089933137,5.87539254477437));
#133202=CARTESIAN_POINT('Ctrl Pts',(17.0103292381764,14.3631016133924,5.87538002377966));
#133203=CARTESIAN_POINT('Ctrl Pts',(17.0103304972283,14.3630942338424,5.87536750255111));
#133204=CARTESIAN_POINT('Ctrl Pts',(17.0129669905362,14.3476412299281,5.8491476661129));
#133205=CARTESIAN_POINT('Ctrl Pts',(17.0155288023521,14.333816461648,5.8218980821737));
#133206=CARTESIAN_POINT('Ctrl Pts',(17.018059794483,14.3217298456503,5.79384698268585));
#133207=CARTESIAN_POINT('Ctrl Pts',(17.0183643532261,14.320275441849,5.79047154445453));
#133208=CARTESIAN_POINT('Ctrl Pts',(17.0186684657083,14.3188462012054,5.7870845623239));
#133209=CARTESIAN_POINT('Ctrl Pts',(17.0189722083533,14.3174423095076,5.78368648438178));
#133210=CARTESIAN_POINT('Ctrl Pts',(17.0199941883175,14.3127187410174,5.77225322787141));
#133211=CARTESIAN_POINT('Ctrl Pts',(17.0210119584363,14.3082816751944,5.76069359196684));
#133212=CARTESIAN_POINT('Ctrl Pts',(17.0220282051085,14.3041366315448,5.74902320646588));
#133213=CARTESIAN_POINT('Origin',(13.2437274406976,15.,5.5));
#133214=CARTESIAN_POINT('',(17.5003341500486,14.3042076695831,5.74898600951276));
#133215=CARTESIAN_POINT('',(17.4213402632629,14.3044416670805,5.74885636750768));
#133216=CARTESIAN_POINT('',(13.2437274406976,14.3042076641721,5.74898599439144));
#133217=CARTESIAN_POINT('Ctrl Pts',(17.5003341513661,14.3042076696198,5.74898600961524));
#133218=CARTESIAN_POINT('Ctrl Pts',(17.4972553158012,14.3167672541012,5.78408381518432));
#133219=CARTESIAN_POINT('Ctrl Pts',(17.4942672188542,14.3319708724109,5.81819884060891));
#133220=CARTESIAN_POINT('Ctrl Pts',(17.4881127680215,14.3682787239195,5.88546027188228));
#133221=CARTESIAN_POINT('Ctrl Pts',(17.4849548566992,14.3895632982255,5.91835138223574));
#133222=CARTESIAN_POINT('Ctrl Pts',(17.4805719250421,14.4216642604325,5.96025617662959));
#133223=CARTESIAN_POINT('Ctrl Pts',(17.4794269773732,14.430278752553,5.97087750846475));
#133224=CARTESIAN_POINT('Ctrl Pts',(17.4775083910314,14.4450506291391,5.98809158652496));
#133225=CARTESIAN_POINT('Ctrl Pts',(17.4767414204593,14.4510431997034,5.99482180356909));
#133226=CARTESIAN_POINT('Ctrl Pts',(17.4751976334742,14.4632679565182,6.00805592303277));
#133227=CARTESIAN_POINT('Ctrl Pts',(17.4744209550709,14.4694989702461,6.01455879081484));
#133228=CARTESIAN_POINT('Ctrl Pts',(17.472454575248,14.4854656639902,6.03062378244077));
#133229=CARTESIAN_POINT('Ctrl Pts',(17.4712585933215,14.4953498166343,6.04003270274499));
#133230=CARTESIAN_POINT('Ctrl Pts',(17.4659219023786,14.5401729688918,6.08039526416728));
#133231=CARTESIAN_POINT('Ctrl Pts',(17.4616648018957,14.5777326604915,6.10826666023725));
#133232=CARTESIAN_POINT('Ctrl Pts',(17.4548342759243,14.6413256415667,6.14671353176405));
#133233=CARTESIAN_POINT('Ctrl Pts',(17.4522889052361,14.665775403901,6.15968155006906));
#133234=CARTESIAN_POINT('Ctrl Pts',(17.4487659629934,14.7010388234447,6.17592005403915));
#133235=CARTESIAN_POINT('Ctrl Pts',(17.4477589957908,14.7112873842711,6.18036075857157));
#133236=CARTESIAN_POINT('Ctrl Pts',(17.4459805103426,14.7297342480112,6.18786183205677));
#133237=CARTESIAN_POINT('Ctrl Pts',(17.4452054447519,14.7378936057274,6.19101210962597));
#133238=CARTESIAN_POINT('Ctrl Pts',(17.4439797511875,14.7510109136677,6.19581081915619));
#133239=CARTESIAN_POINT('Ctrl Pts',(17.4435242929751,14.7559334604094,6.19755271581981));
#133240=CARTESIAN_POINT('Ctrl Pts',(17.4426120944944,14.7658962211096,6.2009597631587));
#133241=CARTESIAN_POINT('Ctrl Pts',(17.44215546894,14.7709367198055,6.20262307677959));
#133242=CARTESIAN_POINT('Ctrl Pts',(17.4409175937611,14.7847349068951,6.20701206158565));
#133243=CARTESIAN_POINT('Ctrl Pts',(17.4401420942822,14.7935264853455,6.20962935900119));
#133244=CARTESIAN_POINT('Ctrl Pts',(17.4365288396037,14.835072150401,6.22116014710213));
#133245=CARTESIAN_POINT('Ctrl Pts',(17.4337809467226,14.8683703438025,6.22797486952268));
#133246=CARTESIAN_POINT('Ctrl Pts',(17.4281623663082,14.9374594804032,6.23721630585713));
#133247=CARTESIAN_POINT('Ctrl Pts',(17.4252996026559,14.9731913928919,6.23937834349708));
#133248=CARTESIAN_POINT('Ctrl Pts',(17.4210917831851,15.0247218210748,6.23875502303427));
#133249=CARTESIAN_POINT('Ctrl Pts',(17.4197935663145,15.0404940500274,6.23805848364246));
#133250=CARTESIAN_POINT('Ctrl Pts',(17.4173785191698,15.0694650856811,6.23584764944318));
#133251=CARTESIAN_POINT('Ctrl Pts',(17.4162661623708,15.0826686903264,6.23448145293848));
#133252=CARTESIAN_POINT('Ctrl Pts',(17.4143863539818,15.1046921126254,6.23160131619872));
#133253=CARTESIAN_POINT('Ctrl Pts',(17.4136249880668,15.1135344755246,6.23028133778899));
#133254=CARTESIAN_POINT('Ctrl Pts',(17.4121710105326,15.1302595083462,6.22747355882875));
#133255=CARTESIAN_POINT('Ctrl Pts',(17.4114794823583,15.1381462078188,6.22601717095219));
#133256=CARTESIAN_POINT('Ctrl Pts',(17.4096483898093,15.1588404287998,6.22184631112805));
#133257=CARTESIAN_POINT('Ctrl Pts',(17.4085023743042,15.1716016049001,6.2189194810426));
#133258=CARTESIAN_POINT('Ctrl Pts',(17.4026644463572,15.2355995079454,6.20244036307807));
#133259=CARTESIAN_POINT('Ctrl Pts',(17.3978146161543,15.2853414486772,6.18374533499249));
#133260=CARTESIAN_POINT('Ctrl Pts',(17.3899365297226,15.3618650182442,6.14517078710181));
#133261=CARTESIAN_POINT('Ctrl Pts',(17.3869332843097,15.3900757758338,6.12851646826257));
#133262=CARTESIAN_POINT('Ctrl Pts',(17.3831751251128,15.4247543845494,6.10480647307162));
#133263=CARTESIAN_POINT('Ctrl Pts',(17.3823512528713,15.4323179264026,6.09942338296729));
#133264=CARTESIAN_POINT('Ctrl Pts',(17.3810676167843,15.4440617714532,6.09072713565176));
#133265=CARTESIAN_POINT('Ctrl Pts',(17.3806022536796,15.448310767146,6.08750903591734));
#133266=CARTESIAN_POINT('Ctrl Pts',(17.3796890629601,15.4566368328577,6.08106011388874));
#133267=CARTESIAN_POINT('Ctrl Pts',(17.3792411373661,15.4607153085466,6.07783168987902));
#133268=CARTESIAN_POINT('Ctrl Pts',(17.3780560003865,15.4714818473284,6.0691226805321));
#133269=CARTESIAN_POINT('Ctrl Pts',(17.3773237329482,15.4781086852653,6.06356708854487));
#133270=CARTESIAN_POINT('Ctrl Pts',(17.3729155636115,15.5177434826501,6.02913686594567));
#133271=CARTESIAN_POINT('Ctrl Pts',(17.369399024819,15.5482296430383,5.99748324302881));
#133272=CARTESIAN_POINT('Ctrl Pts',(17.3623485650639,15.6031403928285,5.92924814340135));
#133273=CARTESIAN_POINT('Ctrl Pts',(17.3588270392535,15.6274693853144,5.89282789855888));
#133274=CARTESIAN_POINT('Ctrl Pts',(17.3541259872636,15.6545601417638,5.84327108936484));
#133275=CARTESIAN_POINT('Ctrl Pts',(17.3530546324049,15.6603927359816,5.83191175705035));
#133276=CARTESIAN_POINT('Ctrl Pts',(17.3512232269182,15.6697668239488,5.81242887405811));
#133277=CARTESIAN_POINT('Ctrl Pts',(17.350468550847,15.673461912783,5.80438205821612));
#133278=CARTESIAN_POINT('Ctrl Pts',(17.3490136729502,15.6802601245934,5.78884741519722));
#133279=CARTESIAN_POINT('Ctrl Pts',(17.3483143760169,15.6833864026305,5.7813710711164));
#133280=CARTESIAN_POINT('Ctrl Pts',(17.3464284689983,15.6914364023944,5.76119386100506));
#133281=CARTESIAN_POINT('Ctrl Pts',(17.3452346368047,15.6961326977508,5.74840641126145));
#133282=CARTESIAN_POINT('Ctrl Pts',(17.3405659245649,15.7129493797112,5.69838621438272));
#133283=CARTESIAN_POINT('Ctrl Pts',(17.3370134985905,15.7224550607806,5.66034846312654));
#133284=CARTESIAN_POINT('Ctrl Pts',(17.3303908306401,15.7343481749539,5.58914178676758));
#133285=CARTESIAN_POINT('Ctrl Pts',(17.3273399070407,15.7376000936515,5.5562112461603));
#133286=CARTESIAN_POINT('Ctrl Pts',(17.3232203449116,15.7390203373181,5.51094108151652));
#133287=CARTESIAN_POINT('Ctrl Pts',(17.3221141862803,15.7391002079377,5.49870072897666));
#133288=CARTESIAN_POINT('Ctrl Pts',(17.3201825555629,15.7387047717546,5.47711660377838));
#133289=CARTESIAN_POINT('Ctrl Pts',(17.3193526676311,15.7383561857298,5.46777334067163));
#133290=CARTESIAN_POINT('Ctrl Pts',(17.3180618964234,15.7375298708302,5.45310396790918));
#133291=CARTESIAN_POINT('Ctrl Pts',(17.3175953162649,15.737171516468,5.44777252543667));
#133292=CARTESIAN_POINT('Ctrl Pts',(17.3166818254238,15.736351115501,5.43727062804039));
#133293=CARTESIAN_POINT('Ctrl Pts',(17.3162347928536,15.7358923645335,5.43210028471894));
#133294=CARTESIAN_POINT('Ctrl Pts',(17.3150552043292,15.7345297889885,5.41838633548142));
#133295=CARTESIAN_POINT('Ctrl Pts',(17.3143275088876,15.7335313612004,5.40985254694462));
#133296=CARTESIAN_POINT('Ctrl Pts',(17.3098755623672,15.726453933101,5.3573158777159));
#133297=CARTESIAN_POINT('Ctrl Pts',(17.3063154763725,15.7165656769522,5.31391150405181));
#133298=CARTESIAN_POINT('Ctrl Pts',(17.299258459848,15.6894777051499,5.23053668676709));
#133299=CARTESIAN_POINT('Ctrl Pts',(17.2957747123472,15.6725389913239,5.19067721357551));
#133300=CARTESIAN_POINT('Ctrl Pts',(17.2911133554634,15.6462068937121,5.14125083197125));
#133301=CARTESIAN_POINT('Ctrl Pts',(17.2900410608193,15.6399069496065,5.13013060275953));
#133302=CARTESIAN_POINT('Ctrl Pts',(17.2882085393285,15.6287583889146,5.11159000477155));
#133303=CARTESIAN_POINT('Ctrl Pts',(17.2874537028228,15.6240586683491,5.10408308952639));
#133304=CARTESIAN_POINT('Ctrl Pts',(17.2859988391251,15.6148036617242,5.08987429640336));
#133305=CARTESIAN_POINT('Ctrl Pts',(17.2852997210036,15.6102707973551,5.08315928976659));
#133306=CARTESIAN_POINT('Ctrl Pts',(17.2834151216731,15.5978305048511,5.06536811794136));
#133307=CARTESIAN_POINT('Ctrl Pts',(17.2822224374505,15.5897263981578,5.05443417170294));
#133308=CARTESIAN_POINT('Ctrl Pts',(17.2776065800594,15.5575123116031,5.01339068248128));
#133309=CARTESIAN_POINT('Ctrl Pts',(17.2741085145448,15.5313642809265,4.98496633100814));
#133310=CARTESIAN_POINT('Ctrl Pts',(17.2674998463669,15.4785847887242,4.93590789039152));
#133311=CARTESIAN_POINT('Ctrl Pts',(17.2644070207186,15.4525240480725,4.91479457515334));
#133312=CARTESIAN_POINT('Ctrl Pts',(17.2602387033681,15.4150438298827,4.88843530709106));
#133313=CARTESIAN_POINT('Ctrl Pts',(17.2591250392081,15.4047910983087,4.88160129293183));
#133314=CARTESIAN_POINT('Ctrl Pts',(17.2571819021886,15.3864279797015,4.87001377413554));
#133315=CARTESIAN_POINT('Ctrl Pts',(17.2563479449911,15.3783888842978,4.86515269097576));
#133316=CARTESIAN_POINT('Ctrl Pts',(17.2550523438402,15.3656268249375,4.85776431882953));
#133317=CARTESIAN_POINT('Ctrl Pts',(17.2545849367553,15.3609656982122,4.85513302486518));
#133318=CARTESIAN_POINT('Ctrl Pts',(17.2536712250853,15.3517351974141,4.85005368275396));
#133319=CARTESIAN_POINT('Ctrl Pts',(17.253224782554,15.347167900265,4.84760263840116));
#133320=CARTESIAN_POINT('Ctrl Pts',(17.2520488565903,15.3349955242147,4.84123435738164));
#133321=CARTESIAN_POINT('Ctrl Pts',(17.2513241789541,15.3273472363192,4.83740058874753));
#133322=CARTESIAN_POINT('Ctrl Pts',(17.2468453907719,15.279269591135,4.81433704999345));
#133323=CARTESIAN_POINT('Ctrl Pts',(17.2432584704832,15.2372230829113,4.79867864571787));
#133324=CARTESIAN_POINT('Ctrl Pts',(17.236229241115,15.1529678813465,4.77575478051669));
#133325=CARTESIAN_POINT('Ctrl Pts',(17.2328008102522,15.1110415590772,4.76815342371463));
#133326=CARTESIAN_POINT('Ctrl Pts',(17.2281841570181,15.0557860959489,4.76299452374808));
#133327=CARTESIAN_POINT('Ctrl Pts',(17.227096570197,15.0428459306969,4.76212918119837));
#133328=CARTESIAN_POINT('Ctrl Pts',(17.2252460531384,15.0210099546185,4.76124525410686));
#133329=CARTESIAN_POINT('Ctrl Pts',(17.2244887760184,15.0121241056453,4.76104602023288));
#133330=CARTESIAN_POINT('Ctrl Pts',(17.2230345123442,14.9951692815685,4.76097174808373));
#133331=CARTESIAN_POINT('Ctrl Pts',(17.2223385031601,14.987101661909,4.76106853187728));
#133332=CARTESIAN_POINT('Ctrl Pts',(17.2204756393179,14.9656444599169,4.76167743018121));
#133333=CARTESIAN_POINT('Ctrl Pts',(17.2193018897837,14.9522651578383,4.76242162853785));
#133334=CARTESIAN_POINT('Ctrl Pts',(17.2136806686628,14.8889058233142,4.7676768842616));
#133335=CARTESIAN_POINT('Ctrl Pts',(17.2090948613312,14.8394589897758,4.77690679133383));
#133336=CARTESIAN_POINT('Ctrl Pts',(17.2021276124978,14.7667594346147,4.79830469824513));
#133337=CARTESIAN_POINT('Ctrl Pts',(17.1997724484413,14.7425721087787,4.80681281243023));
#133338=CARTESIAN_POINT('Ctrl Pts',(17.1960619496991,14.7047160181459,4.82238451130966));
#133339=CARTESIAN_POINT('Ctrl Pts',(17.1946867633643,14.6907405367587,4.82864759232853));
#133340=CARTESIAN_POINT('Ctrl Pts',(17.1927685570382,14.6712357464062,4.83812713269096));
#133341=CARTESIAN_POINT('Ctrl Pts',(17.192208449292,14.6655389844987,4.84098750773224));
#133342=CARTESIAN_POINT('Ctrl Pts',(17.1912259241255,14.6555345742557,4.84617393443511));
#133343=CARTESIAN_POINT('Ctrl Pts',(17.1908018582693,14.6512120472506,4.84846955413507));
#133344=CARTESIAN_POINT('Ctrl Pts',(17.1898327539284,14.6413249768413,4.85384701553971));
#133345=CARTESIAN_POINT('Ctrl Pts',(17.1892894797715,14.6357769078452,4.85695801104753));
#133346=CARTESIAN_POINT('Ctrl Pts',(17.1877683150316,14.6202480380471,4.86593107106127));
#133347=CARTESIAN_POINT('Ctrl Pts',(17.1867993688603,14.6103633000766,4.87195681379342));
#133348=CARTESIAN_POINT('Ctrl Pts',(17.181860133925,14.5602415742904,4.90415020883126));
#133349=CARTESIAN_POINT('Ctrl Pts',(17.1780445005885,14.5224781849726,4.93396257138102));
#133350=CARTESIAN_POINT('Ctrl Pts',(17.1719584401556,14.4681245241494,4.98621053043894));
#133351=CARTESIAN_POINT('Ctrl Pts',(17.1697343947959,14.4494512517061,5.00627235077205));
#133352=CARTESIAN_POINT('Ctrl Pts',(17.1661944107989,14.4220653978625,5.03918471847699));
#133353=CARTESIAN_POINT('Ctrl Pts',(17.1649069705786,14.4125699151752,5.05135207933829));
#133354=CARTESIAN_POINT('Ctrl Pts',(17.1628175416868,14.3979544137257,5.07134022138535));
#133355=CARTESIAN_POINT('Ctrl Pts',(17.1620249741564,14.3925894540662,5.07897683467634));
#133356=CARTESIAN_POINT('Ctrl Pts',(17.1604757732621,14.3824586072107,5.093994116164));
#133357=CARTESIAN_POINT('Ctrl Pts',(17.1597198920099,14.3776768745417,5.10136224143373));
#133358=CARTESIAN_POINT('Ctrl Pts',(17.1578917417277,14.3665047766077,5.11926826499025));
#133359=CARTESIAN_POINT('Ctrl Pts',(17.1568150229615,14.3602447117821,5.12988382448421));
#133360=CARTESIAN_POINT('Ctrl Pts',(17.1505592434479,14.3257297973587,5.19190665856902));
#133361=CARTESIAN_POINT('Ctrl Pts',(17.1451777429052,14.303416073196,5.24636693159946));
#133362=CARTESIAN_POINT('Ctrl Pts',(17.1370839950809,14.2799168439172,5.33127148617539));
#133363=CARTESIAN_POINT('Ctrl Pts',(17.134387508867,14.273762103389,5.36011453335841));
#133364=CARTESIAN_POINT('Ctrl Pts',(17.1309577831167,14.268010081453,5.39806279212652));
#133365=CARTESIAN_POINT('Ctrl Pts',(17.1301674933819,14.2668338306156,5.40689884409029));
#133366=CARTESIAN_POINT('Ctrl Pts',(17.1289237390216,14.2652186113887,5.4209751681117));
#133367=CARTESIAN_POINT('Ctrl Pts',(17.1284652089325,14.2646752364168,5.42620223133049));
#133368=CARTESIAN_POINT('Ctrl Pts',(17.1276093151926,14.2637588866787,5.43603611896898));
#133369=CARTESIAN_POINT('Ctrl Pts',(17.1272112647142,14.2633732820652,5.44064145291514));
#133370=CARTESIAN_POINT('Ctrl Pts',(17.1261081807337,14.2624191916769,5.45348417390834));
#133371=CARTESIAN_POINT('Ctrl Pts',(17.1254080284913,14.2619454875646,5.46172826718913));
#133372=CARTESIAN_POINT('Ctrl Pts',(17.120727278434,14.2596842394592,5.51734562730788));
#133373=CARTESIAN_POINT('Ctrl Pts',(17.1169379661085,14.2623203270669,5.56479544511568));
#133374=CARTESIAN_POINT('Ctrl Pts',(17.1099792581425,14.2753797401333,5.65022502463752));
#133375=CARTESIAN_POINT('Ctrl Pts',(17.1068305705428,14.2843152073538,5.68824668079661));
#133376=CARTESIAN_POINT('Ctrl Pts',(17.102902867527,14.2987417464203,5.73329572408496));
#133377=CARTESIAN_POINT('Ctrl Pts',(17.1022094454944,14.3014087825667,5.74116450882544));
#133378=CARTESIAN_POINT('Ctrl Pts',(17.1015120386236,14.3042076645209,5.7489859953664));
#133379=CARTESIAN_POINT('',(17.0432316689992,14.2612664936,5.49980856841249));
#133380=CARTESIAN_POINT('Ctrl Pts',(17.0220737370494,14.3042126623665,5.74899996142335));
#133381=CARTESIAN_POINT('Ctrl Pts',(17.0254895451321,14.2899493039172,5.70914347251323));
#133382=CARTESIAN_POINT('Ctrl Pts',(17.0288728794103,14.2791376675812,5.66813750052812));
#133383=CARTESIAN_POINT('Ctrl Pts',(17.0339152333952,14.2686243049792,5.60759292999941));
#133384=CARTESIAN_POINT('Ctrl Pts',(17.0354997623189,14.2660855606134,5.58863477947617));
#133385=CARTESIAN_POINT('Ctrl Pts',(17.0379545737325,14.2633339362743,5.55954880952728));
#133386=CARTESIAN_POINT('Ctrl Pts',(17.0388087427715,14.2625891360241,5.54947875477171));
#133387=CARTESIAN_POINT('Ctrl Pts',(17.0402426101667,14.2616922806603,5.53267971049496));
#133388=CARTESIAN_POINT('Ctrl Pts',(17.0408187074412,14.2614254076138,5.52595798472993));
#133389=CARTESIAN_POINT('Ctrl Pts',(17.0419554109074,14.2610816714149,5.5127554362252));
#133390=CARTESIAN_POINT('Ctrl Pts',(17.0425157620651,14.2609982333761,5.50627538393103));
#133391=CARTESIAN_POINT('Ctrl Pts',(17.0430787344308,14.2610000283511,5.49979529801652));
#133392=CARTESIAN_POINT('Ctrl Pts',(17.0432403769393,14.2612816658625,5.49980932401545));
#133393=CARTESIAN_POINT('Ctrl Pts',(17.046308805676,14.2612728636063,5.46438385344786));
#133394=CARTESIAN_POINT('Ctrl Pts',(17.0494339926232,14.263783384481,5.42902470624598));
#133395=CARTESIAN_POINT('Ctrl Pts',(17.052595132431,14.2687728192454,5.39408059525951));
#133396=CARTESIAN_POINT('Ctrl Pts',(17.0557641770926,14.27377473076,5.35904910184047));
#133397=CARTESIAN_POINT('Ctrl Pts',(17.0589691313495,14.281268181868,5.32443430767273));
#133398=CARTESIAN_POINT('Ctrl Pts',(17.0621585736971,14.2911823715331,5.29058356494859));
#133399=CARTESIAN_POINT('Ctrl Pts',(17.065079447934,14.3002617333829,5.25958323587894));
#133400=CARTESIAN_POINT('Ctrl Pts',(17.0679867788057,14.3113720892566,5.22922255134883));
#133401=CARTESIAN_POINT('Ctrl Pts',(17.0708225258615,14.3244300074377,5.19977228326336));
#133402=CARTESIAN_POINT('Ctrl Pts',(17.071094799487,14.3256837605594,5.19694462229645));
#133403=CARTESIAN_POINT('Ctrl Pts',(17.0713664131928,14.3269554708206,5.19412531468191));
#133404=CARTESIAN_POINT('Ctrl Pts',(17.0716373156049,14.3282450672071,5.19131457491902));
#133405=CARTESIAN_POINT('Ctrl Pts',(17.0721823852581,14.3308398017824,5.18565922125862));
#133406=CARTESIAN_POINT('Ctrl Pts',(17.0727245311859,14.3335068116493,5.18003875659509));
#133407=CARTESIAN_POINT('Ctrl Pts',(17.0732632874351,14.3362453362973,5.17445512840284));
#133408=CARTESIAN_POINT('Ctrl Pts',(17.0732645465214,14.3362517362952,5.17444207932964));
#133409=CARTESIAN_POINT('Ctrl Pts',(17.0732658055909,14.3362581366937,5.17442903043528));
#133410=CARTESIAN_POINT('Ctrl Pts',(17.0732670646434,14.3362645374928,5.1744159817198));
#133411=CARTESIAN_POINT('Ctrl Pts',(17.0758558186791,14.3494253021247,5.14758635162535));
#133412=CARTESIAN_POINT('Ctrl Pts',(17.0783733027148,14.364283662599,5.12151099280864));
#133413=CARTESIAN_POINT('Ctrl Pts',(17.0808604798743,14.3807146444064,5.09640568306478));
#133414=CARTESIAN_POINT('Ctrl Pts',(17.0811171368961,14.382410191843,5.09381501355526));
#133415=CARTESIAN_POINT('Ctrl Pts',(17.0813734711919,14.3841224438466,5.09123469264477));
#133416=CARTESIAN_POINT('Ctrl Pts',(17.0816295277741,14.3858512340337,5.08866496954552));
#133417=CARTESIAN_POINT('Ctrl Pts',(17.0843638090811,14.4043119924029,5.06122437116249));
#133418=CARTESIAN_POINT('Ctrl Pts',(17.0870672604627,14.4246635102563,5.03498955318868));
#133419=CARTESIAN_POINT('Ctrl Pts',(17.0897868570603,14.4466989954632,5.01021248193811));
#133420=CARTESIAN_POINT('Ctrl Pts',(17.0925036504131,14.4687117674274,4.98546094984072));
#133421=CARTESIAN_POINT('Ctrl Pts',(17.0952370362601,14.4924045217501,4.96216391911936));
#133422=CARTESIAN_POINT('Ctrl Pts',(17.0980162294418,14.517545283025,4.94053749879048));
#133423=CARTESIAN_POINT('Ctrl Pts',(17.1007940979461,14.5426740611825,4.91892138650011));
#133424=CARTESIAN_POINT('Ctrl Pts',(17.1036179549144,14.569249201768,4.89897411650705));
#133425=CARTESIAN_POINT('Ctrl Pts',(17.1064941737705,14.597018984189,4.88087962592021));
#133426=CARTESIAN_POINT('Ctrl Pts',(17.1093727444936,14.6248114737966,4.86277033957565));
#133427=CARTESIAN_POINT('Ctrl Pts',(17.1123038044352,14.6538004830513,4.84651679968675));
#133428=CARTESIAN_POINT('Ctrl Pts',(17.1152689227827,14.6837160968295,4.83227329132449));
#133429=CARTESIAN_POINT('Ctrl Pts',(17.1182354603923,14.7136460297993,4.81802296526741));
#133430=CARTESIAN_POINT('Ctrl Pts',(17.1212359261201,14.7445035682296,4.80578469411534));
#133431=CARTESIAN_POINT('Ctrl Pts',(17.1242278802789,14.7760005656261,4.79568270736877));
#133432=CARTESIAN_POINT('Ctrl Pts',(17.1272256364889,14.8075586425646,4.78556113066843));
#133433=CARTESIAN_POINT('Ctrl Pts',(17.1302143755419,14.8397589414177,4.77758456517678));
#133434=CARTESIAN_POINT('Ctrl Pts',(17.1331319537673,14.8722906572434,4.77184378085331));
#133435=CARTESIAN_POINT('Ctrl Pts',(17.1341646798948,14.8838058079304,4.76981173320786));
#133436=CARTESIAN_POINT('Ctrl Pts',(17.135188350111,14.8953622699967,4.76805946559736));
#133437=CARTESIAN_POINT('Ctrl Pts',(17.1361998550209,14.9069455296076,4.76658975811008));
#133438=CARTESIAN_POINT('Ctrl Pts',(17.1362011141082,14.9069599480604,4.76658792866753));
#133439=CARTESIAN_POINT('Ctrl Pts',(17.1362023731787,14.906974366584,4.76658609965795));
#133440=CARTESIAN_POINT('Ctrl Pts',(17.1362036322324,14.9069887851785,4.76658427108136));
#133441=CARTESIAN_POINT('Ctrl Pts',(17.1387923860856,14.9366350139168,4.76282451490147));
#133442=CARTESIAN_POINT('Ctrl Pts',(17.1413098699205,14.9665846622022,4.7608974322932));
#133443=CARTESIAN_POINT('Ctrl Pts',(17.143797046848,14.996588781652,4.76081728363642));
#133444=CARTESIAN_POINT('Ctrl Pts',(17.1440537041177,14.9996849728769,4.76080901291985));
#133445=CARTESIAN_POINT('Ctrl Pts',(17.1443100386603,15.0027817054289,4.7608203851297));
#133446=CARTESIAN_POINT('Ctrl Pts',(17.1445660954884,15.005878679663,4.760851398323));
#133447=CARTESIAN_POINT('Ctrl Pts',(17.1473003767961,15.038949458605,4.76118257009975));
#133448=CARTESIAN_POINT('Ctrl Pts',(17.1500038281384,15.0720527417223,4.76375602239136));
#133449=CARTESIAN_POINT('Ctrl Pts',(17.152723424668,15.1048643658765,4.76853757504343));
#133450=CARTESIAN_POINT('Ctrl Pts',(17.1554402179507,15.1376421691747,4.77331419907012));
#133451=CARTESIAN_POINT('Ctrl Pts',(17.1581736036993,15.1701288330478,4.78029381047501));
#133452=CARTESIAN_POINT('Ctrl Pts',(17.1609527967733,15.2020162973659,4.78940147819089));
#133453=CARTESIAN_POINT('Ctrl Pts',(17.1637306651674,15.2338885627823,4.7985048048107));
#133454=CARTESIAN_POINT('Ctrl Pts',(17.1665545220162,15.2651622012134,4.80973384193559));
#133455=CARTESIAN_POINT('Ctrl Pts',(17.1694307407666,15.2955451674421,4.8229794762384));
#133456=CARTESIAN_POINT('Ctrl Pts',(17.1723093113792,15.3259529775915,4.83623594139577));
#133457=CARTESIAN_POINT('Ctrl Pts',(17.1752403712242,15.3554686698087,4.85151220363314));
#133458=CARTESIAN_POINT('Ctrl Pts',(17.1782054895142,15.3838149616789,4.8686676481297));
#133459=CARTESIAN_POINT('Ctrl Pts',(17.1811720270636,15.4121748215541,4.88583130411152));
#133460=CARTESIAN_POINT('Ctrl Pts',(17.1841724927706,15.4393641414083,4.904876090957));
#133461=CARTESIAN_POINT('Ctrl Pts',(17.1871644469736,15.4651207184266,4.92562963969941));
#133462=CARTESIAN_POINT('Ctrl Pts',(17.1901622032226,15.4909272430153,4.94642343405885));
#133463=CARTESIAN_POINT('Ctrl Pts',(17.1931509423804,15.5152952548463,4.96893309656858));
#133464=CARTESIAN_POINT('Ctrl Pts',(17.196068520799,15.5379780396529,4.9929489346695));
#133465=CARTESIAN_POINT('Ctrl Pts',(17.1971012463288,15.5460069895539,5.00144974101178));
#133466=CARTESIAN_POINT('Ctrl Pts',(17.19812491597,15.5538249659581,5.01013889140464));
#133467=CARTESIAN_POINT('Ctrl Pts',(17.1991364203344,15.5614216662791,5.01900579169129));
#133468=CARTESIAN_POINT('Ctrl Pts',(17.1991376794173,15.5614311223686,5.01901682887835));
#133469=CARTESIAN_POINT('Ctrl Pts',(17.1991389384834,15.5614405781354,5.01902786636269));
#133470=CARTESIAN_POINT('Ctrl Pts',(17.1991401975326,15.5614500335796,5.01903890414432));
#133471=CARTESIAN_POINT('Ctrl Pts',(17.2017289524822,15.5808915513842,5.04173389603124));
#133472=CARTESIAN_POINT('Ctrl Pts',(17.2042464374443,15.5989691462508,5.0656900281609));
#133473=CARTESIAN_POINT('Ctrl Pts',(17.2067336155454,15.6155340213903,5.09070720489167));
#133474=CARTESIAN_POINT('Ctrl Pts',(17.2069902725584,15.617243384854,5.09328877870422));
#133475=CARTESIAN_POINT('Ctrl Pts',(17.2072466068458,15.6189366390559,5.09588160540596));
#133476=CARTESIAN_POINT('Ctrl Pts',(17.2075026634199,15.6206136208584,5.09848543364811));
#133477=CARTESIAN_POINT('Ctrl Pts',(17.2102369456637,15.638521153918,5.12629023168492));
#133478=CARTESIAN_POINT('Ctrl Pts',(17.2129403980013,15.6545736717429,5.15535510938026));
#133479=CARTESIAN_POINT('Ctrl Pts',(17.2156599955616,15.6686214807986,5.18539051200979));
#133480=CARTESIAN_POINT('Ctrl Pts',(17.2183767898766,15.6826548099718,5.21539495542685));
#133481=CARTESIAN_POINT('Ctrl Pts',(17.2211101766924,15.6946879867136,5.24636754632892));
#133482=CARTESIAN_POINT('Ctrl Pts',(17.2238893708266,15.7046142094085,5.27800977309107));
#133483=CARTESIAN_POINT('Ctrl Pts',(17.2266672402813,15.7145357008532,5.30963691785302));
#133484=CARTESIAN_POINT('Ctrl Pts',(17.2294910981837,15.7223525124384,5.34193288686681));
#133485=CARTESIAN_POINT('Ctrl Pts',(17.2323673179249,15.7279951994938,5.37459374982264));
#133486=CARTESIAN_POINT('Ctrl Pts',(17.2352458895242,15.7336425005215,5.40728131926023));
#133487=CARTESIAN_POINT('Ctrl Pts',(17.2381769502925,15.7371122093331,5.44033433456266));
#133488=CARTESIAN_POINT('Ctrl Pts',(17.2411420693788,15.7383693105905,5.47344387492055));
#133489=CARTESIAN_POINT('Ctrl Pts',(17.2441086077226,15.7396270135607,5.50656926319572));
#133490=CARTESIAN_POINT('Ctrl Pts',(17.2471090740959,15.7386698547313,5.53975129605358));
#133491=CARTESIAN_POINT('Ctrl Pts',(17.2501010287738,15.7354976333302,5.57267618785584));
#133492=CARTESIAN_POINT('Ctrl Pts',(17.2530987854865,15.7323192603188,5.6056649280081));
#133493=CARTESIAN_POINT('Ctrl Pts',(17.2560875249143,15.726916716557,5.63839561513311));
#133494=CARTESIAN_POINT('Ctrl Pts',(17.2590051033636,15.7193294926593,5.6705468779432));
#133495=CARTESIAN_POINT('Ctrl Pts',(17.2600378244874,15.7166438797354,5.6819273048409));
#133496=CARTESIAN_POINT('Ctrl Pts',(17.2610614897705,15.7136849478903,5.69323507658317));
#133497=CARTESIAN_POINT('Ctrl Pts',(17.2620729898636,15.7104558810248,5.70445576275555));
#133498=CARTESIAN_POINT('Ctrl Pts',(17.262074248952,15.7104518615684,5.70446972996684));
#133499=CARTESIAN_POINT('Ctrl Pts',(17.2620755080235,15.7104478416862,5.7044836970721));
#133500=CARTESIAN_POINT('Ctrl Pts',(17.2620767670781,15.7104438213783,5.70449766407129));
#133501=CARTESIAN_POINT('Ctrl Pts',(17.2646655203705,15.7021776311295,5.73321533333194));
#133502=CARTESIAN_POINT('Ctrl Pts',(17.267183003679,15.6921081022342,5.76148721799749));
#133503=CARTESIAN_POINT('Ctrl Pts',(17.2696701801455,15.6803205496886,5.78907901055691));
#133504=CARTESIAN_POINT('Ctrl Pts',(17.269926836768,15.6791041689991,5.79192626180144));
#133505=CARTESIAN_POINT('Ctrl Pts',(17.2701831706658,15.6778695315053,5.79476624510982));
#133506=CARTESIAN_POINT('Ctrl Pts',(17.2704392268509,15.6766167574458,5.79759868601503));
#133507=CARTESIAN_POINT('Ctrl Pts',(17.2731735070861,15.6632390866486,5.82784473213549));
#133508=CARTESIAN_POINT('Ctrl Pts',(17.2758769574401,15.6477889337777,5.85723422131644));
#133509=CARTESIAN_POINT('Ctrl Pts',(17.2785965530498,15.6304258422559,5.88548290756499));
#133510=CARTESIAN_POINT('Ctrl Pts',(17.2813133454188,15.613080647852,5.91370247629913));
#133511=CARTESIAN_POINT('Ctrl Pts',(17.2840467303213,15.5938270059046,5.94078374056712));
#133512=CARTESIAN_POINT('Ctrl Pts',(17.2868259225927,15.5728555255426,5.96647335525849));
#133513=CARTESIAN_POINT('Ctrl Pts',(17.289603790193,15.5518940410031,5.99215072528127));
#133514=CARTESIAN_POINT('Ctrl Pts',(17.2924276462916,15.5292166464172,6.01643789898743));
#133515=CARTESIAN_POINT('Ctrl Pts',(17.2953038643106,15.5050390178502,6.03910975453352));
#133516=CARTESIAN_POINT('Ctrl Pts',(17.2981824342153,15.4808416192177,6.06180014887329));
#133517=CARTESIAN_POINT('Ctrl Pts',(17.3011134933721,15.4551416188525,6.08287263208124));
#133518=CARTESIAN_POINT('Ctrl Pts',(17.3040786109701,15.4281777923325,6.10212809571443));
#133519=CARTESIAN_POINT('Ctrl Pts',(17.3070451478403,15.4012010594086,6.12139277609551));
#133520=CARTESIAN_POINT('Ctrl Pts',(17.3100456128648,15.3729591609748,6.13883861972739));
#133521=CARTESIAN_POINT('Ctrl Pts',(17.3130375663572,15.3437140789445,6.15429292244444));
#133522=CARTESIAN_POINT('Ctrl Pts',(17.3160353219279,15.314412284048,6.16977719456968));
#133523=CARTESIAN_POINT('Ctrl Pts',(17.3190240603795,15.2841030590818,6.18326181658168));
#133524=CARTESIAN_POINT('Ctrl Pts',(17.3219416380291,15.2530765464079,6.19460306592388));
#133525=CARTESIAN_POINT('Ctrl Pts',(17.3229743708641,15.2420941143211,6.19861751969088));
#133526=CARTESIAN_POINT('Ctrl Pts',(17.3239980476698,15.2310220802754,6.20236372539087));
#133527=CARTESIAN_POINT('Ctrl Pts',(17.325009558987,15.2198742485695,6.2058364075973));
#133528=CARTESIAN_POINT('Ctrl Pts',(17.3250108180805,15.219860372143,6.20584073026926));
#133529=CARTESIAN_POINT('Ctrl Pts',(17.3250120771571,15.219846495571,6.20584505252731));
#133530=CARTESIAN_POINT('Ctrl Pts',(17.3250133362169,15.2198326188534,6.20584937437144));
#133531=CARTESIAN_POINT('Ctrl Pts',(17.3276020888975,15.1913007013954,6.21473551761589));
#133532=CARTESIAN_POINT('Ctrl Pts',(17.3301195714695,15.1621495551006,6.22187028834272));
#133533=CARTESIAN_POINT('Ctrl Pts',(17.3326067469824,15.132621798228,6.22719611158677));
#133534=CARTESIAN_POINT('Ctrl Pts',(17.3328634054165,15.1295747483517,6.22774569783293));
#133535=CARTESIAN_POINT('Ctrl Pts',(17.3331197411185,15.126523730433,6.22827603831381));
#133536=CARTESIAN_POINT('Ctrl Pts',(17.3333757991017,15.1234690398434,6.22878708254196));
#133537=CARTESIAN_POINT('Ctrl Pts',(17.3361100800865,15.0908499342459,6.23424420009751));
#133538=CARTESIAN_POINT('Ctrl Pts',(17.3388135309118,15.0578067108807,6.23749927227484));
#133539=CARTESIAN_POINT('Ctrl Pts',(17.341533126788,15.0246645151019,6.23852926515128));
#133540=CARTESIAN_POINT('Ctrl Pts',(17.3442499194075,14.9915564810471,6.23955819634996));
#133541=CARTESIAN_POINT('Ctrl Pts',(17.3469833043578,14.9583498571705,6.23836717331611));
#133542=CARTESIAN_POINT('Ctrl Pts',(17.3497624965953,14.9253610601702,6.23497610112255));
#133543=CARTESIAN_POINT('Ctrl Pts',(17.352540364142,14.8923879871464,6.23158664526983));
#133544=CARTESIAN_POINT('Ctrl Pts',(17.3553642201057,14.8596325874684,6.22599955006262));
#133545=CARTESIAN_POINT('Ctrl Pts',(17.3582404380528,14.8274014872314,6.21827117671232));
#133546=CARTESIAN_POINT('Ctrl Pts',(17.3611190078425,14.7951440320821,6.21053648398104));
#133547=CARTESIAN_POINT('Ctrl Pts',(17.3640500669466,14.7634117402433,6.20065710972179));
#133548=CARTESIAN_POINT('Ctrl Pts',(17.3670151847103,14.732502211224,6.18872301285149));
#133549=CARTESIAN_POINT('Ctrl Pts',(17.3699817217219,14.7015778874172,6.17678320374838));
#133550=CARTESIAN_POINT('Ctrl Pts',(17.3729821871067,14.6714771077787,6.16278655417432));
#133551=CARTESIAN_POINT('Ctrl Pts',(17.3759741413366,14.6424881774962,6.14685692489324));
#133552=CARTESIAN_POINT('Ctrl Pts',(17.3789718975937,14.6134430315937,6.13089640471772));
#133553=CARTESIAN_POINT('Ctrl Pts',(17.3819606371119,14.5855141733538,6.11299489910472));
#133554=CARTESIAN_POINT('Ctrl Pts',(17.3848782163587,14.5589811849392,6.09331572577658));
#133555=CARTESIAN_POINT('Ctrl Pts',(17.3859109408273,14.5495894035875,6.08634996337569));
#133556=CARTESIAN_POINT('Ctrl Pts',(17.3869346094895,14.5403724080828,6.07916186612232));
#133557=CARTESIAN_POINT('Ctrl Pts',(17.3879461129728,14.5313421948412,6.07176006324632));
#133558=CARTESIAN_POINT('Ctrl Pts',(17.3879473720345,14.5313309545482,6.07175084990541));
#133559=CARTESIAN_POINT('Ctrl Pts',(17.3879486310795,14.5313197145191,6.07174163621408));
#133560=CARTESIAN_POINT('Ctrl Pts',(17.3879498901077,14.531308474754,6.0717324221723));
#133561=CARTESIAN_POINT('Ctrl Pts',(17.3905172407073,14.5083888796025,6.05294358580232));
#133562=CARTESIAN_POINT('Ctrl Pts',(17.3930150706138,14.4865659871349,6.03269332893148));
#133563=CARTESIAN_POINT('Ctrl Pts',(17.3954830725674,14.466021281195,6.01114853856156));
#133564=CARTESIAN_POINT('Ctrl Pts',(17.3957679506134,14.4636498342539,6.00866165326039));
#133565=CARTESIAN_POINT('Ctrl Pts',(17.3960524312387,14.4612954273727,6.00615757615927));
#133566=CARTESIAN_POINT('Ctrl Pts',(17.3963365754886,14.4589583459032,6.00363660801193));
#133567=CARTESIAN_POINT('Ctrl Pts',(17.3990370942771,14.4367466262545,5.97967722171588));
#133568=CARTESIAN_POINT('Ctrl Pts',(17.4017080289432,14.4160984659131,5.95418669569636));
#133569=CARTESIAN_POINT('Ctrl Pts',(17.4043944413958,14.3972091715163,5.92741709576108));
#133570=CARTESIAN_POINT('Ctrl Pts',(17.4071502058762,14.3778322338807,5.89995641578101));
#133571=CARTESIAN_POINT('Ctrl Pts',(17.4099228436392,14.3603060093141,5.87115019365405));
#133572=CARTESIAN_POINT('Ctrl Pts',(17.4127425977568,14.3447974178845,5.84129019182417));
#133573=CARTESIAN_POINT('Ctrl Pts',(17.4155623518744,14.329288826455,5.81143018999427));
#133574=CARTESIAN_POINT('Ctrl Pts',(17.4184294660874,14.3157976460623,5.78051669501691));
#133575=CARTESIAN_POINT('Ctrl Pts',(17.4213499029956,14.304450533742,5.74885545845108));
#133576=CARTESIAN_POINT('Origin',(13.2437274406976,15.,5.5));
#133577=CARTESIAN_POINT('',(17.9010383741602,14.3042076641721,5.74898599439144));
#133578=CARTESIAN_POINT('',(17.8222024383386,14.3040135853341,5.74909189204507));
#133579=CARTESIAN_POINT('',(13.2437274406976,14.3042076641721,5.74898599439144));
#133580=CARTESIAN_POINT('Ctrl Pts',(17.9010383741602,14.3042076641721,5.74898599439144));
#133581=CARTESIAN_POINT('Ctrl Pts',(17.9000384603042,14.3078805994981,5.75925002653544));
#133582=CARTESIAN_POINT('Ctrl Pts',(17.8990357742742,14.3117816194058,5.76943549672321));
#133583=CARTESIAN_POINT('Ctrl Pts',(17.894600037722,14.3300218189885,5.81407382881705));
#133584=CARTESIAN_POINT('Ctrl Pts',(17.8911650746411,14.3467321536784,5.84749794462777));
#133585=CARTESIAN_POINT('Ctrl Pts',(17.8870512634926,14.3703816273505,5.88701155111811));
#133586=CARTESIAN_POINT('Ctrl Pts',(17.8862772581325,14.3749984053375,5.89442396414004));
#133587=CARTESIAN_POINT('Ctrl Pts',(17.88505488578,14.3825700483691,5.90611358429325));
#133588=CARTESIAN_POINT('Ctrl Pts',(17.8846016477165,14.3854403739368,5.91044422397341));
#133589=CARTESIAN_POINT('Ctrl Pts',(17.8836930093189,14.3913257897608,5.91912373034288));
#133590=CARTESIAN_POINT('Ctrl Pts',(17.8832377222116,14.3943423619815,5.9234711637284));
#133591=CARTESIAN_POINT('Ctrl Pts',(17.8820084580608,14.402664405411,5.93519388745609));
#133592=CARTESIAN_POINT('Ctrl Pts',(17.8812400921136,14.408059819301,5.94250466435763));
#133593=CARTESIAN_POINT('Ctrl Pts',(17.8771815965658,14.4375218777562,5.98092208253775));
#133594=CARTESIAN_POINT('Ctrl Pts',(17.8740151442579,14.4639112807589,6.01017395289943));
#133595=CARTESIAN_POINT('Ctrl Pts',(17.8682413450271,14.5160426850946,6.0594234311034));
#133596=CARTESIAN_POINT('Ctrl Pts',(17.865640759731,14.5410121975035,6.08008557158004));
#133597=CARTESIAN_POINT('Ctrl Pts',(17.8617627384983,14.5794450817572,6.1078492467406));
#133598=CARTESIAN_POINT('Ctrl Pts',(17.860523755482,14.5919003971697,6.1162806240157));
#133599=CARTESIAN_POINT('Ctrl Pts',(17.8582050200211,14.6154368489631,6.13118667298788));
#133600=CARTESIAN_POINT('Ctrl Pts',(17.8571291043679,14.6264462082628,6.13776402984319));
#133601=CARTESIAN_POINT('Ctrl Pts',(17.855290973987,14.645359064967,6.14840546913147));
#133602=CARTESIAN_POINT('Ctrl Pts',(17.8545341858223,14.6531751626598,6.15261961573129));
#133603=CARTESIAN_POINT('Ctrl Pts',(17.8530757964975,14.6682804200302,6.16041581773013));
#133604=CARTESIAN_POINT('Ctrl Pts',(17.8523751104655,14.6755564652651,6.16402056696697));
#133605=CARTESIAN_POINT('Ctrl Pts',(17.8504863735569,14.6952087361591,6.17335672703167));
#133606=CARTESIAN_POINT('Ctrl Pts',(17.849291109414,14.7076860520455,6.17886633339106));
#133607=CARTESIAN_POINT('Ctrl Pts',(17.843979450735,14.7632628714261,6.20159116583678));
#133608=CARTESIAN_POINT('Ctrl Pts',(17.8397485794156,14.8077692527472,6.21506676510296));
#133609=CARTESIAN_POINT('Ctrl Pts',(17.8329486414327,14.8803065654519,6.22976528263476));
#133610=CARTESIAN_POINT('Ctrl Pts',(17.830407290844,14.9076642256996,6.23372892075528));
#133611=CARTESIAN_POINT('Ctrl Pts',(17.8268887289436,14.9463004534994,6.23713090235582));
#133612=CARTESIAN_POINT('Ctrl Pts',(17.8258824031434,14.9574417272552,6.23785800358135));
#133613=CARTESIAN_POINT('Ctrl Pts',(17.8241045149926,14.9773347265326,6.23870412961868));
#133614=CARTESIAN_POINT('Ctrl Pts',(17.8233294329946,14.986080095653,6.2389206742171));
#133615=CARTESIAN_POINT('Ctrl Pts',(17.8221026698386,15.0000612901527,6.23901852936151));
#133616=CARTESIAN_POINT('Ctrl Pts',(17.8216461887232,15.0052952749617,6.23899956451928));
#133617=CARTESIAN_POINT('Ctrl Pts',(17.8207314458554,15.0158540218926,6.2388491136678));
#133618=CARTESIAN_POINT('Ctrl Pts',(17.8202733090936,15.0211784369813,6.23871567069239));
#133619=CARTESIAN_POINT('Ctrl Pts',(17.8190279724218,15.0357376744717,6.23819322733457));
#133620=CARTESIAN_POINT('Ctrl Pts',(17.8182466222171,15.044967776164,6.23768851536866));
#133621=CARTESIAN_POINT('Ctrl Pts',(17.8145572389187,15.0888834387855,6.23445974063924));
#133622=CARTESIAN_POINT('Ctrl Pts',(17.8117434313418,15.1233616936699,6.22946139450966));
#133623=CARTESIAN_POINT('Ctrl Pts',(17.8061125579971,15.1916311761641,6.21458277587953));
#133624=CARTESIAN_POINT('Ctrl Pts',(17.8033022874982,15.2253221172352,6.204684912613));
#133625=CARTESIAN_POINT('Ctrl Pts',(17.7995643188042,15.2682001810777,6.18869730783189));
#133626=CARTESIAN_POINT('Ctrl Pts',(17.7986865934601,15.2781357857205,6.18474505181408));
#133627=CARTESIAN_POINT('Ctrl Pts',(17.7965061778855,15.3024357126063,6.17446272120241));
#133628=CARTESIAN_POINT('Ctrl Pts',(17.7951973605519,15.3166900371444,6.16788821900382));
#133629=CARTESIAN_POINT('Ctrl Pts',(17.7930819921121,15.3391145368598,6.15666610818905));
#133630=CARTESIAN_POINT('Ctrl Pts',(17.7922852957676,15.3474245970957,6.15230758016244));
#133631=CARTESIAN_POINT('Ctrl Pts',(17.7907335736692,15.3633330250821,6.14357358052954));
#133632=CARTESIAN_POINT('Ctrl Pts',(17.7899793786343,15.3709409727368,6.13921875835267));
#133633=CARTESIAN_POINT('Ctrl Pts',(17.7881648719207,15.388937575467,6.12848795379586));
#133634=CARTESIAN_POINT('Ctrl Pts',(17.7871002931057,15.3992490987736,6.12198847590305));
#133635=CARTESIAN_POINT('Ctrl Pts',(17.78076740689,15.4590942968259,6.08216596608944));
#133636=CARTESIAN_POINT('Ctrl Pts',(17.7752878249124,15.5045937966032,6.04320053010109));
#133637=CARTESIAN_POINT('Ctrl Pts',(17.7671456565326,15.5644643549734,5.97784891596493));
#133638=CARTESIAN_POINT('Ctrl Pts',(17.7644964291953,15.5827562249121,5.95536263593209));
#133639=CARTESIAN_POINT('Ctrl Pts',(17.7611176699925,15.6048558590097,5.92467488315749));
#133640=CARTESIAN_POINT('Ctrl Pts',(17.7603328184777,15.6098999625671,5.91739839937542));
#133641=CARTESIAN_POINT('Ctrl Pts',(17.7590955700563,15.6177209700958,5.90567139697697));
#133642=CARTESIAN_POINT('Ctrl Pts',(17.7586381896056,15.6205831801299,5.90127920620893));
#133643=CARTESIAN_POINT('Ctrl Pts',(17.7577265276395,15.6262330406788,5.89240417700884));
#133644=CARTESIAN_POINT('Ctrl Pts',(17.7572723100364,15.6290198849706,5.88792118929938));
#133645=CARTESIAN_POINT('Ctrl Pts',(17.7560478520044,15.6364487983189,5.87568025118322));
#133646=CARTESIAN_POINT('Ctrl Pts',(17.7552831649684,15.6409971341373,5.86786603678916));
#133647=CARTESIAN_POINT('Ctrl Pts',(17.7512837644971,15.6642332271655,5.82620530852942));
#133648=CARTESIAN_POINT('Ctrl Pts',(17.748168794692,15.6803893692854,5.79101004835711));
#133649=CARTESIAN_POINT('Ctrl Pts',(17.7424137329593,15.7050261840549,5.72390949017262));
#133650=CARTESIAN_POINT('Ctrl Pts',(17.7397798216937,15.7142699582852,5.69239444765107));
#133651=CARTESIAN_POINT('Ctrl Pts',(17.7358606719001,15.7246712388821,5.64560680992097));
#133652=CARTESIAN_POINT('Ctrl Pts',(17.734614964762,15.7274991761849,5.63074648288295));
#133653=CARTESIAN_POINT('Ctrl Pts',(17.7322860581138,15.7318853442907,5.60310371277995));
#133654=CARTESIAN_POINT('Ctrl Pts',(17.7312067842912,15.7335692872186,5.59034706958058));
#133655=CARTESIAN_POINT('Ctrl Pts',(17.7293665494819,15.7358496682767,5.56873758539821));
#133656=CARTESIAN_POINT('Ctrl Pts',(17.7286111087456,15.7366212500323,5.55990583796171));
#133657=CARTESIAN_POINT('Ctrl Pts',(17.7271578981829,15.7377918055203,5.54300559131467));
#133658=CARTESIAN_POINT('Ctrl Pts',(17.7264610725707,15.7382177191518,5.53494019173273));
#133659=CARTESIAN_POINT('Ctrl Pts',(17.7245899423742,15.7390015656981,5.51339629710099));
#133660=CARTESIAN_POINT('Ctrl Pts',(17.7234086093312,15.7391229365185,5.49991295132311));
#133661=CARTESIAN_POINT('Ctrl Pts',(17.719128989283,15.7382346614887,5.45153012444489));
#133662=CARTESIAN_POINT('Ctrl Pts',(17.7159712737335,15.7351214353682,5.41672030624534));
#133663=CARTESIAN_POINT('Ctrl Pts',(17.7099731759565,15.7246829704905,5.352036499593));
#133664=CARTESIAN_POINT('Ctrl Pts',(17.7071476266353,15.7179306639605,5.32214010715026));
#133665=CARTESIAN_POINT('Ctrl Pts',(17.7028842479441,15.7048621289642,5.27741135825029));
#133666=CARTESIAN_POINT('Ctrl Pts',(17.7014302638556,15.699884297055,5.26222202625305));
#133667=CARTESIAN_POINT('Ctrl Pts',(17.6989806038956,15.6905675821346,5.23662938264491));
#133668=CARTESIAN_POINT('Ctrl Pts',(17.6979768736244,15.6864762076922,5.22614214523881));
#133669=CARTESIAN_POINT('Ctrl Pts',(17.6964804699617,15.6799439712499,5.21046591513333));
#133670=CARTESIAN_POINT('Ctrl Pts',(17.6959790340752,15.6776799417493,5.205205675752));
#133671=CARTESIAN_POINT('Ctrl Pts',(17.6950479604336,15.6733316556893,5.19541780124666));
#133672=CARTESIAN_POINT('Ctrl Pts',(17.6946175951702,15.6712625050802,5.19088434848346));
#133673=CARTESIAN_POINT('Ctrl Pts',(17.6935517128162,15.665992422427,5.17964026349543));
#133674=CARTESIAN_POINT('Ctrl Pts',(17.6929194274527,15.6627357863013,5.17295633534131));
#133675=CARTESIAN_POINT('Ctrl Pts',(17.6902579158978,15.6484945915148,5.14481439098841));
#133676=CARTESIAN_POINT('Ctrl Pts',(17.6882765813078,15.6365632969928,5.12384907552866));
#133677=CARTESIAN_POINT('Ctrl Pts',(17.6826442071829,15.5993934126117,5.06538687230828));
#133678=CARTESIAN_POINT('Ctrl Pts',(17.6790535765827,15.5717167211382,5.02957341986894));
#133679=CARTESIAN_POINT('Ctrl Pts',(17.6739532852413,15.5290121786705,4.98369217558182));
#133680=CARTESIAN_POINT('Ctrl Pts',(17.6725181465541,15.5166302967901,4.97130281259466));
#133681=CARTESIAN_POINT('Ctrl Pts',(17.6698810594746,15.4933583087574,4.94961549065774));
#133682=CARTESIAN_POINT('Ctrl Pts',(17.6686851847012,15.4826157001997,4.94017184727217));
#133683=CARTESIAN_POINT('Ctrl Pts',(17.6667055549473,15.4645800091548,4.92522203335335));
#133684=CARTESIAN_POINT('Ctrl Pts',(17.6659294088749,15.4574464802409,4.91952864165879));
#133685=CARTESIAN_POINT('Ctrl Pts',(17.6643938356443,15.4432246853306,4.90860295602732));
#133686=CARTESIAN_POINT('Ctrl Pts',(17.6636348941104,15.4361446565706,4.90336241383473));
#133687=CARTESIAN_POINT('Ctrl Pts',(17.6617430796023,15.4183822588667,4.89070003330132));
#133688=CARTESIAN_POINT('Ctrl Pts',(17.6606047350061,15.4075948418936,4.88343162418332));
#133689=CARTESIAN_POINT('Ctrl Pts',(17.6547182680103,15.3513552918553,4.84765916410755));
#133690=CARTESIAN_POINT('Ctrl Pts',(17.6498075183872,15.3030963671255,4.82388650524745));
#133691=CARTESIAN_POINT('Ctrl Pts',(17.6419098790068,15.2223576673412,4.79450671670751));
#133692=CARTESIAN_POINT('Ctrl Pts',(17.6389472842578,15.1913190883785,4.78546439627623));
#133693=CARTESIAN_POINT('Ctrl Pts',(17.6352322293206,15.1507672843944,4.77648390056853));
#133694=CARTESIAN_POINT('Ctrl Pts',(17.6344124872322,15.1417115889341,4.7746558266021));
#133695=CARTESIAN_POINT('Ctrl Pts',(17.6331335878699,15.1273873595482,4.77204272868788));
#133696=CARTESIAN_POINT('Ctrl Pts',(17.6326689031502,15.1221409192571,4.77114409544008));
#133697=CARTESIAN_POINT('Ctrl Pts',(17.6317555355925,15.1117391030106,4.76947790431085));
#133698=CARTESIAN_POINT('Ctrl Pts',(17.6313067728169,15.1065844509896,4.76870804829337));
#133699=CARTESIAN_POINT('Ctrl Pts',(17.6301167437775,15.0928095386986,4.7667994914346));
#133700=CARTESIAN_POINT('Ctrl Pts',(17.6293804925715,15.0841762227602,4.76575822754224));
#133701=CARTESIAN_POINT('Ctrl Pts',(17.6250160098549,15.0324584782375,4.76044484134559));
#133702=CARTESIAN_POINT('Ctrl Pts',(17.62154249778,14.9890786829572,4.75981269019647));
#133703=CARTESIAN_POINT('Ctrl Pts',(17.6145033534909,14.9018684671185,4.76621574794428));
#133704=CARTESIAN_POINT('Ctrl Pts',(17.6109495026657,14.8582329838677,4.77338420293328));
#133705=CARTESIAN_POINT('Ctrl Pts',(17.6062122060801,14.8031189195521,4.78759397256809));
#133706=CARTESIAN_POINT('Ctrl Pts',(17.6051392942247,14.7908225715475,4.79110701001482));
#133707=CARTESIAN_POINT('Ctrl Pts',(17.603306043425,14.770173349812,4.79759045462644));
#133708=CARTESIAN_POINT('Ctrl Pts',(17.6025511050842,14.761771231832,4.80039547021402));
#133709=CARTESIAN_POINT('Ctrl Pts',(17.601096260436,14.7457859469826,4.80605343979563));
#133710=CARTESIAN_POINT('Ctrl Pts',(17.60039726597,14.7381952558168,4.80888143007729));
#133711=CARTESIAN_POINT('Ctrl Pts',(17.59851355857,14.7179887948858,4.81679020149647));
#133712=CARTESIAN_POINT('Ctrl Pts',(17.5973216553542,14.7054648931511,4.8220951644158));
#133713=CARTESIAN_POINT('Ctrl Pts',(17.5919065423122,14.649781713568,4.8475161089425));
#133714=CARTESIAN_POINT('Ctrl Pts',(17.5875613246051,14.6084883446173,4.87142614538585));
#133715=CARTESIAN_POINT('Ctrl Pts',(17.5806957622174,14.5477641622675,4.91490387860572));
#133716=CARTESIAN_POINT('Ctrl Pts',(17.5782033041361,14.5266226302212,4.93187261042478));
#133717=CARTESIAN_POINT('Ctrl Pts',(17.5747437895731,14.4982395749508,4.95734039382775));
#133718=CARTESIAN_POINT('Ctrl Pts',(17.5737481911643,14.4901853216079,4.96490001219207));
#133719=CARTESIAN_POINT('Ctrl Pts',(17.5719874088784,14.4761129942051,4.97871442797565));
#133720=CARTESIAN_POINT('Ctrl Pts',(17.5712187713798,14.4700299598114,4.98489999090565));
#133721=CARTESIAN_POINT('Ctrl Pts',(17.5700007470199,14.4604721029733,4.99496756896773));
#133722=CARTESIAN_POINT('Ctrl Pts',(17.5695466269355,14.4569271547867,4.99878148582861));
#133723=CARTESIAN_POINT('Ctrl Pts',(17.5686921882016,14.4502886329577,5.00607683150433));
#133724=CARTESIAN_POINT('Ctrl Pts',(17.5682912631719,14.447187136588,5.00955058852532));
#133725=CARTESIAN_POINT('Ctrl Pts',(17.5671681689619,14.4385435135944,5.01941785416487));
#133726=CARTESIAN_POINT('Ctrl Pts',(17.5664511832961,14.4330778083794,5.02587782916741));
#133727=CARTESIAN_POINT('Ctrl Pts',(17.5612718209102,14.3940763707777,5.0736131911522));
#133728=CARTESIAN_POINT('Ctrl Pts',(17.5570484972381,14.3649670176315,5.11831413405712));
#133729=CARTESIAN_POINT('Ctrl Pts',(17.550404627432,14.3277103715715,5.1917810746355));
#133730=CARTESIAN_POINT('Ctrl Pts',(17.5480389773663,14.3160681034596,5.21855879345734));
#133731=CARTESIAN_POINT('Ctrl Pts',(17.5443432185663,14.3006976901226,5.26054488911534));
#133732=CARTESIAN_POINT('Ctrl Pts',(17.543047047265,14.2958176965653,5.27530089849097));
#133733=CARTESIAN_POINT('Ctrl Pts',(17.5409471662091,14.2887517903108,5.29916564517675));
#133734=CARTESIAN_POINT('Ctrl Pts',(17.5401530592254,14.2862674392464,5.30818167766472));
#133735=CARTESIAN_POINT('Ctrl Pts',(17.5386032568386,14.2817852988349,5.32574268440951));
#133736=CARTESIAN_POINT('Ctrl Pts',(17.5378483472904,14.2797673018426,5.33428091515895));
#133737=CARTESIAN_POINT('Ctrl Pts',(17.5360267496239,14.2752947951494,5.35483225656747));
#133738=CARTESIAN_POINT('Ctrl Pts',(17.5349556938405,14.2729864167714,5.36687405158692));
#133739=CARTESIAN_POINT('Ctrl Pts',(17.5286685695326,14.2613008568798,5.43725994863433));
#133740=CARTESIAN_POINT('Ctrl Pts',(17.5232463597049,14.2586515972324,5.49649196972236));
#133741=CARTESIAN_POINT('Ctrl Pts',(17.5151346763136,14.2652698972504,5.58454088115257));
#133742=CARTESIAN_POINT('Ctrl Pts',(17.5124599248356,14.2691887837803,5.613537699438));
#133743=CARTESIAN_POINT('Ctrl Pts',(17.5090536742073,14.2765258409504,5.65094726546426));
#133744=CARTESIAN_POINT('Ctrl Pts',(17.5082659322136,14.2783929847485,5.65963481161436));
#133745=CARTESIAN_POINT('Ctrl Pts',(17.5070252356715,14.2816117531252,5.67339802907555));
#133746=CARTESIAN_POINT('Ctrl Pts',(17.5065672542576,14.2828614985113,5.67849628847932));
#133747=CARTESIAN_POINT('Ctrl Pts',(17.5057115869217,14.2853144601774,5.68806108013354));
#133748=CARTESIAN_POINT('Ctrl Pts',(17.505313223435,14.2865054772999,5.69253041433309));
#133749=CARTESIAN_POINT('Ctrl Pts',(17.5042079666093,14.2899452142966,5.70496765274709));
#133750=CARTESIAN_POINT('Ctrl Pts',(17.5035059867801,14.2922860716379,5.71290972519018));
#133751=CARTESIAN_POINT('Ctrl Pts',(17.5019765370958,14.29772112311,5.73026850801131));
#133752=CARTESIAN_POINT('Ctrl Pts',(17.5011520742185,14.3008710928694,5.73966193347026));
#133753=CARTESIAN_POINT('Ctrl Pts',(17.5003341513661,14.3042076696198,5.74898600961524));
#133754=CARTESIAN_POINT('',(17.4440936240989,14.2607889278854,5.49961548488437));
#133755=CARTESIAN_POINT('Ctrl Pts',(17.4211934345165,14.3041892428936,5.74893451005237));
#133756=CARTESIAN_POINT('Ctrl Pts',(17.4224519124576,14.2993228908923,5.73533229768884));
#133757=CARTESIAN_POINT('Ctrl Pts',(17.4237230400774,14.2948568242566,5.72159138443025));
#133758=CARTESIAN_POINT('Ctrl Pts',(17.4274963788901,14.2829172297248,5.6808287340023));
#133759=CARTESIAN_POINT('Ctrl Pts',(17.4300299028855,14.2765757763358,5.65350491668053));
#133760=CARTESIAN_POINT('Ctrl Pts',(17.4364551078773,14.2645924814883,5.58418881435459));
#133761=CARTESIAN_POINT('Ctrl Pts',(17.4403722648504,14.2609787020888,5.54194608807033));
#133762=CARTESIAN_POINT('Ctrl Pts',(17.4442144194927,14.2610000944162,5.49962643999587));
#133763=CARTESIAN_POINT('Ctrl Pts',(17.4440936240989,14.2607889278854,5.49961548488437));
#133764=CARTESIAN_POINT('Ctrl Pts',(17.4463925298371,14.2607552983813,5.47398865868977));
#133765=CARTESIAN_POINT('Ctrl Pts',(17.4486651958888,14.2620694570682,5.44839224160943));
#133766=CARTESIAN_POINT('Ctrl Pts',(17.4508827009377,14.2647377317864,5.42293429490633));
#133767=CARTESIAN_POINT('Ctrl Pts',(17.4508839600479,14.2647392468458,5.42291983976008));
#133768=CARTESIAN_POINT('Ctrl Pts',(17.4508852191412,14.2647407623429,5.42290538464378));
#133769=CARTESIAN_POINT('Ctrl Pts',(17.4508864782176,14.2647422782778,5.42289092955747));
#133770=CARTESIAN_POINT('Ctrl Pts',(17.4534752245319,14.2678591428434,5.39317029482624));
#133771=CARTESIAN_POINT('Ctrl Pts',(17.4559927009204,14.2728295072601,5.36357321786261));
#133772=CARTESIAN_POINT('Ctrl Pts',(17.4584798706255,14.2796103457723,5.33434531442345));
#133773=CARTESIAN_POINT('Ctrl Pts',(17.4587365249233,14.2803100693751,5.33132924880557));
#133774=CARTESIAN_POINT('Ctrl Pts',(17.458992856502,14.2810290391182,5.32831714642689));
#133775=CARTESIAN_POINT('Ctrl Pts',(17.4592489103732,14.2817671846145,5.32530929854553));
#133776=CARTESIAN_POINT('Ctrl Pts',(17.4619831816311,14.289649471282,5.29318999500387));
#133777=CARTESIAN_POINT('Ctrl Pts',(17.4646866232128,14.2997220837668,5.26155162396274));
#133778=CARTESIAN_POINT('Ctrl Pts',(17.4674062102649,14.311877644897,5.23070195007791));
#133779=CARTESIAN_POINT('Ctrl Pts',(17.4701229941021,14.3240206766796,5.19988407450164));
#133780=CARTESIAN_POINT('Ctrl Pts',(17.4728563706849,14.3382417983359,5.16985322151559));
#133781=CARTESIAN_POINT('Ctrl Pts',(17.4756355548843,14.3543976419034,5.14089216370232));
#133782=CARTESIAN_POINT('Ctrl Pts',(17.4784134144559,14.3705457851971,5.11194490944399));
#133783=CARTESIAN_POINT('Ctrl Pts',(17.4812372627742,14.3886264976727,5.08406635675437));
#133784=CARTESIAN_POINT('Ctrl Pts',(17.484113473344,14.4084667951577,5.05751587338498));
#133785=CARTESIAN_POINT('Ctrl Pts',(17.4869920359349,14.4283233170452,5.0309436783589));
#133786=CARTESIAN_POINT('Ctrl Pts',(17.4899230881165,14.4499422088045,5.00570169173601));
#133787=CARTESIAN_POINT('Ctrl Pts',(17.4928881991985,14.4731231936543,4.98202770814059));
#133788=CARTESIAN_POINT('Ctrl Pts',(17.4958547296242,14.4963152748123,4.95834239224758));
#133789=CARTESIAN_POINT('Ctrl Pts',(17.4988551886701,14.5210710856156,4.93622663440896));
#133790=CARTESIAN_POINT('Ctrl Pts',(17.5018471367613,14.5471628832735,4.9158962898947));
#133791=CARTESIAN_POINT('Ctrl Pts',(17.5048448871375,14.5733052807554,4.89552651874272));
#133792=CARTESIAN_POINT('Ctrl Pts',(17.5078336209821,14.6007892643748,4.87694940277729));
#133793=CARTESIAN_POINT('Ctrl Pts',(17.5107511946049,14.6293542969684,4.86035718671592));
#133794=CARTESIAN_POINT('Ctrl Pts',(17.5117839811728,14.6394659807813,4.85448373840042));
#133795=CARTESIAN_POINT('Ctrl Pts',(17.512807710816,14.6497128091566,4.84885876088503));
#133796=CARTESIAN_POINT('Ctrl Pts',(17.5138192735669,14.6600821110534,4.84348986345622));
#133797=CARTESIAN_POINT('Ctrl Pts',(17.5138205326936,14.6600950180781,4.84348318060596));
#133798=CARTESIAN_POINT('Ctrl Pts',(17.5138217918035,14.6601079253185,4.8434764981378));
#133799=CARTESIAN_POINT('Ctrl Pts',(17.5138230508965,14.6601208327746,4.84346981605176));
#133800=CARTESIAN_POINT('Ctrl Pts',(17.5164117982747,14.6866590966042,4.82973117061418));
#133801=CARTESIAN_POINT('Ctrl Pts',(17.5189292749153,14.714113311098,4.81760861770762));
#133802=CARTESIAN_POINT('Ctrl Pts',(17.5214164434176,14.7422546666011,4.8072012718735));
#133803=CARTESIAN_POINT('Ctrl Pts',(17.5216731105494,14.7451587565303,4.80612727001093));
#133804=CARTESIAN_POINT('Ctrl Pts',(17.5219294549139,14.7480701194309,4.80507152471403));
#133805=CARTESIAN_POINT('Ctrl Pts',(17.5221855215289,14.7509884732826,4.80403413735497));
#133806=CARTESIAN_POINT('Ctrl Pts',(17.5249198036721,14.7821506879431,4.79295690367745));
#133807=CARTESIAN_POINT('Ctrl Pts',(17.5276232542732,14.8141155650103,4.78397362308434));
#133808=CARTESIAN_POINT('Ctrl Pts',(17.5303428489279,14.8465669963551,4.77716383381978));
#133809=CARTESIAN_POINT('Ctrl Pts',(17.5330596402498,14.8789849770681,4.77036106402229));
#133810=CARTESIAN_POINT('Ctrl Pts',(17.5357930229162,14.9118882390937,4.76572680621878));
#133811=CARTESIAN_POINT('Ctrl Pts',(17.5385722125199,14.9449617596833,4.76329679466272));
#133812=CARTESIAN_POINT('Ctrl Pts',(17.5413500773439,14.9780195148378,4.76086794144083));
#133813=CARTESIAN_POINT('Ctrl Pts',(17.5441739302386,15.0112472583002,4.76064093479088));
#133814=CARTESIAN_POINT('Ctrl Pts',(17.5470501455451,15.0443332319865,4.76261390234366));
#133815=CARTESIAN_POINT('Ctrl Pts',(17.5499287125112,15.0774462575234,4.76458848303993));
#133816=CARTESIAN_POINT('Ctrl Pts',(17.5528597692182,15.1104172579024,4.76876653967552));
#133817=CARTESIAN_POINT('Ctrl Pts',(17.555824885858,15.1429374873463,4.77511154133677));
#133818=CARTESIAN_POINT('Ctrl Pts',(17.5587914216427,15.1754732814116,4.7814595798016));
#133819=CARTESIAN_POINT('Ctrl Pts',(17.5617918870776,15.2075579056174,4.78997678500314));
#133820=CARTESIAN_POINT('Ctrl Pts',(17.5647838434917,15.2388858369081,4.80059162129109));
#133821=CARTESIAN_POINT('Ctrl Pts',(17.5677816017304,15.270274517466,4.81122704124027));
#133822=CARTESIAN_POINT('Ctrl Pts',(17.5707703453829,15.3009035352746,4.82396875050107));
#133823=CARTESIAN_POINT('Ctrl Pts',(17.5736879316955,15.3304690561188,4.83870483921705));
#133824=CARTESIAN_POINT('Ctrl Pts',(17.5747206290912,15.3409339517916,4.84392076731959));
#133825=CARTESIAN_POINT('Ctrl Pts',(17.5757442715644,15.3512656426126,4.84938615583841));
#133826=CARTESIAN_POINT('Ctrl Pts',(17.5767557500387,15.3614508091328,4.85509460692846));
#133827=CARTESIAN_POINT('Ctrl Pts',(17.5767570089466,15.3614634858098,4.85510171178929));
#133828=CARTESIAN_POINT('Ctrl Pts',(17.5767582678376,15.3614761622863,4.85510881704021));
#133829=CARTESIAN_POINT('Ctrl Pts',(17.5767595267117,15.3614888385623,4.85511592268124));
#133830=CARTESIAN_POINT('Ctrl Pts',(17.5793483248545,15.3875568298914,4.86972824171119));
#133831=CARTESIAN_POINT('Ctrl Pts',(17.5818658542699,15.412778570209,4.88599428489849));
#133832=CARTESIAN_POINT('Ctrl Pts',(17.5843530787296,15.4369454539258,4.90377742783721));
#133833=CARTESIAN_POINT('Ctrl Pts',(17.5846097249538,15.4394391329468,4.90561239551419));
#133834=CARTESIAN_POINT('Ctrl Pts',(17.5848660485118,15.4419215639731,4.90746347358738));
#133835=CARTESIAN_POINT('Ctrl Pts',(17.5851220944084,15.4443925073284,4.90933048228485));
#133836=CARTESIAN_POINT('Ctrl Pts',(17.5878564130194,15.4707797546574,4.92926830083465));
#133837=CARTESIAN_POINT('Ctrl Pts',(17.5905599041572,15.4958593325918,4.95102793994418));
#133838=CARTESIAN_POINT('Ctrl Pts',(17.5932795419803,15.5193909909641,4.97438909846681));
#133839=CARTESIAN_POINT('Ctrl Pts',(17.5959963766293,15.5428983948807,4.99772617827074));
#133840=CARTESIAN_POINT('Ctrl Pts',(17.5987298052276,15.5648613381575,5.02266097655755));
#133841=CARTESIAN_POINT('Ctrl Pts',(17.6015090409049,15.585076754593,5.04895001344882));
#133842=CARTESIAN_POINT('Ctrl Pts',(17.6042869519286,15.6052825358525,5.07522652032378));
#133843=CARTESIAN_POINT('Ctrl Pts',(17.60711085115,15.6237426458637,5.10285572076104));
#133844=CARTESIAN_POINT('Ctrl Pts',(17.6099871097348,15.6402872241836,5.13157618360784));
#133845=CARTESIAN_POINT('Ctrl Pts',(17.6128657200272,15.6568453298027,5.16032012908953));
#133846=CARTESIAN_POINT('Ctrl Pts',(17.6157968169858,15.6714848383772,5.19015704918847));
#133847=CARTESIAN_POINT('Ctrl Pts',(17.6187619671962,15.6840664940894,5.22080897116232));
#133848=CARTESIAN_POINT('Ctrl Pts',(17.6217285365992,15.6966541716867,5.25147556388791));
#133849=CARTESIAN_POINT('Ctrl Pts',(17.6247290289276,15.7071819212573,5.28295804698363));
#133850=CARTESIAN_POINT('Ctrl Pts',(17.6277210019063,15.7155414967452,5.31496189073705));
#133851=CARTESIAN_POINT('Ctrl Pts',(17.6307187765062,15.7239172819685,5.34702779192869));
#133852=CARTESIAN_POINT('Ctrl Pts',(17.6337075260791,15.7301160283842,5.37961733394));
#133853=CARTESIAN_POINT('Ctrl Pts',(17.636625105088,15.7340641420407,5.41241519569096));
#133854=CARTESIAN_POINT('Ctrl Pts',(17.6376576570014,15.7354614074784,5.42402259168815));
#133855=CARTESIAN_POINT('Ctrl Pts',(17.6386811548528,15.7365771384209,5.43565588644526));
#133856=CARTESIAN_POINT('Ctrl Pts',(17.6396924907964,15.7374093556554,5.44730044262293));
#133857=CARTESIAN_POINT('Ctrl Pts',(17.6396937501104,15.737410391931,5.44731494240699));
#133858=CARTESIAN_POINT('Ctrl Pts',(17.6396950094076,15.7374114277703,5.4473294422381));
#133859=CARTESIAN_POINT('Ctrl Pts',(17.6396962686879,15.7374124631733,5.44734394211627));
#133860=CARTESIAN_POINT('Ctrl Pts',(17.6422849540133,15.7395409268393,5.47715114426387));
#133861=CARTESIAN_POINT('Ctrl Pts',(17.6448023693862,15.7398229088094,5.50716082859561));
#133862=CARTESIAN_POINT('Ctrl Pts',(17.6472894785076,15.7382578165603,5.53712364710993));
#133863=CARTESIAN_POINT('Ctrl Pts',(17.6475461208021,15.7380963162616,5.54021548028671));
#133864=CARTESIAN_POINT('Ctrl Pts',(17.6478024403967,15.7379151748501,5.54330677711932));
#133865=CARTESIAN_POINT('Ctrl Pts',(17.6480584823002,15.7377144106899,5.54639723855675));
#133866=CARTESIAN_POINT('Ctrl Pts',(17.6507926814368,15.7355705069541,5.57939940295987));
#133867=CARTESIAN_POINT('Ctrl Pts',(17.6534960514656,15.7311860084348,5.61231109590126));
#133868=CARTESIAN_POINT('Ctrl Pts',(17.6562155679204,15.7246128128331,5.64481052808752));
#133869=CARTESIAN_POINT('Ctrl Pts',(17.6589322813081,15.7180463923725,5.67727646237531));
#133870=CARTESIAN_POINT('Ctrl Pts',(17.6616655883834,15.7092963512731,5.70933093486746));
#133871=CARTESIAN_POINT('Ctrl Pts',(17.6644447048133,15.698454394239,5.74067046867308));
#133872=CARTESIAN_POINT('Ctrl Pts',(17.6672224968963,15.6876176037791,5.77199506808764));
#133873=CARTESIAN_POINT('Ctrl Pts',(17.6700462794709,15.6746912077568,5.80260542889568));
#133874=CARTESIAN_POINT('Ctrl Pts',(17.6729224273329,15.6598001639789,5.83221593928102));
#133875=CARTESIAN_POINT('Ctrl Pts',(17.675800928172,15.6448969378356,5.86185067402984));
#133876=CARTESIAN_POINT('Ctrl Pts',(17.6787319216953,15.6280259466993,5.89048393857087));
#133877=CARTESIAN_POINT('Ctrl Pts',(17.6816969788667,15.6093427930072,5.91784658956881));
#133878=CARTESIAN_POINT('Ctrl Pts',(17.6846634558833,15.5906506927132,5.94522234342655));
#133879=CARTESIAN_POINT('Ctrl Pts',(17.6876638663243,15.5701445460918,5.97132623845906));
#133880=CARTESIAN_POINT('Ctrl Pts',(17.6906557722056,15.5480108339518,5.99590593065765));
#133881=CARTESIAN_POINT('Ctrl Pts',(17.6936534818921,15.5258341860522,6.02053330341454));
#133882=CARTESIAN_POINT('Ctrl Pts',(17.6966421815377,15.5020231917903,6.04363032092347));
#133883=CARTESIAN_POINT('Ctrl Pts',(17.6995597280143,15.476800747688,6.06496215169117));
#133884=CARTESIAN_POINT('Ctrl Pts',(17.7005929302518,15.4678686241065,6.07251647703187));
#133885=CARTESIAN_POINT('Ctrl Pts',(17.7016170689804,15.4587598479432,6.07984962154434));
#133886=CARTESIAN_POINT('Ctrl Pts',(17.7026290303306,15.449485577811,6.08695186598542));
#133887=CARTESIAN_POINT('Ctrl Pts',(17.7026302896054,15.4494740369995,6.08696070394931));
#133888=CARTESIAN_POINT('Ctrl Pts',(17.7026315488634,15.4494624959087,6.08696954157464));
#133889=CARTESIAN_POINT('Ctrl Pts',(17.7026328081046,15.4494509545388,6.08697837886135));
#133890=CARTESIAN_POINT('Ctrl Pts',(17.705221542436,15.4257243305525,6.10514597762664));
#133891=CARTESIAN_POINT('Ctrl Pts',(17.7077390018072,15.4008132845558,6.12188257860068));
#133892=CARTESIAN_POINT('Ctrl Pts',(17.7102261456198,15.3749257598694,6.13705058790182));
#133893=CARTESIAN_POINT('Ctrl Pts',(17.7104828757241,15.3722535754633,6.1386162732432));
#133894=CARTESIAN_POINT('Ctrl Pts',(17.7107392828173,15.3695710324748,6.14016524690346));
#133895=CARTESIAN_POINT('Ctrl Pts',(17.710995411948,15.366878391042,6.14169735964926));
#133896=CARTESIAN_POINT('Ctrl Pts',(17.713729728643,15.3381329906211,6.15805349003897));
#133897=CARTESIAN_POINT('Ctrl Pts',(17.7164332042827,15.3082310928872,6.1724882306324));
#133898=CARTESIAN_POINT('Ctrl Pts',(17.7191528169111,15.2774700364291,6.18486798769374));
#133899=CARTESIAN_POINT('Ctrl Pts',(17.7218696256405,15.2467406943755,6.19723498132404));
#133900=CARTESIAN_POINT('Ctrl Pts',(17.7246030187271,15.2151543181013,6.20755167245362));
#133901=CARTESIAN_POINT('Ctrl Pts',(17.7273822157546,15.1830148370127,6.21572778788368));
#133902=CARTESIAN_POINT('Ctrl Pts',(17.7301600872982,15.1508906842223,6.22390000387509));
#133903=CARTESIAN_POINT('Ctrl Pts',(17.7329839439362,15.1182141126201,6.22993396079429));
#133904=CARTESIAN_POINT('Ctrl Pts',(17.7358601647421,15.0852924129001,6.2337769843443));
#133905=CARTESIAN_POINT('Ctrl Pts',(17.7387387356219,15.0523438138463,6.23762314791363));
#133906=CARTESIAN_POINT('Ctrl Pts',(17.7416697979649,15.0191497260224,6.23927488801611));
#133907=CARTESIAN_POINT('Ctrl Pts',(17.7446349270463,14.9860205343245,6.23871418193894));
#133908=CARTESIAN_POINT('Ctrl Pts',(17.7476014743928,14.9528754964446,6.23815320766777));
#133909=CARTESIAN_POINT('Ctrl Pts',(17.7506019582001,14.9197953589216,6.23537753125499));
#133910=CARTESIAN_POINT('Ctrl Pts',(17.7535939449745,14.8870934545809,6.2304041588691));
#133911=CARTESIAN_POINT('Ctrl Pts',(17.7565917316453,14.8543281583636,6.22542114571718));
#133912=CARTESIAN_POINT('Ctrl Pts',(17.7595805158066,14.8219425048939,6.2182313951504));
#133913=CARTESIAN_POINT('Ctrl Pts',(17.7624981597374,14.7902552237342,6.20889196031308));
#133914=CARTESIAN_POINT('Ctrl Pts',(17.7635305207602,14.7790431928056,6.20558735264657));
#133915=CARTESIAN_POINT('Ctrl Pts',(17.7645538352473,14.7679186330585,6.20201401295087));
#133916=CARTESIAN_POINT('Ctrl Pts',(17.7655649975604,14.7568957630668,6.19817590699701));
#133917=CARTESIAN_POINT('Ctrl Pts',(17.7655662553768,14.7568820513741,6.19817113265698));
#133918=CARTESIAN_POINT('Ctrl Pts',(17.7655675131764,14.7568683398103,6.19816635789855));
#133919=CARTESIAN_POINT('Ctrl Pts',(17.7655687709592,14.7568546283756,6.19816158272171));
#133920=CARTESIAN_POINT('Ctrl Pts',(17.7681578335635,14.7286305475446,6.18833219726503));
#133921=CARTESIAN_POINT('Ctrl Pts',(17.7706756363368,14.7009506171342,6.17672629876546));
#133922=CARTESIAN_POINT('Ctrl Pts',(17.7731631483601,14.6740441602152,6.16344195838684));
#133923=CARTESIAN_POINT('Ctrl Pts',(17.7734197974233,14.6712680864123,6.16207134651384));
#133924=CARTESIAN_POINT('Ctrl Pts',(17.7736761240389,14.6685002701096,6.16068290654834));
#133925=CARTESIAN_POINT('Ctrl Pts',(17.7739321732037,14.665740978691,6.15927677356913));
#133926=CARTESIAN_POINT('Ctrl Pts',(17.7766666913574,14.6362726830942,6.14425975072063));
#133927=CARTESIAN_POINT('Ctrl Pts',(17.779370402119,14.6077734432019,6.12722017812163));
#133928=CARTESIAN_POINT('Ctrl Pts',(17.7820902725442,14.5805183433097,6.10833296822113));
#133929=CARTESIAN_POINT('Ctrl Pts',(17.7848072466106,14.5532922670595,6.08946587109295));
#133930=CARTESIAN_POINT('Ctrl Pts',(17.7875408262062,14.5273075043819,6.06875561023286));
#133931=CARTESIAN_POINT('Ctrl Pts',(17.7903202095314,14.5028065590824,6.04640639711805));
#133932=CARTESIAN_POINT('Ctrl Pts',(17.7930996912874,14.4783047460923,6.02405639251532));
#133933=CARTESIAN_POINT('Ctrl Pts',(17.7959252069821,14.4552867150597,6.00006760155612));
#133934=CARTESIAN_POINT('Ctrl Pts',(17.7988031159527,14.4339657418564,5.97466806841847));
#133935=CARTESIAN_POINT('Ctrl Pts',(17.8016809333757,14.4126454468827,5.94926934325114));
#133936=CARTESIAN_POINT('Ctrl Pts',(17.804611178714,14.3930220433968,5.92246005215071));
#133937=CARTESIAN_POINT('Ctrl Pts',(17.8075754145475,14.3752810566636,5.89448927635161));
#133938=CARTESIAN_POINT('Ctrl Pts',(17.8105439488833,14.3575143433425,5.8664779395268));
#133939=CARTESIAN_POINT('Ctrl Pts',(17.8135464127681,14.3416355993389,5.83730161808677));
#133940=CARTESIAN_POINT('Ctrl Pts',(17.8165402612616,14.3278032035129,5.80723189254072));
#133941=CARTESIAN_POINT('Ctrl Pts',(17.8184366140737,14.3190415367889,5.78818523446117));
#133942=CARTESIAN_POINT('Ctrl Pts',(17.8203290112871,14.3111003597056,5.76878054731838));
#133943=CARTESIAN_POINT('Ctrl Pts',(17.8222024383386,14.3040135853341,5.74909189204504));
#133944=CARTESIAN_POINT('Origin',(13.2437274406976,15.,5.5));
#133945=CARTESIAN_POINT('',(17.8436773584655,14.2610291961454,5.50063939925591));
#133946=CARTESIAN_POINT('Ctrl Pts',(17.8222024383946,14.3040135851224,5.74909189145678));
#133947=CARTESIAN_POINT('Ctrl Pts',(17.8243357978047,14.295943542177,5.72667149457543));
#133948=CARTESIAN_POINT('Ctrl Pts',(17.8264445030159,14.2889817446023,5.70388266077197));
#133949=CARTESIAN_POINT('Ctrl Pts',(17.8285029552338,14.2831690256882,5.68084193278501));
#133950=CARTESIAN_POINT('Ctrl Pts',(17.828504216325,14.2831654645812,5.68082781710211));
#133951=CARTESIAN_POINT('Ctrl Pts',(17.8285054773985,14.2831619039007,5.68081370130835));
#133952=CARTESIAN_POINT('Ctrl Pts',(17.8285067384545,14.2831583436466,5.68079958540374));
#133953=CARTESIAN_POINT('Ctrl Pts',(17.8312998697714,14.2752726846418,5.64953406105414));
#133954=CARTESIAN_POINT('Ctrl Pts',(17.8340065810712,14.2694783607943,5.6177204690563));
#133955=CARTESIAN_POINT('Ctrl Pts',(17.8366815091306,14.2658017005483,5.58560485200468));
#133956=CARTESIAN_POINT('Ctrl Pts',(17.8375267351236,14.2646399463859,5.57545693261783));
#133957=CARTESIAN_POINT('Ctrl Pts',(17.8383687877544,14.2636896841653,5.56527924594083));
#133958=CARTESIAN_POINT('Ctrl Pts',(17.8392093907452,14.2629518112339,5.55508063474149));
#133959=CARTESIAN_POINT('Ctrl Pts',(17.8407006737749,14.2616427778463,5.53698765152026));
#133960=CARTESIAN_POINT('Ctrl Pts',(17.8421872462419,14.2610012335988,5.51882616272172));
#133961=CARTESIAN_POINT('Ctrl Pts',(17.8436773584384,14.2610291961449,5.50063939958663));
#133962=CARTESIAN_POINT('',(18.1999951595719,14.4315705875013,5.97264794125123));
#133963=CARTESIAN_POINT('Ctrl Pts',(17.8436773585104,14.2610291961463,5.50063939870812));
#133964=CARTESIAN_POINT('Ctrl Pts',(17.8463594095494,14.2610795259361,5.46790506697329));
#133965=CARTESIAN_POINT('Ctrl Pts',(17.8490517590635,14.2633033205486,5.43512841146423));
#133966=CARTESIAN_POINT('Ctrl Pts',(17.8517858606446,14.2676752024076,5.40262005104255));
#133967=CARTESIAN_POINT('Ctrl Pts',(17.8545179415039,14.2720438530929,5.37013571692455));
#133968=CARTESIAN_POINT('Ctrl Pts',(17.8572919721943,14.2785570835378,5.33791937843377));
#133969=CARTESIAN_POINT('Ctrl Pts',(17.8601181797673,14.2871520781629,5.30627092034022));
#133970=CARTESIAN_POINT('Ctrl Pts',(17.8629460917766,14.2957522562788,5.27460337561596));
#133971=CARTESIAN_POINT('Ctrl Pts',(17.8658263187323,14.3064365697756,5.24350444886535));
#133972=CARTESIAN_POINT('Ctrl Pts',(17.8687454375362,14.31910807561,5.21326341890527));
#133973=CARTESIAN_POINT('Ctrl Pts',(17.8716654355075,14.3317833977924,5.18301328108585));
#133974=CARTESIAN_POINT('Ctrl Pts',(17.8746242343264,14.3464471824028,5.15362159625291));
#133975=CARTESIAN_POINT('Ctrl Pts',(17.8775849802679,14.3629689473109,5.12536610898706));
#133976=CARTESIAN_POINT('Ctrl Pts',(17.8805516191879,14.3795235966361,5.09705438286081));
#133977=CARTESIAN_POINT('Ctrl Pts',(17.8835198303149,14.3979440054524,5.06988351684653));
#133978=CARTESIAN_POINT('Ctrl Pts',(17.8864326303791,14.4180620188063,5.04411993333822));
#133979=CARTESIAN_POINT('Ctrl Pts',(17.8881248041672,14.4297494584233,5.02915273348248));
#133980=CARTESIAN_POINT('Ctrl Pts',(17.889797916704,14.4420091275208,5.01466025184568));
#133981=CARTESIAN_POINT('Ctrl Pts',(17.8914388206508,14.4548013425205,5.00069220202942));
#133982=CARTESIAN_POINT('Ctrl Pts',(17.8914400802631,14.4548111622496,5.00068147969052));
#133983=CARTESIAN_POINT('Ctrl Pts',(17.8914413398586,14.4548209823129,5.0006707576363));
#133984=CARTESIAN_POINT('Ctrl Pts',(17.8914425994372,14.4548308027104,5.00066003586679));
#133985=CARTESIAN_POINT('Ctrl Pts',(17.8940314338703,14.4750148415794,4.97862339112774));
#133986=CARTESIAN_POINT('Ctrl Pts',(17.8965489662599,14.496615226222,4.95778864968078));
#133987=CARTESIAN_POINT('Ctrl Pts',(17.8990361340503,14.5194513004904,4.93832760805207));
#133988=CARTESIAN_POINT('Ctrl Pts',(17.8992933057813,14.5218125375449,4.93631534744756));
#133989=CARTESIAN_POINT('Ctrl Pts',(17.8995501528709,14.5241869404141,4.93431778010501));
#133990=CARTESIAN_POINT('Ctrl Pts',(17.899806720575,14.5265742779001,4.93233509938062));
#133991=CARTESIAN_POINT('Ctrl Pts',(17.902541477429,14.552020923942,4.91120169243526));
#133992=CARTESIAN_POINT('Ctrl Pts',(17.9052453302838,14.578942617527,4.89175844415563));
#133993=CARTESIAN_POINT('Ctrl Pts',(17.9079652717836,14.6070698664759,4.87418892292457));
#133994=CARTESIAN_POINT('Ctrl Pts',(17.9106824052865,14.635168077584,4.85663754001058));
#133995=CARTESIAN_POINT('Ctrl Pts',(17.9134160753429,14.6644689296677,4.84095563974389));
#133996=CARTESIAN_POINT('Ctrl Pts',(17.91619552483,14.694688870348,4.82728527763572));
#133997=CARTESIAN_POINT('Ctrl Pts',(17.918973643444,14.7248943409312,4.81362146125409));
#133998=CARTESIAN_POINT('Ctrl Pts',(17.9217977227498,14.756017816082,4.80196701342871));
#133999=CARTESIAN_POINT('Ctrl Pts',(17.9246741683966,14.7877658634584,4.7924275524122));
#134000=CARTESIAN_POINT('Ctrl Pts',(17.927552951004,14.8195397044511,4.78288034108607));
#134001=CARTESIAN_POINT('Ctrl Pts',(17.9304842268543,14.8519390777149,4.77545147120308));
#134002=CARTESIAN_POINT('Ctrl Pts',(17.9334495989564,14.8846614480637,4.77021298268738));
#134003=CARTESIAN_POINT('Ctrl Pts',(17.9364163821299,14.9173993893415,4.76497200143866));
#134004=CARTESIAN_POINT('Ctrl Pts',(17.9394171311389,14.9504607166395,4.76192361340681));
#134005=CARTESIAN_POINT('Ctrl Pts',(17.9424094410172,14.9835338646715,4.76110588474489));
#134006=CARTESIAN_POINT('Ctrl Pts',(17.9454075337696,15.016670929163,4.76028657575803));
#134007=CARTESIAN_POINT('Ctrl Pts',(17.9483966821973,15.0498200071206,4.76170705120555));
#134008=CARTESIAN_POINT('Ctrl Pts',(17.9513147792807,15.0826572162376,4.76536688948503));
#134009=CARTESIAN_POINT('Ctrl Pts',(17.952343720405,15.0942358422743,4.76665737366236));
#134010=CARTESIAN_POINT('Ctrl Pts',(17.9533636886311,15.1057755873781,4.7682258913146));
#134011=CARTESIAN_POINT('Ctrl Pts',(17.9543716120705,15.1172619072478,4.77007104090789));
#134012=CARTESIAN_POINT('Ctrl Pts',(17.9543728624177,15.1172761562348,4.77007332984923));
#134013=CARTESIAN_POINT('Ctrl Pts',(17.9543741127484,15.1172904051685,4.77007561921983));
#134014=CARTESIAN_POINT('Ctrl Pts',(17.9543753630624,15.1173046540489,4.77007790901972));
#134015=CARTESIAN_POINT('Ctrl Pts',(17.956966132579,15.1468296885974,4.77482259201186));
#134016=CARTESIAN_POINT('Ctrl Pts',(17.959485714194,15.1761291355963,4.78141356596197));
#134017=CARTESIAN_POINT('Ctrl Pts',(17.9619751194107,15.2049597393243,4.78979421528902));
#134018=CARTESIAN_POINT('Ctrl Pts',(17.962230909525,15.2079221270356,4.79065533955868));
#134019=CARTESIAN_POINT('Ctrl Pts',(17.9624863810408,15.210879534695,4.79153532500646));
#134020=CARTESIAN_POINT('Ctrl Pts',(17.9627415784489,15.2138316785748,4.79243408630913));
#134021=CARTESIAN_POINT('Ctrl Pts',(17.9654772791855,15.245478481916,4.80206875296297));
#134022=CARTESIAN_POINT('Ctrl Pts',(17.9681823166877,15.2765243880882,4.81386500752228));
#134023=CARTESIAN_POINT('Ctrl Pts',(17.9709036077638,15.3066678945923,4.82769865939054));
#134024=CARTESIAN_POINT('Ctrl Pts',(17.9736221022352,15.3367804233474,4.84151809475102));
#134025=CARTESIAN_POINT('Ctrl Pts',(17.9763572964495,15.3659924876036,4.85737017958949));
#134026=CARTESIAN_POINT('Ctrl Pts',(17.979138305386,15.3940294988691,4.87509618555731));
#134027=CARTESIAN_POINT('Ctrl Pts',(17.9819179950805,15.4220532100699,4.89281378274626));
#134028=CARTESIAN_POINT('Ctrl Pts',(17.9847436800359,15.4489030742888,4.91240322043754));
#134029=CARTESIAN_POINT('Ctrl Pts',(17.987621605196,15.4743294733481,4.93367749389957));
#134030=CARTESIAN_POINT('Ctrl Pts',(17.9905018851045,15.4997766765523,4.95496917419406));
#134031=CARTESIAN_POINT('Ctrl Pts',(17.993434531532,15.5237981235656,4.97794835812273));
#134032=CARTESIAN_POINT('Ctrl Pts',(17.9964009679253,15.5461672042858,5.00240196307429));
#134033=CARTESIAN_POINT('Ctrl Pts',(17.9993688260062,15.5685470055611,5.02686728760528));
#134034=CARTESIAN_POINT('Ctrl Pts',(18.0023703420288,15.5892727947365,5.05280858692245));
#134035=CARTESIAN_POINT('Ctrl Pts',(18.005362930613,15.6081413450034,5.07998651472653));
#134036=CARTESIAN_POINT('Ctrl Pts',(18.0083613143937,15.6270464345251,5.10721707303048));
#134037=CARTESIAN_POINT('Ctrl Pts',(18.011350260665,15.6440867502017,5.13568945173416));
#134038=CARTESIAN_POINT('Ctrl Pts',(18.0142675126761,15.6590844306501,5.16513277119679));
#134039=CARTESIAN_POINT('Ctrl Pts',(18.0152947004806,15.6643652340887,5.17549999986241));
#134040=CARTESIAN_POINT('Ctrl Pts',(18.0163128615438,15.6693930587093,5.18598730274498));
#134041=CARTESIAN_POINT('Ctrl Pts',(18.0173189327465,15.6741611019489,5.19658180756563));
#134042=CARTESIAN_POINT('Ctrl Pts',(18.0173202085358,15.6741671482592,5.19659524235646));
#134043=CARTESIAN_POINT('Ctrl Pts',(18.0173214843078,15.6741731941654,5.19660867734728));
#134044=CARTESIAN_POINT('Ctrl Pts',(18.0173227600623,15.6741792396675,5.19662211253806));
#134045=CARTESIAN_POINT('Ctrl Pts',(18.0199069065493,15.6864249048209,5.22383620391819));
#134046=CARTESIAN_POINT('Ctrl Pts',(18.0224197289205,15.697011589596,5.25187499153676));
#134047=CARTESIAN_POINT('Ctrl Pts',(18.0249021843778,15.7058528471292,5.28050526628785));
#134048=CARTESIAN_POINT('Ctrl Pts',(18.0251587405207,15.7067665710492,5.28346414026898));
#134049=CARTESIAN_POINT('Ctrl Pts',(18.0254149723221,15.7076616645656,5.28642928749976));
#134050=CARTESIAN_POINT('Ctrl Pts',(18.0256709249919,15.7085380415357,5.28940042032651));
#134051=CARTESIAN_POINT('Ctrl Pts',(18.0284003719407,15.7178836148767,5.32108420560131));
#134052=CARTESIAN_POINT('Ctrl Pts',(18.0310989130854,15.7250996821711,5.35345416599969));
#134053=CARTESIAN_POINT('Ctrl Pts',(18.0338135819061,15.7301240673385,5.3861910161145));
#134054=CARTESIAN_POINT('Ctrl Pts',(18.0365254513628,15.7351432713645,5.41889410801899));
#134055=CARTESIAN_POINT('Ctrl Pts',(18.0392538957621,15.7379758245001,5.451963087929));
#134056=CARTESIAN_POINT('Ctrl Pts',(18.0420282370079,15.7386032531471,5.4850821085239));
#134057=CARTESIAN_POINT('Ctrl Pts',(18.044801265282,15.7392303848602,5.51818545536712));
#134058=CARTESIAN_POINT('Ctrl Pts',(18.0476203722892,15.7376547832463,5.5513387005063));
#134059=CARTESIAN_POINT('Ctrl Pts',(18.0504920836694,15.7338953786096,5.58423131758289));
#134060=CARTESIAN_POINT('Ctrl Pts',(18.0533661966296,15.7301328300251,5.61715144238518));
#134061=CARTESIAN_POINT('Ctrl Pts',(18.0562930450686,15.7241829251285,5.64981048106769));
#134062=CARTESIAN_POINT('Ctrl Pts',(18.0592543812016,15.7160990512311,5.68190285989289));
#134063=CARTESIAN_POINT('Ctrl Pts',(18.0622171618623,15.7080112340529,5.71401089325004));
#134064=CARTESIAN_POINT('Ctrl Pts',(18.0652143040956,15.6977872225133,5.74555173553004));
#134065=CARTESIAN_POINT('Ctrl Pts',(18.0682035479844,15.6855151363698,5.7762250552271));
#134066=CARTESIAN_POINT('Ctrl Pts',(18.071198680356,15.6732188755617,5.80695879800219));
#134067=CARTESIAN_POINT('Ctrl Pts',(18.0741854168822,15.6588659589358,5.83682153768798));
#134068=CARTESIAN_POINT('Ctrl Pts',(18.0771017174444,15.6425845871123,5.865516948982));
#134069=CARTESIAN_POINT('Ctrl Pts',(18.078160626474,15.6366728193537,5.87593625573006));
#134070=CARTESIAN_POINT('Ctrl Pts',(18.0792101010587,15.6305072187241,5.88620172070509));
#134071=CARTESIAN_POINT('Ctrl Pts',(18.0802467831717,15.6240954635429,5.89629941435817));
#134072=CARTESIAN_POINT('Ctrl Pts',(18.0802480395688,15.6240876928765,5.89631165216296));
#134073=CARTESIAN_POINT('Ctrl Pts',(18.0802492959491,15.6240799218336,5.89632388974701));
#134074=CARTESIAN_POINT('Ctrl Pts',(18.0802505523126,15.6240721504142,5.8963361271103));
#134075=CARTESIAN_POINT('Ctrl Pts',(18.0828415305574,15.6080452773152,5.92157304428439));
#134076=CARTESIAN_POINT('Ctrl Pts',(18.085361043973,15.5904128634294,5.94587256850564));
#134077=CARTESIAN_POINT('Ctrl Pts',(18.0878498837288,15.5713228325143,5.96903414038106));
#134078=CARTESIAN_POINT('Ctrl Pts',(18.0881100761095,15.5693270910931,5.97145553553635));
#134079=CARTESIAN_POINT('Ctrl Pts',(18.0883699332463,15.5673154634936,5.9738644790996));
#134080=CARTESIAN_POINT('Ctrl Pts',(18.0886295017471,15.5652881502086,5.9762607327977));
#134081=CARTESIAN_POINT('Ctrl Pts',(18.0913687823211,15.5438934899064,6.00154889829641));
#134082=CARTESIAN_POINT('Ctrl Pts',(18.0940767605781,15.520746688581,6.02542590128219));
#134083=CARTESIAN_POINT('Ctrl Pts',(18.0968005095287,15.4960817934527,6.04766341424653));
#134084=CARTESIAN_POINT('Ctrl Pts',(18.0995214210206,15.4714425929172,6.06987776133736));
#134085=CARTESIAN_POINT('Ctrl Pts',(18.1022585547669,15.4452889468507,6.09045633377021));
#134086=CARTESIAN_POINT('Ctrl Pts',(18.1050412775618,15.4178759723684,6.1092093085127));
#134087=CARTESIAN_POINT('Ctrl Pts',(18.1078226284374,15.3904765128458,6.12795303779016));
#134088=CARTESIAN_POINT('Ctrl Pts',(18.110649750084,15.3618192081673,6.14487317653914));
#134089=CARTESIAN_POINT('Ctrl Pts',(18.1135291801814,15.332175245214,6.15981408324162));
#134090=CARTESIAN_POINT('Ctrl Pts',(18.1164108409359,15.3025083174676,6.1747665644705));
#134091=CARTESIAN_POINT('Ctrl Pts',(18.1193449331285,15.2718532680766,6.18773681972673));
#134092=CARTESIAN_POINT('Ctrl Pts',(18.1223131902413,15.2404961073911,6.19860068044639));
#134093=CARTESIAN_POINT('Ctrl Pts',(18.1252828002271,15.2091246547293,6.20946949269979));
#134094=CARTESIAN_POINT('Ctrl Pts',(18.128286442416,15.1770503451651,6.21822987810168));
#134095=CARTESIAN_POINT('Ctrl Pts',(18.1312818493294,15.1445740698856,6.22478953106497));
#134096=CARTESIAN_POINT('Ctrl Pts',(18.13428289449,15.1120366645917,6.23136153124717));
#134097=CARTESIAN_POINT('Ctrl Pts',(18.1372751985486,15.0790955465581,6.23572404130749));
#134098=CARTESIAN_POINT('Ctrl Pts',(18.1401968316883,15.0460705208212,6.23782052554615));
#134099=CARTESIAN_POINT('Ctrl Pts',(18.1411943618116,15.0347948210935,6.23853632594998));
#134100=CARTESIAN_POINT('Ctrl Pts',(18.1421835232276,15.0235095039505,6.23898831423258));
#134101=CARTESIAN_POINT('Ctrl Pts',(18.1431615371195,15.0122278243948,6.23917541247216));
#134102=CARTESIAN_POINT('Ctrl Pts',(18.1431627392938,15.0122139569584,6.23917564245324));
#134103=CARTESIAN_POINT('Ctrl Pts',(18.1431639414532,15.0122000894994,6.23917587203561));
#134104=CARTESIAN_POINT('Ctrl Pts',(18.1431651435976,15.0121862220177,6.23917610121923));
#134105=CARTESIAN_POINT('Ctrl Pts',(18.1457442399221,14.9824347454704,6.23966779475253));
#134106=CARTESIAN_POINT('Ctrl Pts',(18.1482544763774,14.9525758663653,6.23832151875025));
#134107=CARTESIAN_POINT('Ctrl Pts',(18.1507358914744,14.9228585657899,6.23514796266056));
#134108=CARTESIAN_POINT('Ctrl Pts',(18.1509738968701,14.9200082253161,6.23484357043135));
#134109=CARTESIAN_POINT('Ctrl Pts',(18.1512116371173,14.917159217899,6.23452239287036));
#134110=CARTESIAN_POINT('Ctrl Pts',(18.1514491475457,14.9143117821302,6.23418445593601));
#134111=CARTESIAN_POINT('Ctrl Pts',(18.1541598189073,14.8818144191945,6.23032763172769));
#134112=CARTESIAN_POINT('Ctrl Pts',(18.1568413521458,14.8495173610134,6.22428465180375));
#134113=CARTESIAN_POINT('Ctrl Pts',(18.1595386565067,14.8177334913946,6.21612134156257));
#134114=CARTESIAN_POINT('Ctrl Pts',(18.1622333190795,14.7859807514648,6.20796602661311));
#134115=CARTESIAN_POINT('Ctrl Pts',(18.1649441825578,14.7547402622896,6.19769508183801));
#134116=CARTESIAN_POINT('Ctrl Pts',(18.1676990754875,14.7243051351502,6.18541363159718));
#134117=CARTESIAN_POINT('Ctrl Pts',(18.170454816463,14.6938606390862,6.17312840072546));
#134118=CARTESIAN_POINT('Ctrl Pts',(18.1732548315693,14.6642220109734,6.15883174278628));
#134119=CARTESIAN_POINT('Ctrl Pts',(18.1761050002291,14.6356632829083,6.14266198635992));
#134120=CARTESIAN_POINT('Ctrl Pts',(18.1789554229838,14.6071020088089,6.12649078838641));
#134121=CARTESIAN_POINT('Ctrl Pts',(18.1818560391891,14.5796208401452,6.1084462818842));
#134122=CARTESIAN_POINT('Ctrl Pts',(18.1847889192762,14.5534743933048,6.08869663707073));
#134123=CARTESIAN_POINT('Ctrl Pts',(18.1877272800705,14.5272790862942,6.06891008586564));
#134124=CARTESIAN_POINT('Ctrl Pts',(18.1906978645508,14.5024235641472,6.04741190910945));
#134125=CARTESIAN_POINT('Ctrl Pts',(18.193659652731,14.4791437569311,6.02440097586502));
#134126=CARTESIAN_POINT('Ctrl Pts',(18.195783601337,14.4624494118007,6.0078994448261));
#134127=CARTESIAN_POINT('Ctrl Pts',(18.1979025422642,14.4465649110223,5.99062033918995));
#134128=CARTESIAN_POINT('Ctrl Pts',(18.1999951595719,14.4315705875013,5.97264794125123));
#134129=CARTESIAN_POINT('',(18.2,15.2587465130648,6.19222196005097));
#134130=CARTESIAN_POINT('Origin',(18.2,15.,5.5));
#134131=CARTESIAN_POINT('',(17.9231997159231,14.2612470260202,5.49963276901434));
#134132=CARTESIAN_POINT('Ctrl Pts',(17.9231997159231,14.2612470260202,5.49963276901434));
#134133=CARTESIAN_POINT('Ctrl Pts',(17.9262586431742,14.2612187711484,5.46303332832203));
#134134=CARTESIAN_POINT('Ctrl Pts',(17.9292580652234,14.2638801053733,5.42651463730436));
#134135=CARTESIAN_POINT('Ctrl Pts',(17.9322433460566,14.2691950817959,5.39045683330052));
#134136=CARTESIAN_POINT('Ctrl Pts',(17.9350059852405,14.2741136683366,5.3570882131299));
#134137=CARTESIAN_POINT('Ctrl Pts',(17.9377571858871,14.2813058278008,5.32411334875332));
#134138=CARTESIAN_POINT('Ctrl Pts',(17.9405516084341,14.2907103743296,5.29184004945994));
#134139=CARTESIAN_POINT('Ctrl Pts',(17.9407977040603,14.2915386018895,5.2889978458681));
#134140=CARTESIAN_POINT('Ctrl Pts',(17.9410441349047,14.2923839944149,5.28616105055996));
#134141=CARTESIAN_POINT('Ctrl Pts',(17.9412909383015,14.2932465145934,5.28332985490843));
#134142=CARTESIAN_POINT('Ctrl Pts',(17.9433011938874,14.3002718879439,5.26026928545832));
#134143=CARTESIAN_POINT('Ctrl Pts',(17.9453367038473,14.3084321983208,5.23758299047853));
#134144=CARTESIAN_POINT('Ctrl Pts',(17.9474199441049,14.3176914668121,5.21538482826282));
#134145=CARTESIAN_POINT('Ctrl Pts',(17.9474212056243,14.3176970738209,5.21537138602483));
#134146=CARTESIAN_POINT('Ctrl Pts',(17.9474224671611,14.3177026812326,5.21535794396523));
#134147=CARTESIAN_POINT('Ctrl Pts',(17.9474237287155,14.3177082890473,5.21534450208405));
#134148=CARTESIAN_POINT('Ctrl Pts',(17.9500793537949,14.3295129750619,5.18704877605385));
#134149=CARTESIAN_POINT('Ctrl Pts',(17.9528186941826,14.3431481780221,5.15945251371052));
#134150=CARTESIAN_POINT('Ctrl Pts',(17.9555881595096,14.3584881298957,5.13278509509163));
#134151=CARTESIAN_POINT('Ctrl Pts',(17.9558022896295,14.3596741876162,5.13072321784466));
#134152=CARTESIAN_POINT('Ctrl Pts',(17.9560165998394,14.3608704140577,5.12866690604059));
#134153=CARTESIAN_POINT('Ctrl Pts',(17.956231065369,14.3620767396463,5.12661627172541));
#134154=CARTESIAN_POINT('Ctrl Pts',(17.959214568465,14.3788583461549,5.0980891986902));
#134155=CARTESIAN_POINT('Ctrl Pts',(17.9622275004938,14.3975989598379,5.0706576239006));
#134156=CARTESIAN_POINT('Ctrl Pts',(17.9652194777493,14.4181104527675,5.04457671855219));
#134157=CARTESIAN_POINT('Ctrl Pts',(17.9682083269364,14.4386005012313,5.01852308040877));
#134158=CARTESIAN_POINT('Ctrl Pts',(17.9711760074106,14.4608575905549,4.99381705473338));
#134159=CARTESIAN_POINT('Ctrl Pts',(17.9740950538289,14.4846693294737,4.97068678059164));
#134160=CARTESIAN_POINT('Ctrl Pts',(17.9770126517411,14.5084692523937,4.9475679842883));
#134161=CARTESIAN_POINT('Ctrl Pts',(17.9798816370051,14.53382229895,4.92602338806137));
#134162=CARTESIAN_POINT('Ctrl Pts',(17.982699375066,14.5604923181853,4.9062561976417));
#134163=CARTESIAN_POINT('Ctrl Pts',(17.9855192979158,14.5871830165468,4.88647368034056));
#134164=CARTESIAN_POINT('Ctrl Pts',(17.988288046098,14.6151928189579,4.86847155315384));
#134165=CARTESIAN_POINT('Ctrl Pts',(17.9910268829266,14.6442600716981,4.85242704013227));
#134166=CARTESIAN_POINT('Ctrl Pts',(17.9937669623233,14.6733405118036,4.83637524796198));
#134167=CARTESIAN_POINT('Ctrl Pts',(17.9964774831177,14.7034794728911,4.8222833046908));
#134168=CARTESIAN_POINT('Ctrl Pts',(17.9991997379415,14.7343884256453,4.81029712951543));
#134169=CARTESIAN_POINT('Ctrl Pts',(18.0017724321862,14.7635992416821,4.79896947435947));
#134170=CARTESIAN_POINT('Ctrl Pts',(18.0043562329034,14.7934981500566,4.78952287559149));
#134171=CARTESIAN_POINT('Ctrl Pts',(18.0069960990905,14.8238172483661,4.78204727574495));
#134172=CARTESIAN_POINT('Ctrl Pts',(18.0071548466427,14.8256404781444,4.78159773281623));
#134173=CARTESIAN_POINT('Ctrl Pts',(18.0073137969379,14.8274652383969,4.78115530619246));
#134174=CARTESIAN_POINT('Ctrl Pts',(18.0074729597527,14.8292914752232,4.78072001126449));
#134175=CARTESIAN_POINT('Ctrl Pts',(18.0084596254331,14.8406124939122,4.77802157591165));
#134176=CARTESIAN_POINT('Ctrl Pts',(18.0094545130156,14.8519895282679,4.77559725406811));
#134177=CARTESIAN_POINT('Ctrl Pts',(18.0104600051911,14.863407987732,4.77345012771598));
#134178=CARTESIAN_POINT('Ctrl Pts',(18.0104612096985,14.8634216662258,4.77344755561293));
#134179=CARTESIAN_POINT('Ctrl Pts',(18.0104624142211,14.8634353447791,4.77344498390754));
#134180=CARTESIAN_POINT('Ctrl Pts',(18.0104636187589,14.8634490233919,4.77344241259979));
#134181=CARTESIAN_POINT('Ctrl Pts',(18.0131276391294,14.8937013768235,4.76775557053046));
#134182=CARTESIAN_POINT('Ctrl Pts',(18.0158740544306,14.9243765590572,4.76399716531421));
#134183=CARTESIAN_POINT('Ctrl Pts',(18.0186488845286,14.9552108250908,4.76218805642328));
#134184=CARTESIAN_POINT('Ctrl Pts',(18.0188507331611,14.9574537928449,4.76205645695853));
#134185=CARTESIAN_POINT('Ctrl Pts',(18.0190527321505,14.9596975819019,4.76193516207424));
#134186=CARTESIAN_POINT('Ctrl Pts',(18.0192548607188,14.9619420812788,4.76182417475526));
#134187=CARTESIAN_POINT('Ctrl Pts',(18.0222310129887,14.9949902147955,4.76018999130471));
#134188=CARTESIAN_POINT('Ctrl Pts',(18.0252346457585,15.0281975228741,4.76079239557386));
#134189=CARTESIAN_POINT('Ctrl Pts',(18.0282161966136,15.0612477944481,4.76361442227235));
#134190=CARTESIAN_POINT('Ctrl Pts',(18.0311947334598,15.0942646559551,4.7664335962227));
#134191=CARTESIAN_POINT('Ctrl Pts',(18.0341509866931,15.127124915222,4.77146767607796));
#134192=CARTESIAN_POINT('Ctrl Pts',(18.0370585499895,15.1595213805558,4.77866468462933));
#134193=CARTESIAN_POINT('Ctrl Pts',(18.0399647749284,15.1919029337276,4.78585838038234));
#134194=CARTESIAN_POINT('Ctrl Pts',(18.0428223355274,15.2238211150562,4.79521304283486));
#134195=CARTESIAN_POINT('Ctrl Pts',(18.0456297593615,15.2549763339614,4.80664310001928));
#134196=CARTESIAN_POINT('Ctrl Pts',(18.0484395231808,15.286157520714,4.81808268414624));
#134197=CARTESIAN_POINT('Ctrl Pts',(18.051199226476,15.3165743283291,4.83160133119134));
#134198=CARTESIAN_POINT('Ctrl Pts',(18.0539312956373,15.3459347183123,4.84707770639228));
#134199=CARTESIAN_POINT('Ctrl Pts',(18.0566646943394,15.3753093963082,4.86256161305463));
#134200=CARTESIAN_POINT('Ctrl Pts',(18.059370824189,15.4036263000318,4.88000550871002));
#134201=CARTESIAN_POINT('Ctrl Pts',(18.0620919965398,15.430604726856,4.89924808088519));
#134202=CARTESIAN_POINT('Ctrl Pts',(18.0646486288197,15.4559518596304,4.91732711992713));
#134203=CARTESIAN_POINT('Ctrl Pts',(18.0672191753305,15.4801174868315,4.9369943935669));
#134204=CARTESIAN_POINT('Ctrl Pts',(18.0698483381693,15.5028828544892,4.95807777932273));
#134205=CARTESIAN_POINT('Ctrl Pts',(18.0700229900163,15.5043951280735,4.95947832105024));
#134206=CARTESIAN_POINT('Ctrl Pts',(18.0701979005238,15.505901241427,4.96088511527658));
#134207=CARTESIAN_POINT('Ctrl Pts',(18.0703730827954,15.5074011384115,4.96229811330113));
#134208=CARTESIAN_POINT('Ctrl Pts',(18.0713722545889,15.5159559695936,4.97035730648927));
#134209=CARTESIAN_POINT('Ctrl Pts',(18.0723803185353,15.5243081081095,4.97861772452402));
#134210=CARTESIAN_POINT('Ctrl Pts',(18.0733997415326,15.5324466368762,4.98706847934758));
#134211=CARTESIAN_POINT('Ctrl Pts',(18.0734011530142,15.5324579053915,4.98708018016755));
#134212=CARTESIAN_POINT('Ctrl Pts',(18.0734025645176,15.5324691734975,4.98709188135243));
#134213=CARTESIAN_POINT('Ctrl Pts',(18.0734039760428,15.5324804411942,4.98710358290217));
#134214=CARTESIAN_POINT('Ctrl Pts',(18.0760361129181,15.55349184138,5.00892400905151));
#134215=CARTESIAN_POINT('Ctrl Pts',(18.0787525505888,15.5731714229398,5.03212001337143));
#134216=CARTESIAN_POINT('Ctrl Pts',(18.0814995687192,15.5913606132484,5.05649077204578));
#134217=CARTESIAN_POINT('Ctrl Pts',(18.0817129673223,15.5927736173208,5.05838398338004));
#134218=CARTESIAN_POINT('Ctrl Pts',(18.0819265504713,15.5941776246337,5.06028425816411));
#134219=CARTESIAN_POINT('Ctrl Pts',(18.0821402929818,15.5955725599306,5.06219148916643));
#134220=CARTESIAN_POINT('Ctrl Pts',(18.0851007307266,15.6148930923556,5.08860756631621));
#134221=CARTESIAN_POINT('Ctrl Pts',(18.0880911152758,15.632474380568,5.11636357154761));
#134222=CARTESIAN_POINT('Ctrl Pts',(18.0910604661353,15.6481590152578,5.14519179339049));
#134223=CARTESIAN_POINT('Ctrl Pts',(18.0940267905801,15.663827663892,5.1739906330025));
#134224=CARTESIAN_POINT('Ctrl Pts',(18.0969718624657,15.6776037789831,5.20385944642274));
#134225=CARTESIAN_POINT('Ctrl Pts',(18.0998672483404,15.6893644578681,5.23451869707503));
#134226=CARTESIAN_POINT('Ctrl Pts',(18.1027613698272,15.7011200009754,5.26516455912119));
#134227=CARTESIAN_POINT('Ctrl Pts',(18.105605811157,15.7108618521799,5.29660014770083));
#134228=CARTESIAN_POINT('Ctrl Pts',(18.1083967095201,15.7184995766532,5.32853413618579));
#134229=CARTESIAN_POINT('Ctrl Pts',(18.1111903662473,15.7261448498155,5.36049968639429));
#134230=CARTESIAN_POINT('Ctrl Pts',(18.1139305056239,15.7316816118874,5.39296458302346));
#134231=CARTESIAN_POINT('Ctrl Pts',(18.1166371406068,15.7350533739779,5.4256248738587));
#134232=CARTESIAN_POINT('Ctrl Pts',(18.1193452857107,15.7384270172859,5.45830338694855));
#134233=CARTESIAN_POINT('Ctrl Pts',(18.1220202337102,15.7396328222108,5.49117741633699));
#134234=CARTESIAN_POINT('Ctrl Pts',(18.1247024284304,15.7386532460656,5.52393168756679));
#134235=CARTESIAN_POINT('Ctrl Pts',(18.1273905478049,15.7376715061513,5.55675830914863));
#134236=CARTESIAN_POINT('Ctrl Pts',(18.1300865965977,15.7344940531765,5.5894643583877));
#134237=CARTESIAN_POINT('Ctrl Pts',(18.1328444052418,15.7291506235284,5.62172425242653));
#134238=CARTESIAN_POINT('Ctrl Pts',(18.1340515200849,15.7268117617459,5.63584466539077));
#134239=CARTESIAN_POINT('Ctrl Pts',(18.1352705770035,15.7240585966878,5.64987951970821));
#134240=CARTESIAN_POINT('Ctrl Pts',(18.1365062824139,15.7208970220618,5.66380134551847));
#134241=CARTESIAN_POINT('Ctrl Pts',(18.1365074611802,15.7208940061668,5.66381462585182));
#134242=CARTESIAN_POINT('Ctrl Pts',(18.1365086399617,15.7208909899003,5.66382790608253));
#134243=CARTESIAN_POINT('Ctrl Pts',(18.1365098187584,15.7208879732623,5.66384118621058));
#134244=CARTESIAN_POINT('Ctrl Pts',(18.1391948817415,15.7140166752005,5.69409066155985));
#134245=CARTESIAN_POINT('Ctrl Pts',(18.1419671514301,15.7051788823793,5.72394224967107));
#134246=CARTESIAN_POINT('Ctrl Pts',(18.1447739657266,15.694462611726,5.75314652340991));
#134247=CARTESIAN_POINT('Ctrl Pts',(18.1450263104535,15.6934991727144,5.75577211374216));
#134248=CARTESIAN_POINT('Ctrl Pts',(18.1452789343971,15.6925205776409,5.75839245032495));
#134249=CARTESIAN_POINT('Ctrl Pts',(18.145531799289,15.6915269069812,5.7610073396442));
#134250=CARTESIAN_POINT('Ctrl Pts',(18.1485916398169,15.6795028029924,5.79264931356071));
#134251=CARTESIAN_POINT('Ctrl Pts',(18.151686076699,15.6652670591775,5.82349779433561));
#134252=CARTESIAN_POINT('Ctrl Pts',(18.1547633469966,15.6489696089779,5.85325730727982));
#134253=CARTESIAN_POINT('Ctrl Pts',(18.1578363265298,15.6326948829827,5.88297532531258));
#134254=CARTESIAN_POINT('Ctrl Pts',(18.1608919108916,15.6143643562405,5.91160769582046));
#134255=CARTESIAN_POINT('Ctrl Pts',(18.1639015842225,15.5941559133991,5.93888206377511));
#134256=CARTESIAN_POINT('Ctrl Pts',(18.167046497236,15.5730394041011,5.96738200555838));
#134257=CARTESIAN_POINT('Ctrl Pts',(18.1701410440723,15.5498720918774,5.99439903315508));
#134258=CARTESIAN_POINT('Ctrl Pts',(18.1731820964075,15.524889787163,6.01964515254271));
#134259=CARTESIAN_POINT('Ctrl Pts',(18.1760889395079,15.5010100139497,6.04377709762875));
#134260=CARTESIAN_POINT('Ctrl Pts',(18.1789472914065,15.4754719407094,6.06629093511547));
#134261=CARTESIAN_POINT('Ctrl Pts',(18.1817788165681,15.4485123983593,6.08695637872067));
#134262=CARTESIAN_POINT('Ctrl Pts',(18.184610023612,15.4215558848736,6.10761950059419));
#134263=CARTESIAN_POINT('Ctrl Pts',(18.1874148502887,15.393177972699,6.12643415537824));
#134264=CARTESIAN_POINT('Ctrl Pts',(18.1902341341642,15.3636490638303,6.14319609094456));
#134265=CARTESIAN_POINT('Ctrl Pts',(18.1928660235342,15.3360829070351,6.15884388023692));
#134266=CARTESIAN_POINT('Ctrl Pts',(18.1955111969388,15.307513215976,6.17270255698526));
#134267=CARTESIAN_POINT('Ctrl Pts',(18.1982110692341,15.27819089864,6.18463367103899));
#134268=CARTESIAN_POINT('Ctrl Pts',(18.198405389526,15.2760804576117,6.18549239964232));
#134269=CARTESIAN_POINT('Ctrl Pts',(18.1985999931712,15.2739661059831,6.18634116207877));
#134270=CARTESIAN_POINT('Ctrl Pts',(18.1987948956111,15.2718479315203,6.18717991544739));
#134271=CARTESIAN_POINT('Ctrl Pts',(18.199195287804,15.2674965210454,6.18890298418335));
#134272=CARTESIAN_POINT('Ctrl Pts',(18.1995969446575,15.2631290938655,6.19058378968675));
#134273=CARTESIAN_POINT('Ctrl Pts',(18.2,15.2587465130648,6.19222196005096));
#134274=CARTESIAN_POINT('Ctrl Pts',(17.923341485608,14.2610000854617,5.49964459555407));
#134275=CARTESIAN_POINT('Ctrl Pts',(17.9225815974421,14.2609956726983,5.50882014690639));
#134276=CARTESIAN_POINT('Ctrl Pts',(17.9218174632575,14.2611621479354,5.5179946088016));
#134277=CARTESIAN_POINT('Ctrl Pts',(17.9203821612323,14.2617915619612,5.5351068011193));
#134278=CARTESIAN_POINT('Ctrl Pts',(17.9197123156157,14.2622118728923,5.54304480225922));
#134279=CARTESIAN_POINT('Ctrl Pts',(17.9183512131026,14.2633194823334,5.5590641664964));
#134280=CARTESIAN_POINT('Ctrl Pts',(17.9176598927818,14.2640119385344,5.5671440470472));
#134281=CARTESIAN_POINT('Ctrl Pts',(17.9162760949469,14.2656539206357,5.5831939763794));
#134282=CARTESIAN_POINT('Ctrl Pts',(17.9155837976166,14.2666006122747,5.59116319934));
#134283=CARTESIAN_POINT('Ctrl Pts',(17.9137274759009,14.2694695281316,5.61236051175744));
#134284=CARTESIAN_POINT('Ctrl Pts',(17.9125565197848,14.2716210926636,5.62555385800917));
#134285=CARTESIAN_POINT('Ctrl Pts',(17.9079979409858,14.2812957517057,5.67619215007037));
#134286=CARTESIAN_POINT('Ctrl Pts',(17.9045372590169,14.2913553792326,5.71307023382596));
#134287=CARTESIAN_POINT('Ctrl Pts',(17.9010383741602,14.3042076641721,5.74898599439144));
#134288=CARTESIAN_POINT('Origin',(16.125,15.,5.5));
#134289=CARTESIAN_POINT('',(18.1999858262452,15.63646577564,4.77232089562845));
#134290=CARTESIAN_POINT('Ctrl Pts',(18.0542644868187,14.0332501467026,5.49946741256401));
#134291=CARTESIAN_POINT('Ctrl Pts',(18.057199765697,14.0332748136958,5.45469201895388));
#134292=CARTESIAN_POINT('Ctrl Pts',(18.0601350445753,14.0364143245651,5.41002345185869));
#134293=CARTESIAN_POINT('Ctrl Pts',(18.0630703234536,14.0425996866789,5.3658724392504));
#134294=CARTESIAN_POINT('Ctrl Pts',(18.0660254309054,14.0488268325252,5.32142317504943));
#134295=CARTESIAN_POINT('Ctrl Pts',(18.0689805383573,14.0581409715527,5.27749883510395));
#134296=CARTESIAN_POINT('Ctrl Pts',(18.0719356458091,14.0704217023092,5.23450093980893));
#134297=CARTESIAN_POINT('Ctrl Pts',(18.0744302810105,14.0807888188164,5.19820308433721));
#134298=CARTESIAN_POINT('Ctrl Pts',(18.0769249162119,14.0932691063426,5.16256523878398));
#134299=CARTESIAN_POINT('Ctrl Pts',(18.0794195514133,14.1077639963729,5.12781660927507));
#134300=CARTESIAN_POINT('Ctrl Pts',(18.0820953694329,14.123311635528,5.09054422213671));
#134301=CARTESIAN_POINT('Ctrl Pts',(18.0847711874525,14.1412341479741,5.05416295996415));
#134302=CARTESIAN_POINT('Ctrl Pts',(18.0874470054721,14.1614073125235,5.01899286178791));
#134303=CARTESIAN_POINT('Ctrl Pts',(18.0901187885368,14.181550057288,4.98387579777091));
#134304=CARTESIAN_POINT('Ctrl Pts',(18.0927905716015,14.2039364576989,4.94996678884093));
#134305=CARTESIAN_POINT('Ctrl Pts',(18.0954623546662,14.2283949697251,4.91756439003576));
#134306=CARTESIAN_POINT('Ctrl Pts',(18.0981313920739,14.2528283469689,4.88519528954568));
#134307=CARTESIAN_POINT('Ctrl Pts',(18.1008004294816,14.2793292742131,4.85433020017197));
#134308=CARTESIAN_POINT('Ctrl Pts',(18.1034694668893,14.3076828035228,4.8252389593627));
#134309=CARTESIAN_POINT('Ctrl Pts',(18.1061370431678,14.3360208110682,4.79616364416803));
#134310=CARTESIAN_POINT('Ctrl Pts',(18.1088046194463,14.366209006091,4.76886067145898));
#134311=CARTESIAN_POINT('Ctrl Pts',(18.1114721957247,14.3979940771723,4.7435646548578));
#134312=CARTESIAN_POINT('Ctrl Pts',(18.1141415978985,14.4298009044114,4.71825132370897));
#134313=CARTESIAN_POINT('Ctrl Pts',(18.1168110000722,14.4632063406363,4.69494806480106));
#134314=CARTESIAN_POINT('Ctrl Pts',(18.119480402246,14.4979240827197,4.67384908413343));
#134315=CARTESIAN_POINT('Ctrl Pts',(18.1221505771933,14.5326518753514,4.65274399545559));
#134316=CARTESIAN_POINT('Ctrl Pts',(18.1248207521407,14.5686922188595,4.63384473813471));
#134317=CARTESIAN_POINT('Ctrl Pts',(18.127490927088,14.605733371958,4.61729994419824));
#134318=CARTESIAN_POINT('Ctrl Pts',(18.1301663774595,14.6428477067007,4.60072246296345));
#134319=CARTESIAN_POINT('Ctrl Pts',(18.132841827831,14.6809662559188,4.5865089510119));
#134320=CARTESIAN_POINT('Ctrl Pts',(18.1355172782025,14.7197581761722,4.57475944604785));
#134321=CARTESIAN_POINT('Ctrl Pts',(18.137824033639,14.7532043106584,4.56462910136252));
#134322=CARTESIAN_POINT('Ctrl Pts',(18.1401307890754,14.7871505220092,4.55632967343333));
#134323=CARTESIAN_POINT('Ctrl Pts',(18.1424375445119,14.8213793569691,4.54989462248485));
#134324=CARTESIAN_POINT('Ctrl Pts',(18.1450794771382,14.8605817251136,4.54252454294207));
#134325=CARTESIAN_POINT('Ctrl Pts',(18.1477214097645,14.9003400967497,4.53756637294437));
#134326=CARTESIAN_POINT('Ctrl Pts',(18.1503633423907,14.9403264071641,4.53509346316959));
#134327=CARTESIAN_POINT('Ctrl Pts',(18.153001353725,14.9802533678442,4.53262422381442));
#134328=CARTESIAN_POINT('Ctrl Pts',(18.1556393650593,15.0204070062996,4.5326329975251));
#134329=CARTESIAN_POINT('Ctrl Pts',(18.1582773763936,15.0604508144803,4.53514184382954));
#134330=CARTESIAN_POINT('Ctrl Pts',(18.1609128218753,15.1004556741906,4.53764824991336));
#134331=CARTESIAN_POINT('Ctrl Pts',(18.1635482673571,15.1403503188792,4.54264988585039));
#134332=CARTESIAN_POINT('Ctrl Pts',(18.1661837128388,15.1797982127067,4.55011676232945));
#134333=CARTESIAN_POINT('Ctrl Pts',(18.1688179428531,15.2192279131654,4.55758019508506));
#134334=CARTESIAN_POINT('Ctrl Pts',(18.1714521728674,15.2582106825453,4.56750650590994));
#134335=CARTESIAN_POINT('Ctrl Pts',(18.1740864028817,15.2964183852975,4.57981431039294));
#134336=CARTESIAN_POINT('Ctrl Pts',(18.1767224548429,15.3346525141424,4.59213062748356));
#134337=CARTESIAN_POINT('Ctrl Pts',(18.1793585068041,15.3721099340013,4.60683154494961));
#134338=CARTESIAN_POINT('Ctrl Pts',(18.1819945587653,15.4084785178229,4.62378606323728));
#134339=CARTESIAN_POINT('Ctrl Pts',(18.1846317349793,15.4448626125227,4.64074781247653));
#134340=CARTESIAN_POINT('Ctrl Pts',(18.1872689111933,15.4801564184663,4.65996479166206));
#134341=CARTESIAN_POINT('Ctrl Pts',(18.1899060874073,15.5140723338457,4.68125999360335));
#134342=CARTESIAN_POINT('Ctrl Pts',(18.192547721285,15.5480455778733,4.70259119118638));
#134343=CARTESIAN_POINT('Ctrl Pts',(18.1951893551628,15.5806358017996,4.72600726524789));
#134344=CARTESIAN_POINT('Ctrl Pts',(18.1978309890405,15.6115864189532,4.75128936520711));
#134345=CARTESIAN_POINT('Ctrl Pts',(18.1985492681088,15.6200021122244,4.75816374827521));
#134346=CARTESIAN_POINT('Ctrl Pts',(18.199267547177,15.6282967904242,4.7651758787105));
#134347=CARTESIAN_POINT('Ctrl Pts',(18.1999858262452,15.63646577564,4.77232089562845));
#134348=CARTESIAN_POINT('',(18.2,14.8153312661022,4.55105162352181));
#134349=CARTESIAN_POINT('Origin',(18.2,15.,5.5));
#134350=CARTESIAN_POINT('Ctrl Pts',(18.2,14.8153312661022,4.55105162352181));
#134351=CARTESIAN_POINT('Ctrl Pts',(18.1972671579687,14.7745953964148,4.55897896885046));
#134352=CARTESIAN_POINT('Ctrl Pts',(18.1945343159374,14.7343346850379,4.56954063396579));
#134353=CARTESIAN_POINT('Ctrl Pts',(18.1918014739061,14.6948998275967,4.58265630906431));
#134354=CARTESIAN_POINT('Ctrl Pts',(18.1890702629705,14.6554885068346,4.59576415607738));
#134355=CARTESIAN_POINT('Ctrl Pts',(18.1863390520349,14.6169025808847,4.61142281906072));
#134356=CARTESIAN_POINT('Ctrl Pts',(18.1836078410993,14.5794777686934,4.62950208760912));
#134357=CARTESIAN_POINT('Ctrl Pts',(18.1808772139826,14.5420609563654,4.64757749156423));
#134358=CARTESIAN_POINT('Ctrl Pts',(18.178146586866,14.5058052572839,4.6680722364678));
#134359=CARTESIAN_POINT('Ctrl Pts',(18.1754159597493,14.4710241480299,4.69080897772373));
#134360=CARTESIAN_POINT('Ctrl Pts',(18.1726848705559,14.4362371531159,4.71354956649145));
#134361=CARTESIAN_POINT('Ctrl Pts',(18.1699537813624,14.402925699129,4.73853260300311));
#134362=CARTESIAN_POINT('Ctrl Pts',(18.167222692169,14.3713742597232,4.76553744740701));
#134363=CARTESIAN_POINT('Ctrl Pts',(18.1644876254829,14.3397768695595,4.79258162101713));
#134364=CARTESIAN_POINT('Ctrl Pts',(18.1617525587968,14.3099450268696,4.82165312352018));
#134365=CARTESIAN_POINT('Ctrl Pts',(18.1590174921107,14.2821287646877,4.85249212204697));
#134366=CARTESIAN_POINT('Ctrl Pts',(18.1562804141889,14.2542920477726,4.883353798081));
#134367=CARTESIAN_POINT('Ctrl Pts',(18.1535433362672,14.2284742061419,4.91598513157478));
#134368=CARTESIAN_POINT('Ctrl Pts',(18.1508062583454,14.2048846110525,4.95009357090598));
#134369=CARTESIAN_POINT('Ctrl Pts',(18.1480629990315,14.1812417414341,4.98427904042942));
#134370=CARTESIAN_POINT('Ctrl Pts',(18.1453197397175,14.1598374571409,5.01994781177225));
#134371=CARTESIAN_POINT('Ctrl Pts',(18.1425764804036,14.1408366890334,5.05678000091504));
#134372=CARTESIAN_POINT('Ctrl Pts',(18.140738797881,14.12810826074,5.08145352336108));
#134373=CARTESIAN_POINT('Ctrl Pts',(18.1389011153584,14.1164574565062,5.1066486149651));
#134374=CARTESIAN_POINT('Ctrl Pts',(18.1370634328358,14.1059216241396,5.13226446959972));
#134375=CARTESIAN_POINT('Ctrl Pts',(18.1341448700766,14.0891888710095,5.17294694791745));
#134376=CARTESIAN_POINT('Ctrl Pts',(18.1312263073175,14.0752047801112,5.21485093037565));
#134377=CARTESIAN_POINT('Ctrl Pts',(18.1283077445583,14.0641310269153,5.25760604851314));
#134378=CARTESIAN_POINT('Ctrl Pts',(18.1254081725836,14.0531293294803,5.30008296354149));
#134379=CARTESIAN_POINT('Ctrl Pts',(18.1225086006089,14.045000411785,5.34339961698888));
#134380=CARTESIAN_POINT('Ctrl Pts',(18.1196090286342,14.0398567688201,5.38717031366046));
#134381=CARTESIAN_POINT('Ctrl Pts',(18.117151479958,14.0354972450457,5.42426841593273));
#134382=CARTESIAN_POINT('Ctrl Pts',(18.1146939312818,14.0332814876152,5.46169218001169));
#134383=CARTESIAN_POINT('Ctrl Pts',(18.1122363826056,14.0332503335345,5.49919695023161));
#134384=CARTESIAN_POINT('Ctrl Pts',(13.8510043077487,14.6757204956766,6.16261990718442));
#134385=CARTESIAN_POINT('Ctrl Pts',(13.8720142555048,14.4570381267508,6.05560288018805));
#134386=CARTESIAN_POINT('Ctrl Pts',(13.9140302009604,14.1375601906771,5.61006110330474));
#134387=CARTESIAN_POINT('Ctrl Pts',(13.9770521441157,14.4351930444452,4.83797560757758));
#134388=CARTESIAN_POINT('Ctrl Pts',(14.0400701372144,15.2432695205923,4.66524858954316));
#134389=CARTESIAN_POINT('Ctrl Pts',(14.103088130313,15.8314236186915,5.24489867692567));
#134390=CARTESIAN_POINT('Ctrl Pts',(14.1661061234117,15.6694783302998,6.05523004482602));
#134391=CARTESIAN_POINT('Ctrl Pts',(14.2291241165104,14.9032753408017,6.36426544000879));
#134392=CARTESIAN_POINT('Ctrl Pts',(14.292142109609,14.2244118963622,5.89348843559075));
#134393=CARTESIAN_POINT('Ctrl Pts',(14.3551601027077,14.2454329761124,5.06755325204506));
#134394=CARTESIAN_POINT('Ctrl Pts',(14.4181780958064,14.9474094818699,4.63190231135811));
#134395=CARTESIAN_POINT('Ctrl Pts',(14.481196088905,15.6968379606444,4.97962926523951));
#134396=CARTESIAN_POINT('Ctrl Pts',(14.5442140820037,15.817424801238,5.79696136639344));
#134397=CARTESIAN_POINT('Ctrl Pts',(14.6072320751024,15.2003436632176,6.34630312821531));
#134398=CARTESIAN_POINT('Ctrl Pts',(14.670250068201,14.4024679858008,6.13192048352086));
#134399=CARTESIAN_POINT('Ctrl Pts',(14.7332680612997,14.1438207552115,5.34727465160558));
#134400=CARTESIAN_POINT('Ctrl Pts',(14.7962860543983,14.6578129302989,4.7004528760265));
#134401=CARTESIAN_POINT('Ctrl Pts',(14.859304047497,15.480603779217,4.77516359700903));
#134402=CARTESIAN_POINT('Ctrl Pts',(14.9223220405957,15.8696849336051,5.50398631841823));
#134403=CARTESIAN_POINT('Ctrl Pts',(14.9853400336943,15.4739390057675,6.22921159789105));
#134404=CARTESIAN_POINT('Ctrl Pts',(15.048358026793,14.6504978046365,6.29637678311753));
#134405=CARTESIAN_POINT('Ctrl Pts',(15.1113760198917,14.1424567647499,5.64487014355418));
#134406=CARTESIAN_POINT('Ctrl Pts',(15.1743940129904,14.4082857825444,4.86262880555434));
#134407=CARTESIAN_POINT('Ctrl Pts',(15.237412006089,15.2080936039251,4.65556835048665));
#134408=CARTESIAN_POINT('Ctrl Pts',(15.3004299991877,15.8201121680078,5.21054570412811));
#134409=CARTESIAN_POINT('Ctrl Pts',(15.3634479922863,15.6920394790885,6.02673438894278));
#134410=CARTESIAN_POINT('Ctrl Pts',(15.426465985385,14.9394517732209,6.36758381144615));
#134411=CARTESIAN_POINT('Ctrl Pts',(15.4894839784837,14.2415044136345,5.92550229484266));
#134412=CARTESIAN_POINT('Ctrl Pts',(15.5525019715823,14.2280438479273,5.09943607663833));
#134413=CARTESIAN_POINT('Ctrl Pts',(15.615519964681,14.9112172520766,4.63484950374971));
#134414=CARTESIAN_POINT('Ctrl Pts',(15.6785379577797,15.6745105930848,4.95099798062628));
#134415=CARTESIAN_POINT('Ctrl Pts',(15.7415559508783,15.8291074544448,5.76258062846155));
#134416=CARTESIAN_POINT('Ctrl Pts',(15.804573943977,15.2354954753046,6.33720346307143));
#134417=CARTESIAN_POINT('Ctrl Pts',(15.8675919370757,14.429366052762,6.15631140148769));
#134418=CARTESIAN_POINT('Ctrl Pts',(15.9306099301743,14.1381920340439,5.38314629968156));
#134419=CARTESIAN_POINT('Ctrl Pts',(15.993627923273,14.624736675904,4.71543311626554));
#134420=CARTESIAN_POINT('Ctrl Pts',(16.0566459163717,15.4499290227168,4.75573416578379));
#134421=CARTESIAN_POINT('Ctrl Pts',(16.1196639094703,15.8690933322795,5.46768069848062));
#134422=CARTESIAN_POINT('Ctrl Pts',(16.182681902569,15.503964470976,6.20879303711113));
#134423=CARTESIAN_POINT('Ctrl Pts',(16.2456998956676,14.6840445322729,6.31027149763592));
#134424=CARTESIAN_POINT('Ctrl Pts',(16.3087178887663,14.1492512956584,5.68053919109209));
#134425=CARTESIAN_POINT('Ctrl Pts',(16.371735881865,14.3821965448323,4.88788346841236));
#134426=CARTESIAN_POINT('Ctrl Pts',(16.4347538749637,15.1726642289878,4.64761814805864));
#134427=CARTESIAN_POINT('Ctrl Pts',(16.4977718680623,15.8073150743269,5.17656510981916));
#134428=CARTESIAN_POINT('Ctrl Pts',(16.560789861161,15.713423108475,5.99738840531947));
#134429=CARTESIAN_POINT('Ctrl Pts',(16.6238078542597,14.9757189636257,6.36935504192598));
#134430=CARTESIAN_POINT('Ctrl Pts',(16.6868258473583,14.2599266785039,5.95679233347536));
#134431=CARTESIAN_POINT('Ctrl Pts',(16.749843840457,14.2119964400548,5.13200795249525));
#134432=CARTESIAN_POINT('Ctrl Pts',(16.8128618335556,14.8751817842497,4.63930947971334));
#134433=CARTESIAN_POINT('Ctrl Pts',(16.8758798266543,15.6510064380201,4.92332125728043));
#134434=CARTESIAN_POINT('Ctrl Pts',(16.938897819753,15.8393453960448,5.72774341912552));
#134435=CARTESIAN_POINT('Ctrl Pts',(17.0019158128517,15.2702365143165,6.32664381179715));
#134436=CARTESIAN_POINT('Ctrl Pts',(17.0649338059503,14.4572589533998,6.17955860087412));
#134437=CARTESIAN_POINT('Ctrl Pts',(17.127951799049,14.1340654717869,5.41922149219832));
#134438=CARTESIAN_POINT('Ctrl Pts',(17.1909697921477,14.5923146135604,4.73178100167847));
#134439=CARTESIAN_POINT('Ctrl Pts',(17.2539877852463,15.4184699182281,4.73760212378108));
#134440=CARTESIAN_POINT('Ctrl Pts',(17.317005778345,15.866986886601,5.43143127746081));
#134441=CARTESIAN_POINT('Ctrl Pts',(17.3800237714436,15.5331112858198,6.18713925984319));
#134442=CARTESIAN_POINT('Ctrl Pts',(17.4430417645423,14.7181423454594,6.32275320163177));
#134443=CARTESIAN_POINT('Ctrl Pts',(17.506059757641,14.1575281433043,5.71589471852043));
#134444=CARTESIAN_POINT('Ctrl Pts',(17.5690777507396,14.3571854776964,4.91420282101584));
#134445=CARTESIAN_POINT('Ctrl Pts',(17.6320957438383,15.1369314259542,4.64115825426989));
#134446=CARTESIAN_POINT('Ctrl Pts',(17.695113736937,15.7931155014792,5.1431395445431));
#134447=CARTESIAN_POINT('Ctrl Pts',(17.7581317300356,15.7335538507685,5.96719246940726));
#134448=CARTESIAN_POINT('Ctrl Pts',(17.8211497231343,15.0120465880597,6.36957765047564));
#134449=CARTESIAN_POINT('Ctrl Pts',(17.884167716233,14.279603718542,5.98735083367125));
#134450=CARTESIAN_POINT('Ctrl Pts',(17.9471857093316,14.1973913188042,5.16509520215214));
#134451=CARTESIAN_POINT('Ctrl Pts',(18.0102037024303,14.8392299862402,4.6455159570919));
#134452=CARTESIAN_POINT('Ctrl Pts',(18.073221695529,15.6266295424263,4.89616342462223));
#134453=CARTESIAN_POINT('Ctrl Pts',(18.1362428391242,15.8476078068145,5.69356706237978));
#134454=CARTESIAN_POINT('Ctrl Pts',(18.1782579850199,15.4862513157781,6.10585161173504));
#134455=CARTESIAN_POINT('Ctrl Pts',(18.1992671332161,15.2581937444145,6.19105595229305));
#134456=CARTESIAN_POINT('Ctrl Pts',(13.8957032291166,14.6416883768802,6.23215979205983));
#134457=CARTESIAN_POINT('Ctrl Pts',(13.9167131768727,14.4000559779379,6.11391166310539));
#134458=CARTESIAN_POINT('Ctrl Pts',(13.9587291223284,14.0470498326241,5.62161167154166));
#134459=CARTESIAN_POINT('Ctrl Pts',(14.0217510654837,14.3759183226323,4.76849822011212));
#134460=CARTESIAN_POINT('Ctrl Pts',(14.0847690585823,15.2687998952042,4.57764404227048));
#134461=CARTESIAN_POINT('Ctrl Pts',(14.147787051681,15.9186789246364,5.21812659168372));
#134462=CARTESIAN_POINT('Ctrl Pts',(14.2108050447797,15.7397379852103,6.11349969983931));
#134463=CARTESIAN_POINT('Ctrl Pts',(14.2738230378784,14.8931243906229,6.45496739228697));
#134464=CARTESIAN_POINT('Ctrl Pts',(14.336841030977,14.1430163529249,5.93478381505961));
#134465=CARTESIAN_POINT('Ctrl Pts',(14.3998590240757,14.1662435291866,5.02216931965564));
#134466=CARTESIAN_POINT('Ctrl Pts',(14.4628770171744,14.941890271631,4.54079817658305));
#134467=CARTESIAN_POINT('Ctrl Pts',(14.525895010273,15.7699689231081,4.92501798568779));
#134468=CARTESIAN_POINT('Ctrl Pts',(14.5889130033717,15.9032109751155,5.82812653213556));
#134469=CARTESIAN_POINT('Ctrl Pts',(14.6519309964703,15.2213691034807,6.43511999210321));
#134470=CARTESIAN_POINT('Ctrl Pts',(14.714948989569,14.3397588715313,6.19823855998974));
#134471=CARTESIAN_POINT('Ctrl Pts',(14.7779669826677,14.0539674238071,5.33124660441028));
#134472=CARTESIAN_POINT('Ctrl Pts',(14.8409849757663,14.6219014685772,4.61654290841046));
#134473=CARTESIAN_POINT('Ctrl Pts',(14.904002968865,15.531041641278,4.69909428567233));
#134474=CARTESIAN_POINT('Ctrl Pts',(14.9670209619637,15.96095564477,5.50440467005673));
#134475=CARTESIAN_POINT('Ctrl Pts',(15.0300389550623,15.5236774207196,6.30574007223561));
#134476=CARTESIAN_POINT('Ctrl Pts',(15.093056948161,14.6138186433772,6.37995403338573));
#134477=CARTESIAN_POINT('Ctrl Pts',(15.1560749412596,14.0524602868168,5.66007381159285));
#134478=CARTESIAN_POINT('Ctrl Pts',(15.2190929343583,14.3461872278302,4.79573869403778));
#134479=CARTESIAN_POINT('Ctrl Pts',(15.282110927457,15.2299323762038,4.56694789242973));
#134480=CARTESIAN_POINT('Ctrl Pts',(15.3451289205557,15.9061803726147,5.18016838193572));
#134481=CARTESIAN_POINT('Ctrl Pts',(15.4081469136543,15.764666855935,6.08201351407901));
#134482=CARTESIAN_POINT('Ctrl Pts',(15.471164906753,14.9330974263714,6.45863401641825));
#134483=CARTESIAN_POINT('Ctrl Pts',(15.5341828998516,14.1619026763754,5.9701574286181));
#134484=CARTESIAN_POINT('Ctrl Pts',(15.5972008929503,14.1470294664366,5.05739814687831));
#134485=CARTESIAN_POINT('Ctrl Pts',(15.660218886049,14.9018997806234,4.54405466758972));
#134486=CARTESIAN_POINT('Ctrl Pts',(15.7232368791476,15.7452983682207,4.8933819373869));
#134487=CARTESIAN_POINT('Ctrl Pts',(15.7862548722463,15.9161196862029,5.79013764338932));
#134488=CARTESIAN_POINT('Ctrl Pts',(15.849272865345,15.2602099882008,6.42506534558968));
#134489=CARTESIAN_POINT('Ctrl Pts',(15.9122908584437,14.3694798064137,6.22518922843951));
#134490=CARTESIAN_POINT('Ctrl Pts',(15.9753088515423,14.0477479859742,5.37088286965281));
#134491=CARTESIAN_POINT('Ctrl Pts',(16.038326844641,14.5853539648314,4.63309527796577));
#134492=CARTESIAN_POINT('Ctrl Pts',(16.1013448377396,15.4971476651128,4.67762579646536));
#134493=CARTESIAN_POINT('Ctrl Pts',(16.1643628308383,15.9603019567375,5.46428888896427));
#134494=CARTESIAN_POINT('Ctrl Pts',(16.227380823937,15.5568539645045,6.28317864742375));
#134495=CARTESIAN_POINT('Ctrl Pts',(16.2903988170356,14.6508859950583,6.39530695469434));
#134496=CARTESIAN_POINT('Ctrl Pts',(16.3534168101343,14.0599678824732,5.6994862140051));
#134497=CARTESIAN_POINT('Ctrl Pts',(16.416434803233,14.3173600062946,4.82364375470104));
#134498=CARTESIAN_POINT('Ctrl Pts',(16.4794527963316,15.1907847992811,4.55816334114562));
#134499=CARTESIAN_POINT('Ctrl Pts',(16.5424707894303,15.8920402640143,5.14262163063297));
#134500=CARTESIAN_POINT('Ctrl Pts',(16.605488782529,15.7882946302824,6.04958776134433));
#134501=CARTESIAN_POINT('Ctrl Pts',(16.6685067756276,14.973170744872,6.46059113199196));
#134502=CARTESIAN_POINT('Ctrl Pts',(16.7315247687263,14.1822583002706,6.00473125884937));
#134503=CARTESIAN_POINT('Ctrl Pts',(16.794542761825,14.1292979333455,5.09338833913761));
#134504=CARTESIAN_POINT('Ctrl Pts',(16.8575607549236,14.8620825032599,4.54898270406844));
#134505=CARTESIAN_POINT('Ctrl Pts',(16.9205787480223,15.7193275256635,4.86280062857004));
#134506=CARTESIAN_POINT('Ctrl Pts',(16.9835967411209,15.9274320677232,5.75164437799412));
#134507=CARTESIAN_POINT('Ctrl Pts',(17.0466147342196,15.2985969904974,6.41339749197198));
#134508=CARTESIAN_POINT('Ctrl Pts',(17.1096327273182,14.4002999796526,6.25087614862437));
#134509=CARTESIAN_POINT('Ctrl Pts',(17.172650720417,14.0431883539269,5.41074404068799));
#134510=CARTESIAN_POINT('Ctrl Pts',(17.2356687135156,14.5495293085446,4.65115882277445));
#134511=CARTESIAN_POINT('Ctrl Pts',(17.2986867066143,15.4623870260932,4.65759085341827));
#134512=CARTESIAN_POINT('Ctrl Pts',(17.361704699713,15.9579744461793,5.42423520469007));
#134513=CARTESIAN_POINT('Ctrl Pts',(17.4247226928116,15.5890596463198,6.25925237402038));
#134514=CARTESIAN_POINT('Ctrl Pts',(17.4877406859102,14.6885622669929,6.40909857444962));
#134515=CARTESIAN_POINT('Ctrl Pts',(17.550758679009,14.0691133593682,5.73855219335379));
#134516=CARTESIAN_POINT('Ctrl Pts',(17.6137766721076,14.289724105962,4.85272524096548));
#134517=CARTESIAN_POINT('Ctrl Pts',(17.6767946652063,15.1513019504334,4.55102550172695));
#134518=CARTESIAN_POINT('Ctrl Pts',(17.739812658305,15.876350490449,5.10568815692254));
#134519=CARTESIAN_POINT('Ctrl Pts',(17.8028306514036,15.8105380309588,6.01622285648888));
#134520=CARTESIAN_POINT('Ctrl Pts',(17.8658486445023,15.0133108397638,6.46083710261201));
#134521=CARTESIAN_POINT('Ctrl Pts',(17.9288666376009,14.20400038406,6.03849677797505));
#134522=CARTESIAN_POINT('Ctrl Pts',(17.9918846306996,14.1131600503421,5.12994799206374));
#134523=CARTESIAN_POINT('Ctrl Pts',(18.0549026237983,14.8223576765992,4.55584053181802));
#134524=CARTESIAN_POINT('Ctrl Pts',(18.1179206168969,15.6923923511911,4.83279266639408));
#134525=CARTESIAN_POINT('Ctrl Pts',(18.1809417604922,15.936561592637,5.71388131959968));
#134526=CARTESIAN_POINT('Ctrl Pts',(18.2229569063879,15.5372818691211,6.16943384172064));
#134527=CARTESIAN_POINT('Ctrl Pts',(18.243966054584,15.2852903695951,6.26358011108135));
#134528=CARTESIAN_POINT('Ctrl Pts',(13.9404021504847,14.6076562580839,6.30169967693524));
#134529=CARTESIAN_POINT('Ctrl Pts',(13.9614120982408,14.3430738291251,6.17222044602273));
#134530=CARTESIAN_POINT('Ctrl Pts',(14.0034280436965,13.956539474571,5.63316223977858));
#134531=CARTESIAN_POINT('Ctrl Pts',(14.0664499868517,14.3166436008192,4.69902083264669));
#134532=CARTESIAN_POINT('Ctrl Pts',(14.1294679799503,15.2943302698161,4.49003949499779));
#134533=CARTESIAN_POINT('Ctrl Pts',(14.192485973049,16.0059342305812,5.19135450644176));
#134534=CARTESIAN_POINT('Ctrl Pts',(14.2555039661476,15.8099976401209,6.1717693548526));
#134535=CARTESIAN_POINT('Ctrl Pts',(14.3185219592463,14.8829734404442,6.54566934456515));
#134536=CARTESIAN_POINT('Ctrl Pts',(14.381539952345,14.0616208094874,5.97607919452845));
#134537=CARTESIAN_POINT('Ctrl Pts',(14.4445579454437,14.0870540822609,4.97678538726625));
#134538=CARTESIAN_POINT('Ctrl Pts',(14.5075759385423,14.9363710613919,4.44969404180798));
#134539=CARTESIAN_POINT('Ctrl Pts',(14.570593931641,15.8430998855718,4.87040670613608));
#134540=CARTESIAN_POINT('Ctrl Pts',(14.6336119247396,15.988997148993,5.85929169787771));
#134541=CARTESIAN_POINT('Ctrl Pts',(14.6966299178383,15.242394543744,6.52393685599109));
#134542=CARTESIAN_POINT('Ctrl Pts',(14.759647910937,14.277049757262,6.26455663645863));
#134543=CARTESIAN_POINT('Ctrl Pts',(14.8226659040356,13.9641140924029,5.31521855721497));
#134544=CARTESIAN_POINT('Ctrl Pts',(14.8856838971343,14.5859900068555,4.53263294079442));
#134545=CARTESIAN_POINT('Ctrl Pts',(14.948701890233,15.581479503339,4.62302497433563));
#134546=CARTESIAN_POINT('Ctrl Pts',(15.0117198833317,16.052226355935,5.50482302169524));
#134547=CARTESIAN_POINT('Ctrl Pts',(15.0747378764303,15.5734158356716,6.38226854658017));
#134548=CARTESIAN_POINT('Ctrl Pts',(15.137755869529,14.5771394821179,6.46353128365394));
#134549=CARTESIAN_POINT('Ctrl Pts',(15.2007738626276,13.9624638088836,5.67527747963153));
#134550=CARTESIAN_POINT('Ctrl Pts',(15.2637918557263,14.284088673116,4.72884858252123));
#134551=CARTESIAN_POINT('Ctrl Pts',(15.326809848825,15.2517711484823,4.47832743437281));
#134552=CARTESIAN_POINT('Ctrl Pts',(15.3898278419236,15.9922485772217,5.14979105974335));
#134553=CARTESIAN_POINT('Ctrl Pts',(15.4528458350223,15.8372942327814,6.13729263921524));
#134554=CARTESIAN_POINT('Ctrl Pts',(15.5158638281209,14.9267430795219,6.54968422139037));
#134555=CARTESIAN_POINT('Ctrl Pts',(15.5788818212196,14.0823009391162,6.01481256239352));
#134556=CARTESIAN_POINT('Ctrl Pts',(15.6418998143183,14.0660150849458,5.01536021711829));
#134557=CARTESIAN_POINT('Ctrl Pts',(15.704917807417,14.8925823091702,4.45325983142974));
#134558=CARTESIAN_POINT('Ctrl Pts',(15.7679358005156,15.8160861433567,4.8357658941475));
#134559=CARTESIAN_POINT('Ctrl Pts',(15.8309537936143,16.0031319179609,5.81769465831711));
#134560=CARTESIAN_POINT('Ctrl Pts',(15.893971786713,15.284924501097,6.51292722810789));
#134561=CARTESIAN_POINT('Ctrl Pts',(15.9569897798116,14.3095935600653,6.29406705539134));
#134562=CARTESIAN_POINT('Ctrl Pts',(16.0200077729103,13.9573039379045,5.35861943962407));
#134563=CARTESIAN_POINT('Ctrl Pts',(16.083025766009,14.5459712537588,4.55075743966601));
#134564=CARTESIAN_POINT('Ctrl Pts',(16.1460437591076,15.5443663075088,4.59951742714692));
#134565=CARTESIAN_POINT('Ctrl Pts',(16.2090617522063,16.0515105811953,5.46089707944791));
#134566=CARTESIAN_POINT('Ctrl Pts',(16.272079745305,15.6097434580332,6.35756425773636));
#134567=CARTESIAN_POINT('Ctrl Pts',(16.3350977384036,14.6177274578437,6.48034241175276));
#134568=CARTESIAN_POINT('Ctrl Pts',(16.3981157315023,13.9706844692882,5.71843323691812));
#134569=CARTESIAN_POINT('Ctrl Pts',(16.461133724601,14.2525234677569,4.75940404098975));
#134570=CARTESIAN_POINT('Ctrl Pts',(16.5241517176996,15.2089053695745,4.46870853423261));
#134571=CARTESIAN_POINT('Ctrl Pts',(16.5871697107983,15.9767654537018,5.10867815144677));
#134572=CARTESIAN_POINT('Ctrl Pts',(16.6501877038969,15.8631661520898,6.10178711736918));
#134573=CARTESIAN_POINT('Ctrl Pts',(16.7132056969956,14.9706225261181,6.55182722205794));
#134574=CARTESIAN_POINT('Ctrl Pts',(16.7762236900943,14.1045899220371,6.05267018422339));
#134575=CARTESIAN_POINT('Ctrl Pts',(16.839241683193,14.0465994266362,5.05476872577994));
#134576=CARTESIAN_POINT('Ctrl Pts',(16.9022596762916,14.8489832222702,4.45865592842353));
#134577=CARTESIAN_POINT('Ctrl Pts',(16.9652776693903,15.787648613307,4.80227999985966));
#134578=CARTESIAN_POINT('Ctrl Pts',(17.0282956624889,16.0155187394014,5.77554533686269));
#134579=CARTESIAN_POINT('Ctrl Pts',(17.0913136555876,15.3269574666784,6.5001511721468));
#134580=CARTESIAN_POINT('Ctrl Pts',(17.1543316486863,14.3433410059052,6.3221936963746));
#134581=CARTESIAN_POINT('Ctrl Pts',(17.217349641785,13.952311236067,5.40226658917767));
#134582=CARTESIAN_POINT('Ctrl Pts',(17.2803676348836,14.5067440035288,4.57053664387043));
#134583=CARTESIAN_POINT('Ctrl Pts',(17.3433856279823,15.5063041339583,4.57757958305543));
#134584=CARTESIAN_POINT('Ctrl Pts',(17.4064036210809,16.0489620057577,5.41703913191933));
#134585=CARTESIAN_POINT('Ctrl Pts',(17.4694216141796,15.6450080068199,6.33136548819757));
#134586=CARTESIAN_POINT('Ctrl Pts',(17.5324396072783,14.6589821885264,6.49544394726743));
#134587=CARTESIAN_POINT('Ctrl Pts',(17.5954576003769,13.9806985754322,5.76120966818718));
#134588=CARTESIAN_POINT('Ctrl Pts',(17.6584755934756,14.2222627342275,4.7912476609151));
#134589=CARTESIAN_POINT('Ctrl Pts',(17.7214935865743,15.1656724749127,4.46089274918404));
#134590=CARTESIAN_POINT('Ctrl Pts',(17.7845115796729,15.9595854794191,5.06823676930197));
#134591=CARTESIAN_POINT('Ctrl Pts',(17.8475295727716,15.8875222111491,6.0652532435705));
#134592=CARTESIAN_POINT('Ctrl Pts',(17.9105475658703,15.0145750914678,6.5520965547484));
#134593=CARTESIAN_POINT('Ctrl Pts',(17.9735655589689,14.1283970495782,6.08964272227883));
#134594=CARTESIAN_POINT('Ctrl Pts',(18.0365835520676,14.0289287818801,5.09480078197536));
#134595=CARTESIAN_POINT('Ctrl Pts',(18.0996015451662,14.8054853669582,4.46616510654412));
#134596=CARTESIAN_POINT('Ctrl Pts',(18.1626195382649,15.7581551599557,4.76942190816593));
#134597=CARTESIAN_POINT('Ctrl Pts',(18.2256406818602,16.0255153784595,5.73419557681956));
#134598=CARTESIAN_POINT('Ctrl Pts',(18.2676558277559,15.5883124224641,6.23301607170624));
#134599=CARTESIAN_POINT('Ctrl Pts',(18.2886649759521,15.3123869947755,6.33610426986964));
#134600=CARTESIAN_POINT('Ctrl Pts',(13.9851010718527,14.5736241392876,6.37123956181065));
#134601=CARTESIAN_POINT('Ctrl Pts',(14.0061110196089,14.2860916803124,6.23052922894009));
#134602=CARTESIAN_POINT('Ctrl Pts',(14.0481269650644,13.8660291165181,5.64471280801549));
#134603=CARTESIAN_POINT('Ctrl Pts',(14.1111489082198,14.2573688790063,4.62954344518124));
#134604=CARTESIAN_POINT('Ctrl Pts',(14.1741669013184,15.3198606444279,4.4024349477251));
#134605=CARTESIAN_POINT('Ctrl Pts',(14.2371848944171,16.0931895365261,5.16458242119979));
#134606=CARTESIAN_POINT('Ctrl Pts',(14.3002028875157,15.8802572950314,6.23003900986589));
#134607=CARTESIAN_POINT('Ctrl Pts',(14.3632208806144,14.8728224902654,6.63637129684331));
#134608=CARTESIAN_POINT('Ctrl Pts',(14.426238873713,13.9802252660501,6.0173745739973));
#134609=CARTESIAN_POINT('Ctrl Pts',(14.4892568668117,14.0078646353351,4.93140145487682));
#134610=CARTESIAN_POINT('Ctrl Pts',(14.5522748599104,14.930851851153,4.35858990703292));
#134611=CARTESIAN_POINT('Ctrl Pts',(14.615292853009,15.9162308480355,4.81579542658434));
#134612=CARTESIAN_POINT('Ctrl Pts',(14.6783108461077,16.0747833228706,5.89045686361985));
#134613=CARTESIAN_POINT('Ctrl Pts',(14.7413288392064,15.263419984007,6.61275371987895));
#134614=CARTESIAN_POINT('Ctrl Pts',(14.8043468323051,14.2143406429926,6.33087471292751));
#134615=CARTESIAN_POINT('Ctrl Pts',(14.8673648254037,13.8742607609987,5.29919051001966));
#134616=CARTESIAN_POINT('Ctrl Pts',(14.9303828185024,14.5500785451338,4.4487229731784));
#134617=CARTESIAN_POINT('Ctrl Pts',(14.993400811601,15.6319173654,4.54695566299893));
#134618=CARTESIAN_POINT('Ctrl Pts',(15.0564188046997,16.1434970671,5.50524137333374));
#134619=CARTESIAN_POINT('Ctrl Pts',(15.1194367977984,15.6231542506237,6.45879702092473));
#134620=CARTESIAN_POINT('Ctrl Pts',(15.1824547908971,14.5404603208586,6.54710853392214));
#134621=CARTESIAN_POINT('Ctrl Pts',(15.2454727839957,13.8724673309506,5.6904811476702));
#134622=CARTESIAN_POINT('Ctrl Pts',(15.3084907770944,14.2219901184019,4.66195847100467));
#134623=CARTESIAN_POINT('Ctrl Pts',(15.371508770193,15.2736099207609,4.38970697631589));
#134624=CARTESIAN_POINT('Ctrl Pts',(15.4345267632917,16.0783167818286,5.11941373755096));
#134625=CARTESIAN_POINT('Ctrl Pts',(15.4975447563904,15.9099216096279,6.19257176435145));
#134626=CARTESIAN_POINT('Ctrl Pts',(15.560562749489,14.9203887326725,6.64073442636246));
#134627=CARTESIAN_POINT('Ctrl Pts',(15.6235807425877,14.002699201857,6.05946769616896));
#134628=CARTESIAN_POINT('Ctrl Pts',(15.6865987356864,13.9850007034551,4.97332228735827));
#134629=CARTESIAN_POINT('Ctrl Pts',(15.749616728785,14.8832648377169,4.36246499526975));
#134630=CARTESIAN_POINT('Ctrl Pts',(15.8126347218837,15.8868739184927,4.7781498509081));
#134631=CARTESIAN_POINT('Ctrl Pts',(15.8756527149824,16.090144149719,5.84525167324489));
#134632=CARTESIAN_POINT('Ctrl Pts',(15.938670708081,15.3096390139932,6.60078911062615));
#134633=CARTESIAN_POINT('Ctrl Pts',(16.0016887011797,14.2497073137171,6.36294488234316));
#134634=CARTESIAN_POINT('Ctrl Pts',(16.0647066942784,13.866859889835,5.34635600959533));
#134635=CARTESIAN_POINT('Ctrl Pts',(16.127724687377,14.5065885426861,4.46841960136624));
#134636=CARTESIAN_POINT('Ctrl Pts',(16.1907426804757,15.5915849499048,4.5214090578285));
#134637=CARTESIAN_POINT('Ctrl Pts',(16.2537606735744,16.1427192056532,5.45750526993156));
#134638=CARTESIAN_POINT('Ctrl Pts',(16.316778666673,15.6626329515618,6.43194986804897));
#134639=CARTESIAN_POINT('Ctrl Pts',(16.3797966597717,14.5845689206292,6.56537786881118));
#134640=CARTESIAN_POINT('Ctrl Pts',(16.4428146528704,13.881401056103,5.73738025983114));
#134641=CARTESIAN_POINT('Ctrl Pts',(16.505832645969,14.1876869292192,4.69516432727843));
#134642=CARTESIAN_POINT('Ctrl Pts',(16.5688506390677,15.2270259398679,4.37925372731961));
#134643=CARTESIAN_POINT('Ctrl Pts',(16.6318686321664,16.0614906433893,5.07473467226058));
#134644=CARTESIAN_POINT('Ctrl Pts',(16.694886625265,15.9380376738973,6.15398647339405));
#134645=CARTESIAN_POINT('Ctrl Pts',(16.7579046183637,14.9680743073643,6.64306331212394));
#134646=CARTESIAN_POINT('Ctrl Pts',(16.8209226114623,14.0269215438038,6.10060910959739));
#134647=CARTESIAN_POINT('Ctrl Pts',(16.883940604561,13.9639009199269,5.0161491124223));
#134648=CARTESIAN_POINT('Ctrl Pts',(16.9469585976597,14.8358839412804,4.36832915277863));
#134649=CARTESIAN_POINT('Ctrl Pts',(17.0099765907584,15.8559697009506,4.74175937114927));
#134650=CARTESIAN_POINT('Ctrl Pts',(17.072994583857,16.1036054110797,5.79944629573126));
#134651=CARTESIAN_POINT('Ctrl Pts',(17.1360125769557,15.3553179428593,6.58690485232163));
#134652=CARTESIAN_POINT('Ctrl Pts',(17.1990305700544,14.286382032158,6.39351124412484));
#134653=CARTESIAN_POINT('Ctrl Pts',(17.262048563153,13.861434118207,5.39378913766735));
#134654=CARTESIAN_POINT('Ctrl Pts',(17.3250665562517,14.463958698513,4.48991446496641));
#134655=CARTESIAN_POINT('Ctrl Pts',(17.3880845493504,15.5502212418235,4.49756831269261));
#134656=CARTESIAN_POINT('Ctrl Pts',(17.451102542449,16.139949565336,5.40984305914861));
#134657=CARTESIAN_POINT('Ctrl Pts',(17.5141205355477,15.7009563673201,6.40347860237476));
#134658=CARTESIAN_POINT('Ctrl Pts',(17.5771385286463,14.6294021100598,6.58178932008526));
#134659=CARTESIAN_POINT('Ctrl Pts',(17.640156521745,13.8922837914963,5.78386714302055));
#134660=CARTESIAN_POINT('Ctrl Pts',(17.7031745148437,14.154801362493,4.72977008086474));
#134661=CARTESIAN_POINT('Ctrl Pts',(17.7661925079424,15.180042999392,4.3707599966411));
#134662=CARTESIAN_POINT('Ctrl Pts',(17.829210501041,16.042820468389,5.03078538168141));
#134663=CARTESIAN_POINT('Ctrl Pts',(17.8922284941397,15.9645063913394,6.11428363065212));
#134664=CARTESIAN_POINT('Ctrl Pts',(17.9552464872383,15.0158393431718,6.64335600688478));
#134665=CARTESIAN_POINT('Ctrl Pts',(18.018264480337,14.0527937150962,6.14078866658263));
#134666=CARTESIAN_POINT('Ctrl Pts',(18.0812824734357,13.9446975134179,5.05965357188695));
#134667=CARTESIAN_POINT('Ctrl Pts',(18.1443004665343,14.7886130573173,4.37648968127024));
#134668=CARTESIAN_POINT('Ctrl Pts',(18.207318459633,15.8239179687204,4.70605114993779));
#134669=CARTESIAN_POINT('Ctrl Pts',(18.2703396032283,16.114469164282,5.75450983403944));
#134670=CARTESIAN_POINT('Ctrl Pts',(18.312354749124,15.6393429758072,6.29659830169184));
#134671=CARTESIAN_POINT('Ctrl Pts',(18.3333638973201,15.3394836199561,6.40862842865793));
#134672=CARTESIAN_POINT('',(14.0280374670081,14.0780374670081,5.50000000327438));
#134673=CARTESIAN_POINT('Ctrl Pts',(14.0280374670081,14.0780374670081,5.50000000654876));
#134674=CARTESIAN_POINT('Ctrl Pts',(14.0336707525267,14.0836707516792,5.38068063053235));
#134675=CARTESIAN_POINT('Ctrl Pts',(14.0394414468597,14.1127440757323,5.26304138084325));
#134676=CARTESIAN_POINT('Ctrl Pts',(14.0496371634471,14.2112191405822,5.05112665797812));
#134677=CARTESIAN_POINT('Ctrl Pts',(14.0540832508647,14.2782937417532,4.95704494172787));
#134678=CARTESIAN_POINT('Ctrl Pts',(14.0646664677378,14.4586721851121,4.78677377365687));
#134679=CARTESIAN_POINT('Ctrl Pts',(14.0701889998458,14.5559376608619,4.73662342738342));
#134680=CARTESIAN_POINT('Ctrl Pts',(14.0796677175689,14.7331134953084,4.66368605021134));
#134681=CARTESIAN_POINT('Ctrl Pts',(14.08506495303,14.84742847341,4.64092381676413));
#134682=CARTESIAN_POINT('Ctrl Pts',(14.0944011777295,15.0592500270387,4.6409810781504));
#134683=CARTESIAN_POINT('Ctrl Pts',(14.0984589285287,15.1558116203124,4.65722900890055));
#134684=CARTESIAN_POINT('Ctrl Pts',(14.108532644215,15.351725110515,4.7275697529941));
#134685=CARTESIAN_POINT('Ctrl Pts',(14.1145177155538,15.4478924506123,4.78605667147313));
#134686=CARTESIAN_POINT('Ctrl Pts',(14.1249265358644,15.6016864042129,4.92708381458633));
#134687=CARTESIAN_POINT('Ctrl Pts',(14.129415714943,15.6619331275998,5.00531324896704));
#134688=CARTESIAN_POINT('Ctrl Pts',(14.1386402801144,15.7544728653423,5.18408713983558));
#134689=CARTESIAN_POINT('Ctrl Pts',(14.1435958781485,15.7837880958418,5.28377178093206));
#134690=CARTESIAN_POINT('Ctrl Pts',(14.1545039313174,15.8014139214458,5.48546862399363));
#134691=CARTESIAN_POINT('Ctrl Pts',(14.1598505847911,15.7917261955478,5.58470225767358));
#134692=CARTESIAN_POINT('Ctrl Pts',(14.1696529264411,15.7378044704229,5.77166909773013));
#134693=CARTESIAN_POINT('Ctrl Pts',(14.1740949113336,15.6946341146314,5.85877380590229));
#134694=CARTESIAN_POINT('Ctrl Pts',(14.1851465525943,15.5609075800702,6.03474948161481));
#134695=CARTESIAN_POINT('Ctrl Pts',(14.1911371129321,15.4767337706299,6.09477078358694));
#134696=CARTESIAN_POINT('Ctrl Pts',(14.2007965388827,15.328712435131,6.1804779565484));
#134697=CARTESIAN_POINT('Ctrl Pts',(14.2060770183145,15.2336306819364,6.21318772401287));
#134698=CARTESIAN_POINT('Ctrl Pts',(14.2111576979006,15.1353877924827,6.22633194409867));
#134699=CARTESIAN_POINT('',(18.2,15.6465738458316,4.7812873840077));
#134700=CARTESIAN_POINT('Ctrl Pts',(18.2,15.6465738458316,4.78128738400769));
#134701=CARTESIAN_POINT('Ctrl Pts',(18.2,15.6619638572722,4.79851741080685));
#134702=CARTESIAN_POINT('Ctrl Pts',(18.2,15.6766698976115,4.81631464232827));
#134703=CARTESIAN_POINT('Ctrl Pts',(18.2,15.6906448654999,4.83466849716618));
#134704=CARTESIAN_POINT('Ctrl Pts',(18.2,15.7133028676804,4.8644261099392));
#134705=CARTESIAN_POINT('Ctrl Pts',(18.2,15.7340406678333,4.89564678969883));
#134706=CARTESIAN_POINT('Ctrl Pts',(18.2,15.752815722504,4.92811617435309));
#134707=CARTESIAN_POINT('Ctrl Pts',(18.2,15.7609364545188,4.94216008400264));
#134708=CARTESIAN_POINT('Ctrl Pts',(18.2,15.7686896018272,4.9564376928423));
#134709=CARTESIAN_POINT('Ctrl Pts',(18.2,15.7760699087929,4.97093183307526));
#134710=CARTESIAN_POINT('Ctrl Pts',(18.2,15.7809487495338,4.98051335891182));
#134711=CARTESIAN_POINT('Ctrl Pts',(18.2,15.7856650391499,4.99019075750296));
#134712=CARTESIAN_POINT('Ctrl Pts',(18.2,15.7902099091838,4.99994269671711));
#134713=CARTESIAN_POINT('Ctrl Pts',(18.2,15.8078416972689,5.03777526934493));
#134714=CARTESIAN_POINT('Ctrl Pts',(18.2,15.8229264746598,5.07678379042559));
#134715=CARTESIAN_POINT('Ctrl Pts',(18.2,15.8354041793666,5.11666566334121));
#134716=CARTESIAN_POINT('Ctrl Pts',(18.2,15.8426768939495,5.13991108271611));
#134717=CARTESIAN_POINT('Ctrl Pts',(18.2,15.8490629577306,5.16345335684645));
#134718=CARTESIAN_POINT('Ctrl Pts',(18.2,15.8545422976518,5.18723193817096));
#134719=CARTESIAN_POINT('Ctrl Pts',(18.2,15.8568489985993,5.19724228190916));
#134720=CARTESIAN_POINT('Ctrl Pts',(18.2,15.8589949315482,5.20729448794936));
#134721=CARTESIAN_POINT('Ctrl Pts',(18.2,15.8609782780096,5.21738393794125));
#134722=CARTESIAN_POINT('Ctrl Pts',(18.2,15.8626367821966,5.22582088800598));
#134723=CARTESIAN_POINT('Ctrl Pts',(18.2,15.8641798770857,5.2342752559103));
#134724=CARTESIAN_POINT('Ctrl Pts',(18.2,15.8656067899539,5.24274194350229));
#134725=CARTESIAN_POINT('Ctrl Pts',(18.2,15.8722734405497,5.28229898243267));
#134726=CARTESIAN_POINT('Ctrl Pts',(18.2,15.8764114541761,5.3221428446593));
#134727=CARTESIAN_POINT('Ctrl Pts',(18.2,15.8779609221616,5.36200248215288));
#134728=CARTESIAN_POINT('Ctrl Pts',(18.2,15.8794724375262,5.40088579891964));
#134729=CARTESIAN_POINT('Ctrl Pts',(18.2,15.878520444433,5.43978518781648));
#134730=CARTESIAN_POINT('Ctrl Pts',(18.2,15.8750036525905,5.47843420519303));
#134731=CARTESIAN_POINT('Ctrl Pts',(18.2,15.8732775467615,5.49740385058803));
#134732=CARTESIAN_POINT('Ctrl Pts',(18.2,15.8709328890102,5.51631285417556));
#134733=CARTESIAN_POINT('Ctrl Pts',(18.2,15.867953759687,5.53512721905791));
#134734=CARTESIAN_POINT('Ctrl Pts',(18.2,15.8667539586533,5.54270443105018));
#134735=CARTESIAN_POINT('Ctrl Pts',(18.2,15.8654512196989,5.55026627040294));
#134736=CARTESIAN_POINT('Ctrl Pts',(18.2,15.8640443848231,5.55781041816403));
#134737=CARTESIAN_POINT('Ctrl Pts',(18.2,15.862571092852,5.56571094189791));
#134738=CARTESIAN_POINT('Ctrl Pts',(18.2,15.8609851714727,5.57358365073891));
#134739=CARTESIAN_POINT('Ctrl Pts',(18.2,15.8592867750134,5.58142260636899));
#134740=CARTESIAN_POINT('Ctrl Pts',(18.2,15.8514062407123,5.6177952438591));
#134741=CARTESIAN_POINT('Ctrl Pts',(18.2,15.8411029443695,5.6534686019582));
#134742=CARTESIAN_POINT('Ctrl Pts',(18.2,15.828297120991,5.6882046655143));
#134743=CARTESIAN_POINT('Ctrl Pts',(18.2,15.8160303433657,5.72147855619873));
#134744=CARTESIAN_POINT('Ctrl Pts',(18.2,15.8014660665262,5.75389278659253));
#134745=CARTESIAN_POINT('Ctrl Pts',(18.2,15.7847628740101,5.78528187055323));
#134746=CARTESIAN_POINT('Ctrl Pts',(18.2,15.7761700718178,5.80142969314545));
#134747=CARTESIAN_POINT('Ctrl Pts',(18.2,15.767010787845,5.81730575509916));
#134748=CARTESIAN_POINT('Ctrl Pts',(18.2,15.7573045304862,5.83288422857645));
#134749=CARTESIAN_POINT('Ctrl Pts',(18.2,15.7524647891595,5.84065197871007));
#134750=CARTESIAN_POINT('Ctrl Pts',(18.2,15.7474890404345,5.84834570361276));
#134751=CARTESIAN_POINT('Ctrl Pts',(18.2,15.742379616577,5.85596196283741));
#134752=CARTESIAN_POINT('Ctrl Pts',(18.2,15.7379704818769,5.86253435020793));
#134753=CARTESIAN_POINT('Ctrl Pts',(18.2,15.7334665877127,5.86904185446495));
#134754=CARTESIAN_POINT('Ctrl Pts',(18.2,15.728872202191,5.87547971657246));
#134755=CARTESIAN_POINT('Ctrl Pts',(18.2,15.7072110042844,5.90583237299332));
#134756=CARTESIAN_POINT('Ctrl Pts',(18.2,15.6835253756505,5.93466343247602));
#134757=CARTESIAN_POINT('Ctrl Pts',(18.2,15.6580146973991,5.96178851524292));
#134758=CARTESIAN_POINT('Ctrl Pts',(18.2,15.6328139718729,5.98858403039735));
#134759=CARTESIAN_POINT('Ctrl Pts',(18.2,15.6058311072394,6.01371535851912));
#134760=CARTESIAN_POINT('Ctrl Pts',(18.2,15.5772374383809,6.03695901454861));
#134761=CARTESIAN_POINT('Ctrl Pts',(18.2,15.5637070537067,6.04795779924012));
#134762=CARTESIAN_POINT('Ctrl Pts',(18.2,15.5498157916581,6.05853318696841));
#134763=CARTESIAN_POINT('Ctrl Pts',(18.2,15.535581267231,6.0686573074634));
#134764=CARTESIAN_POINT('Ctrl Pts',(18.2,15.5278719685831,6.07414044593024));
#134765=CARTESIAN_POINT('Ctrl Pts',(18.2,15.5200592747775,6.07949273630841));
#134766=CARTESIAN_POINT('Ctrl Pts',(18.2,15.5121669270856,6.08469624357819));
#134767=CARTESIAN_POINT('Ctrl Pts',(18.2,15.4829267970524,6.10397456672572));
#134768=CARTESIAN_POINT('Ctrl Pts',(18.2,15.4525389626987,6.12125574713354));
#134769=CARTESIAN_POINT('Ctrl Pts',(18.2,15.421162325823,6.13635948517253));
#134770=CARTESIAN_POINT('Ctrl Pts',(18.2,15.39038989133,6.15117237895856));
#134771=CARTESIAN_POINT('Ctrl Pts',(18.2,15.3586654362256,6.16389118075813));
#134772=CARTESIAN_POINT('Ctrl Pts',(18.2,15.3261350604803,6.17429720693868));
#134773=CARTESIAN_POINT('Ctrl Pts',(18.2,15.3040284533689,6.18136881085022));
#134774=CARTESIAN_POINT('Ctrl Pts',(18.2,15.2815495952911,6.18737133729665));
#134775=CARTESIAN_POINT('Ctrl Pts',(18.2,15.2587465130648,6.19222196005096));
#134776=CARTESIAN_POINT('Ctrl Pts',(18.1991564130999,15.6365194374333,4.77236310691848));
#134777=CARTESIAN_POINT('Ctrl Pts',(18.199295405163,15.6381966008544,4.7738318074538));
#134778=CARTESIAN_POINT('Ctrl Pts',(18.1994348289128,15.6398688368353,4.77530606333199));
#134779=CARTESIAN_POINT('Ctrl Pts',(18.1997162076013,15.6432228597935,4.77828289048378));
#134780=CARTESIAN_POINT('Ctrl Pts',(18.1998575472869,15.6448971332663,4.77977896678006));
#134781=CARTESIAN_POINT('Ctrl Pts',(18.2,15.6465738458316,4.78128738400769));
#134782=CARTESIAN_POINT('Ctrl Pts',(13.98325,14.5748808714849,6.36826222368044));
#134783=CARTESIAN_POINT('Ctrl Pts',(13.9875417602103,14.4844399306344,6.31920189146972));
#134784=CARTESIAN_POINT('Ctrl Pts',(13.9922799151223,14.4025086332371,6.25551032335682));
#134785=CARTESIAN_POINT('Ctrl Pts',(14.0008552261829,14.2697005535018,6.11314868208129));
#134786=CARTESIAN_POINT('Ctrl Pts',(14.0047036502539,14.2168248101705,6.03725042346018));
#134787=CARTESIAN_POINT('Ctrl Pts',(14.0105260091161,14.1516119367069,5.90710469125805));
#134788=CARTESIAN_POINT('Ctrl Pts',(14.0126201956516,14.1316248252275,5.85705808156466));
#134789=CARTESIAN_POINT('Ctrl Pts',(14.0187426631304,14.0868108221527,5.70870074149093));
#134790=CARTESIAN_POINT('Ctrl Pts',(14.0229471609679,14.0736800775832,5.60806525442127));
#134791=CARTESIAN_POINT('Ctrl Pts',(14.0278346537838,14.0778421664996,5.50429828067971));
#134792=CARTESIAN_POINT('Ctrl Pts',(14.0279360152398,14.0779360152551,5.50214887005762));
#134793=CARTESIAN_POINT('Ctrl Pts',(14.0280374670081,14.0780374670081,5.50000000654876));
#134794=CARTESIAN_POINT('Origin',(18.2,15.,5.5));
#134795=CARTESIAN_POINT('',(18.2,15.,6.46675));
#134796=CARTESIAN_POINT('Origin',(18.2,15.,5.5));
#134797=CARTESIAN_POINT('',(18.2002863776289,14.4279740780313,5.96873714629846));
#134798=CARTESIAN_POINT('Ctrl Pts',(18.1999951595719,14.4317719229139,5.97248053125074));
#134799=CARTESIAN_POINT('Ctrl Pts',(18.2000922322575,14.4306418421285,5.97112144111024));
#134800=CARTESIAN_POINT('Ctrl Pts',(18.2001893049432,14.4295166373798,5.96975829655493));
#134801=CARTESIAN_POINT('Ctrl Pts',(18.2002863776289,14.428396337634,5.96839113267634));
#134802=CARTESIAN_POINT('Ctrl Pts',(18.2,14.4275267117712,5.96905018147065));
#134803=CARTESIAN_POINT('Ctrl Pts',(18.2,14.4110560788823,5.95432723823809));
#134804=CARTESIAN_POINT('Ctrl Pts',(18.2,14.3953252123756,5.93885849755578));
#134805=CARTESIAN_POINT('Ctrl Pts',(18.2,14.3803983141861,5.92267896053057));
#134806=CARTESIAN_POINT('Ctrl Pts',(18.2,14.3578580110206,5.89824711507976));
#134807=CARTESIAN_POINT('Ctrl Pts',(18.2,14.3371491699726,5.87219655019198));
#134808=CARTESIAN_POINT('Ctrl Pts',(18.2,14.3182680759095,5.84477757422518));
#134809=CARTESIAN_POINT('Ctrl Pts',(18.2,14.312272357361,5.83607063901083));
#134810=CARTESIAN_POINT('Ctrl Pts',(18.2,14.3064611356987,5.82722540504078));
#134811=CARTESIAN_POINT('Ctrl Pts',(18.2,14.3008348537117,5.81824908509359));
#134812=CARTESIAN_POINT('Ctrl Pts',(18.2,14.2956258061032,5.80993843197276));
#134813=CARTESIAN_POINT('Ctrl Pts',(18.2,14.2905790444203,5.80152119332205));
#134814=CARTESIAN_POINT('Ctrl Pts',(18.2,14.2856985275162,5.79301102887662));
#134815=CARTESIAN_POINT('Ctrl Pts',(18.2,14.2679154747507,5.76200269382717));
#134816=CARTESIAN_POINT('Ctrl Pts',(18.2,14.252318999542,5.72973535427369));
#134817=CARTESIAN_POINT('Ctrl Pts',(18.2,14.2389065388398,5.69650131415319));
#134818=CARTESIAN_POINT('Ctrl Pts',(18.2,14.2330453803533,5.68197825379763));
#134819=CARTESIAN_POINT('Ctrl Pts',(18.2,14.2276016983777,5.66727002000594));
#134820=CARTESIAN_POINT('Ctrl Pts',(18.2,14.2225773518228,5.65239869796253));
#134821=CARTESIAN_POINT('Ctrl Pts',(18.2,14.2195918595483,5.64356208277537));
#134822=CARTESIAN_POINT('Ctrl Pts',(18.2,14.2167544515313,5.63466786072778));
#134823=CARTESIAN_POINT('Ctrl Pts',(18.2,14.2140657538221,5.62572048401501));
#134824=CARTESIAN_POINT('Ctrl Pts',(18.2,14.2114827872951,5.61712495671811));
#134825=CARTESIAN_POINT('Ctrl Pts',(18.2,14.2090397158183,5.60848901704883));
#134826=CARTESIAN_POINT('Ctrl Pts',(18.2,14.2067374833686,5.5998213650989));
#134827=CARTESIAN_POINT('Ctrl Pts',(18.2,14.1970355687405,5.56329472364009));
#134828=CARTESIAN_POINT('Ctrl Pts',(18.2,14.1898245868981,5.526184207686));
#134829=CARTESIAN_POINT('Ctrl Pts',(18.2,14.1851036775246,5.48880133972137));
#134830=CARTESIAN_POINT('Ctrl Pts',(18.2,14.1803510104794,5.45116699629885));
#134831=CARTESIAN_POINT('Ctrl Pts',(18.2,14.1781214585709,5.41325537129091));
#134832=CARTESIAN_POINT('Ctrl Pts',(18.2,14.1784579006432,5.37535412581749));
#134833=CARTESIAN_POINT('Ctrl Pts',(18.2,14.1786450716592,5.35426872893824));
#134834=CARTESIAN_POINT('Ctrl Pts',(18.2,14.1796272365876,5.33318611320977));
#134835=CARTESIAN_POINT('Ctrl Pts',(18.2,14.1814185858649,5.31215405814663));
#134836=CARTESIAN_POINT('Ctrl Pts',(18.2,14.1821024176586,5.30412525654898));
#134837=CARTESIAN_POINT('Ctrl Pts',(18.2,14.1829035768574,5.29611199368922));
#134838=CARTESIAN_POINT('Ctrl Pts',(18.2,14.1838216163247,5.28812180317335));
#134839=CARTESIAN_POINT('Ctrl Pts',(18.2,14.1882918266273,5.24921516218645));
#134840=CARTESIAN_POINT('Ctrl Pts',(18.2,14.195532536316,5.21082134697863));
#134841=CARTESIAN_POINT('Ctrl Pts',(18.2,14.2055656184632,5.1732481664357));
#134842=CARTESIAN_POINT('Ctrl Pts',(18.2,14.2152472940966,5.13699097834594));
#134843=CARTESIAN_POINT('Ctrl Pts',(18.2,14.227528570009,5.10149645494108));
#134844=CARTESIAN_POINT('Ctrl Pts',(18.2,14.2421925851606,5.0669049975911));
#134845=CARTESIAN_POINT('Ctrl Pts',(18.2,14.2489467564536,5.05097234709937));
#134846=CARTESIAN_POINT('Ctrl Pts',(18.2,14.2562071429791,5.03523130804939));
#134847=CARTESIAN_POINT('Ctrl Pts',(18.2,14.2639560523831,5.01969608757539));
#134848=CARTESIAN_POINT('Ctrl Pts',(18.2,14.2677892194207,5.01201125195023));
#134849=CARTESIAN_POINT('Ctrl Pts',(18.2,14.2717419603285,5.00437678786767));
#134850=CARTESIAN_POINT('Ctrl Pts',(18.2,14.2758123165251,4.99679447067505));
#134851=CARTESIAN_POINT('Ctrl Pts',(18.2,14.2797099298683,4.98953394131724));
#134852=CARTESIAN_POINT('Ctrl Pts',(18.2,14.2837112647265,4.98232898818152));
#134853=CARTESIAN_POINT('Ctrl Pts',(18.2,14.2878118668406,4.97518441495171));
#134854=CARTESIAN_POINT('Ctrl Pts',(18.2,14.307746884195,4.9404511764259));
#134855=CARTESIAN_POINT('Ctrl Pts',(18.2,14.33003748588,4.90711848704015));
#134856=CARTESIAN_POINT('Ctrl Pts',(18.2,14.3544187642976,4.87534375641278));
#134857=CARTESIAN_POINT('Ctrl Pts',(18.2,14.3788000427153,4.84356902578541));
#134858=CARTESIAN_POINT('Ctrl Pts',(18.2,14.4052726360747,4.81335131532712));
#134859=CARTESIAN_POINT('Ctrl Pts',(18.2,14.4336230376443,4.78485942579126));
#134860=CARTESIAN_POINT('Ctrl Pts',(18.2,14.447387658005,4.77102611052555));
#134861=CARTESIAN_POINT('Ctrl Pts',(18.2,14.4615956412497,4.75759987717825));
#134862=CARTESIAN_POINT('Ctrl Pts',(18.2,14.4762262189405,4.74460203982858));
#134863=CARTESIAN_POINT('Ctrl Pts',(18.2,14.4829425087495,4.73863527321316));
#134864=CARTESIAN_POINT('Ctrl Pts',(18.2,14.489747884209,4.73275880670212));
#134865=CARTESIAN_POINT('Ctrl Pts',(18.2,14.4966404830651,4.72697482667735));
#134866=CARTESIAN_POINT('Ctrl Pts',(18.2,14.5028292708112,4.72178145543251));
#134867=CARTESIAN_POINT('Ctrl Pts',(18.2,14.5090804061117,4.71666934181821));
#134868=CARTESIAN_POINT('Ctrl Pts',(18.2,14.515391912452,4.7116396578817));
#134869=CARTESIAN_POINT('Ctrl Pts',(18.2,14.5484748964647,4.6852755944886));
#134870=CARTESIAN_POINT('Ctrl Pts',(18.2,14.583212849161,4.66117452364675));
#134871=CARTESIAN_POINT('Ctrl Pts',(18.2,14.6193549193654,4.63951288687606));
#134872=CARTESIAN_POINT('Ctrl Pts',(18.2,14.6552623674113,4.61799187016251));
#134873=CARTESIAN_POINT('Ctrl Pts',(18.2,14.6925565889502,4.59887772234494));
#134874=CARTESIAN_POINT('Ctrl Pts',(18.2,14.7310329626811,4.58237205343048));
#134875=CARTESIAN_POINT('Ctrl Pts',(18.2,14.7585486993975,4.57056829969433));
#134876=CARTESIAN_POINT('Ctrl Pts',(18.2,14.7866698996498,4.56009911105786));
#134877=CARTESIAN_POINT('Ctrl Pts',(18.2,14.8153312661022,4.55105162352181));
#134878=CARTESIAN_POINT('Origin',(18.2,15.,5.5));
#134879=CARTESIAN_POINT('Ctrl Pts',(13.9812628603546,15.4268458854961,6.37121714501327));
#134880=CARTESIAN_POINT('Ctrl Pts',(14.0022472159886,15.1396755667749,6.51192110495675));
#134881=CARTESIAN_POINT('Ctrl Pts',(14.0442104273441,14.420290532822,6.48498127166269));
#134882=CARTESIAN_POINT('Ctrl Pts',(14.1071524944209,13.8574310494572,5.55569014930716));
#134883=CARTESIAN_POINT('Ctrl Pts',(14.170089061585,14.3258164373528,4.57705680776936));
#134884=CARTESIAN_POINT('Ctrl Pts',(14.2330256287492,15.3998968445188,4.42900222271004));
#134885=CARTESIAN_POINT('Ctrl Pts',(14.2959621959134,16.1145993730642,5.24532569248693));
#134886=CARTESIAN_POINT('Ctrl Pts',(14.3588987630776,15.8255094218027,6.29084264316953));
#134887=CARTESIAN_POINT('Ctrl Pts',(14.4218353302418,14.7933917703228,6.62441707563672));
#134888=CARTESIAN_POINT('Ctrl Pts',(14.4847718974059,13.9471942622981,5.94566791670918));
#134889=CARTESIAN_POINT('Ctrl Pts',(14.5477084645701,14.0488711730629,4.86570045630136));
#134890=CARTESIAN_POINT('Ctrl Pts',(14.6106450317343,15.006816278288,4.35678006002944));
#134891=CARTESIAN_POINT('Ctrl Pts',(14.6735815988985,15.958636524409,4.87709145345759));
#134892=CARTESIAN_POINT('Ctrl Pts',(14.7365181660626,16.0474005173,5.95819916383029));
#134893=CARTESIAN_POINT('Ctrl Pts',(14.7994547332268,15.1932041177945,6.62679588022745));
#134894=CARTESIAN_POINT('Ctrl Pts',(14.862391300391,14.1650665262539,6.28094989097661));
#134895=CARTESIAN_POINT('Ctrl Pts',(14.9253278675552,13.888611432723,5.23202327700034));
#134896=CARTESIAN_POINT('Ctrl Pts',(14.9882644347194,14.6127271683571,4.42435313218742));
#134897=CARTESIAN_POINT('Ctrl Pts',(15.0512010018835,15.6855007097753,4.58507642183189));
#134898=CARTESIAN_POINT('Ctrl Pts',(15.1141375690477,16.141125178985,5.56949560057099));
#134899=CARTESIAN_POINT('Ctrl Pts',(15.1770741362119,15.5694069032307,6.4913486478301));
#134900=CARTESIAN_POINT('Ctrl Pts',(15.2400107033761,14.4850576496457,6.52070109597772));
#134901=CARTESIAN_POINT('Ctrl Pts',(15.3029472705403,13.8643055049512,5.63112726125519));
#134902=CARTESIAN_POINT('Ctrl Pts',(15.3658838377044,14.2660069674623,4.62350095278392));
#134903=CARTESIAN_POINT('Ctrl Pts',(15.4288204048686,15.3285145156993,4.40497736896518));
#134904=CARTESIAN_POINT('Ctrl Pts',(15.4917569720328,16.0952639548138,5.17229095502555));
#134905=CARTESIAN_POINT('Ctrl Pts',(15.554693539197,15.8759589633338,6.23463749178203));
#134906=CARTESIAN_POINT('Ctrl Pts',(15.6176301063612,14.8680374794508,6.63559774682888));
#134907=CARTESIAN_POINT('Ctrl Pts',(15.6805666735253,13.9789204425895,6.01419148848167));
#134908=CARTESIAN_POINT('Ctrl Pts',(15.7435032406895,14.0090704171655,4.92986412902933));
#134909=CARTESIAN_POINT('Ctrl Pts',(15.8064398078537,14.9313437035418,4.3588240002493));
#134910=CARTESIAN_POINT('Ctrl Pts',(15.8693763750179,15.9154275197398,4.81517242640679));
#134911=CARTESIAN_POINT('Ctrl Pts',(15.9323129421821,16.075361724617,5.88806379719466));
#134912=CARTESIAN_POINT('Ctrl Pts',(15.9952495093462,15.2671592629749,6.61158547924259));
#134913=CARTESIAN_POINT('Ctrl Pts',(16.0581860765104,14.2184361724521,6.33435863567591));
#134914=CARTESIAN_POINT('Ctrl Pts',(16.1211226436746,13.8733466420087,5.30596763057404));
#134915=CARTESIAN_POINT('Ctrl Pts',(16.1840592108388,14.5425710873636,4.45226189372512));
#134916=CARTESIAN_POINT('Ctrl Pts',(16.246995778003,15.623613893471,4.54182357504772));
#134917=CARTESIAN_POINT('Ctrl Pts',(16.3099323451671,16.1432237768698,5.49402125015251));
#134918=CARTESIAN_POINT('Ctrl Pts',(16.3728689123313,15.633601513481,6.45160152982487));
#134919=CARTESIAN_POINT('Ctrl Pts',(16.4358054794955,14.5535545798252,6.55246512355937));
#134920=CARTESIAN_POINT('Ctrl Pts',(16.4987420466597,13.8754376861007,5.70580561592405));
#134921=CARTESIAN_POINT('Ctrl Pts',(16.5616786138239,14.2097522234401,4.67386151216965));
#134922=CARTESIAN_POINT('Ctrl Pts',(16.624615180988,15.2555183875101,4.38568105848424));
#134923=CARTESIAN_POINT('Ctrl Pts',(16.6875517481522,16.0712440781121,5.10071003771423));
#134924=CARTESIAN_POINT('Ctrl Pts',(16.7504883153164,15.9225401760006,6.17521550127969));
#134925=CARTESIAN_POINT('Ctrl Pts',(16.8134248824806,14.9432832128561,6.64183166782179));
#134926=CARTESIAN_POINT('Ctrl Pts',(16.8763614496447,14.0150877694587,6.08046898526848));
#134927=CARTESIAN_POINT('Ctrl Pts',(16.9392980168089,13.9735982749522,4.99651628592629));
#134928=CARTESIAN_POINT('Ctrl Pts',(17.0022345839731,14.8561672921798,4.36584458068467));
#134929=CARTESIAN_POINT('Ctrl Pts',(17.0651711511373,15.8682273403298,4.75624090048179));
#134930=CARTESIAN_POINT('Ctrl Pts',(17.1281077183015,16.0986316303056,5.81623554177613));
#134931=CARTESIAN_POINT('Ctrl Pts',(17.1910442854656,15.3399495359646,6.59152679461439));
#134932=CARTESIAN_POINT('Ctrl Pts',(17.2539808526298,14.2752146452534,6.38412796646659));
#134933=CARTESIAN_POINT('Ctrl Pts',(17.316917419794,13.8629959949843,5.38075852074024));
#134934=CARTESIAN_POINT('Ctrl Pts',(17.3798539869582,14.4744104185701,4.48474024076459));
#134935=CARTESIAN_POINT('Ctrl Pts',(17.4427905541224,15.5590065089138,4.50275076316532));
#134936=CARTESIAN_POINT('Ctrl Pts',(17.5057271212865,16.1403369932313,5.41857159491376));
#134937=CARTESIAN_POINT('Ctrl Pts',(17.5686636884507,15.6950304150661,6.40770645856968));
#134938=CARTESIAN_POINT('Ctrl Pts',(17.6316002556149,14.6240028972271,6.57963333371724));
#134939=CARTESIAN_POINT('Ctrl Pts',(17.6945368227791,13.8914669101736,5.77959649869392));
#134940=CARTESIAN_POINT('Ctrl Pts',(17.7574733899432,14.1569599465065,4.72780560170415));
#134941=CARTESIAN_POINT('Ctrl Pts',(17.8204099571074,15.1813773355444,4.37128384706725));
#134942=CARTESIAN_POINT('Ctrl Pts',(17.8833465242716,16.042610986541,5.03079525142366));
#134943=CARTESIAN_POINT('Ctrl Pts',(17.9462830914358,15.9649819702309,6.11299553207626));
#134944=CARTESIAN_POINT('Ctrl Pts',(18.0092196586,15.0190017581962,6.64279768350049));
#134945=CARTESIAN_POINT('Ctrl Pts',(18.0721562257642,14.0551086903138,6.1447833840553));
#134946=CARTESIAN_POINT('Ctrl Pts',(18.1350967229588,13.9434899186243,5.06410065696252));
#134947=CARTESIAN_POINT('Ctrl Pts',(18.177058364432,14.5009678185522,4.60868560308863));
#134948=CARTESIAN_POINT('Ctrl Pts',(18.1980411501839,14.814855634692,4.54766692269823));
#134949=CARTESIAN_POINT('Ctrl Pts',(14.0259231306101,15.3928122569186,6.30175254026682));
#134950=CARTESIAN_POINT('Ctrl Pts',(14.0469074862441,15.1285388391585,6.43123777590067));
#134951=CARTESIAN_POINT('Ctrl Pts',(14.0888706975995,14.4665124067093,6.4064459316383));
#134952=CARTESIAN_POINT('Ctrl Pts',(14.1518127646763,13.94853130041,5.55124981634076));
#134953=CARTESIAN_POINT('Ctrl Pts',(14.2147493318405,14.3795709978247,4.65064567642131));
#134954=CARTESIAN_POINT('Ctrl Pts',(14.2776858990047,15.3680119391277,4.51439590178259));
#134955=CARTESIAN_POINT('Ctrl Pts',(14.3406224661689,16.0257292155568,5.26563159465118));
#134956=CARTESIAN_POINT('Ctrl Pts',(14.403559033333,15.7596892229829,6.22778652456713));
#134957=CARTESIAN_POINT('Ctrl Pts',(14.4664956004972,14.8098652282821,6.53476412496152));
#134958=CARTESIAN_POINT('Ctrl Pts',(14.5294321676614,14.0311374386496,5.91013355439827));
#134959=CARTESIAN_POINT('Ctrl Pts',(14.5923687348256,14.1247073620134,4.91627495124337));
#134960=CARTESIAN_POINT('Ctrl Pts',(14.6553053019898,15.0062727971596,4.44793221620871));
#134961=CARTESIAN_POINT('Ctrl Pts',(14.718241869154,15.8822017255247,4.92675771200912));
#134962=CARTESIAN_POINT('Ctrl Pts',(14.7811784363181,15.9638883144447,5.92166564977722));
#134963=CARTESIAN_POINT('Ctrl Pts',(14.8441150034823,15.1777994075511,6.53695326074052));
#134964=CARTESIAN_POINT('Ctrl Pts',(14.9070515706465,14.2316381313645,6.21868254946021));
#134965=CARTESIAN_POINT('Ctrl Pts',(14.9699881378107,13.9772255836124,5.25338981833962));
#134966=CARTESIAN_POINT('Ctrl Pts',(15.0329247049749,14.6436055255302,4.51011749638414));
#134967=CARTESIAN_POINT('Ctrl Pts',(15.095861272139,15.6308438011843,4.65802586399385));
#134968=CARTESIAN_POINT('Ctrl Pts',(15.1587978393032,16.0501400440184,5.56395451996565));
#134969=CARTESIAN_POINT('Ctrl Pts',(15.2217344064674,15.5240064818785,6.41230561891176));
#134970=CARTESIAN_POINT('Ctrl Pts',(15.2846709736316,14.5261154582979,6.43931771342815));
#134971=CARTESIAN_POINT('Ctrl Pts',(15.3476075407957,13.9548576361425,5.62067211419259));
#134972=CARTESIAN_POINT('Ctrl Pts',(15.4105441079599,14.3245303059707,4.69338669851791));
#134973=CARTESIAN_POINT('Ctrl Pts',(15.4734806751241,15.302321125088,4.49228661751318));
#134974=CARTESIAN_POINT('Ctrl Pts',(15.5364172422883,16.007935464839,5.19842012317987));
#134975=CARTESIAN_POINT('Ctrl Pts',(15.5993538094524,15.8061162800138,6.17606276871713));
#134976=CARTESIAN_POINT('Ctrl Pts',(15.6622903766167,14.8785592240971,6.54505332964661));
#134977=CARTESIAN_POINT('Ctrl Pts',(15.7252269437808,14.0603340009386,5.97319354816815));
#134978=CARTESIAN_POINT('Ctrl Pts',(15.788163510945,14.0880800328476,4.9753226730392));
#134979=CARTESIAN_POINT('Ctrl Pts',(15.8511000781092,14.9368178640586,4.44981318729933));
#134980=CARTESIAN_POINT('Ctrl Pts',(15.9140366452733,15.8424378968923,4.86977566394798));
#134981=CARTESIAN_POINT('Ctrl Pts',(15.9769732124375,15.989620095693,5.85712237410304));
#134982=CARTESIAN_POINT('Ctrl Pts',(16.0399097796017,15.2458579000332,6.52295562800579));
#134983=CARTESIAN_POINT('Ctrl Pts',(16.1028463467659,14.2807524648661,6.26783286402901));
#134984=CARTESIAN_POINT('Ctrl Pts',(16.1657829139301,13.963177897795,5.32143837966034));
#134985=CARTESIAN_POINT('Ctrl Pts',(16.2287194810942,14.5790431871124,4.53580101350342));
#134986=CARTESIAN_POINT('Ctrl Pts',(16.2916560482584,15.5738913956158,4.61822168890217));
#134987=CARTESIAN_POINT('Ctrl Pts',(16.3545926154226,16.0520713147637,5.49449795277187));
#134988=CARTESIAN_POINT('Ctrl Pts',(16.4175291825868,15.5830826744606,6.37572765093743));
#134989=CARTESIAN_POINT('Ctrl Pts',(16.480465749751,14.5891509346843,6.46854910533599));
#134990=CARTESIAN_POINT('Ctrl Pts',(16.5434023169151,13.9651022170329,5.68939615262709));
#134991=CARTESIAN_POINT('Ctrl Pts',(16.6063388840793,14.2727609116468,4.73973186820137));
#134992=CARTESIAN_POINT('Ctrl Pts',(16.6692754512435,15.2351451844627,4.47452885639193));
#134993=CARTESIAN_POINT('Ctrl Pts',(16.7322120184077,15.985830760779,5.13254655467003));
#134994=CARTESIAN_POINT('Ctrl Pts',(16.7951485855719,15.8489834409714,6.12137866142463));
#134995=CARTESIAN_POINT('Ctrl Pts',(16.858085152736,14.9478054025582,6.55079020250375));
#134996=CARTESIAN_POINT('Ctrl Pts',(16.9210217199002,14.0936176046393,6.03418655285762));
#134997=CARTESIAN_POINT('Ctrl Pts',(16.9839582870644,14.0554361847655,5.03666046512959));
#134998=CARTESIAN_POINT('Ctrl Pts',(17.0468948542286,14.8676354803984,4.45627399701871));
#134999=CARTESIAN_POINT('Ctrl Pts',(17.1098314213928,15.799001121159,4.81554291510618));
#135000=CARTESIAN_POINT('Ctrl Pts',(17.1727679885569,16.0110346260479,5.79102118845218));
#135001=CARTESIAN_POINT('Ctrl Pts',(17.2357045557211,15.312844398876,6.50449627898228));
#135002=CARTESIAN_POINT('Ctrl Pts',(17.2986411228853,14.3330038295935,6.3136339454439));
#135003=CARTESIAN_POINT('Ctrl Pts',(17.3615776900495,13.9536525371054,5.39026598081901));
#135004=CARTESIAN_POINT('Ctrl Pts',(17.4245142572136,14.5163171610417,4.56568977016024));
#135005=CARTESIAN_POINT('Ctrl Pts',(17.4874508243779,15.5144353403885,4.58226426271812));
#135006=CARTESIAN_POINT('Ctrl Pts',(17.550387391542,16.0494147025417,5.4250641117413));
#135007=CARTESIAN_POINT('Ctrl Pts',(17.6133239587062,15.6396136761443,6.33533245774653));
#135008=CARTESIAN_POINT('Ctrl Pts',(17.6762605258703,14.653982208676,6.49355111732947));
#135009=CARTESIAN_POINT('Ctrl Pts',(17.7391970930346,13.9798533857772,5.75730347980486));
#135010=CARTESIAN_POINT('Ctrl Pts',(17.8021336601987,14.2241779121268,4.78937484304891));
#135011=CARTESIAN_POINT('Ctrl Pts',(17.8650702273629,15.1669156080684,4.46127957532304));
#135012=CARTESIAN_POINT('Ctrl Pts',(17.9280067945271,15.9594806665067,5.06820627184672));
#135013=CARTESIAN_POINT('Ctrl Pts',(17.9909433616913,15.8880412310211,6.06411966617906));
#135014=CARTESIAN_POINT('Ctrl Pts',(18.0538799288554,15.0174866943225,6.55167919502274));
#135015=CARTESIAN_POINT('Ctrl Pts',(18.1168164960196,14.1304475443887,6.09337298289774));
#135016=CARTESIAN_POINT('Ctrl Pts',(18.1797569932142,14.0277284527642,5.09885614329179));
#135017=CARTESIAN_POINT('Ctrl Pts',(18.2217186346875,14.5407570644806,4.67975261851716));
#135018=CARTESIAN_POINT('Ctrl Pts',(18.2427014204393,14.8296177180955,4.62359912993311));
#135019=CARTESIAN_POINT('Ctrl Pts',(14.0705834008655,15.3587786283412,6.23228793552038));
#135020=CARTESIAN_POINT('Ctrl Pts',(14.0915677564996,15.1174021115421,6.35055444684459));
#135021=CARTESIAN_POINT('Ctrl Pts',(14.1335309678549,14.5127342805966,6.32791059161392));
#135022=CARTESIAN_POINT('Ctrl Pts',(14.1964730349317,14.0396315513625,5.54680948337434));
#135023=CARTESIAN_POINT('Ctrl Pts',(14.2594096020959,14.4333255582968,4.72423454507328));
#135024=CARTESIAN_POINT('Ctrl Pts',(14.3223461692601,15.3361270337367,4.59978958085514));
#135025=CARTESIAN_POINT('Ctrl Pts',(14.3852827364243,15.9368590580494,5.28593749681547));
#135026=CARTESIAN_POINT('Ctrl Pts',(14.4482193035884,15.6938690241632,6.16473040596473));
#135027=CARTESIAN_POINT('Ctrl Pts',(14.5111558707526,14.8263386862416,6.44511117428634));
#135028=CARTESIAN_POINT('Ctrl Pts',(14.5740924379168,14.115080615001,5.87459919208737));
#135029=CARTESIAN_POINT('Ctrl Pts',(14.637029005081,14.2005435509639,4.96684944618539));
#135030=CARTESIAN_POINT('Ctrl Pts',(14.6999655722452,15.0057293160312,4.53908437238796));
#135031=CARTESIAN_POINT('Ctrl Pts',(14.7629021394093,15.8057669266405,4.97642397056065));
#135032=CARTESIAN_POINT('Ctrl Pts',(14.8258387065735,15.8803761115893,5.88513213572415));
#135033=CARTESIAN_POINT('Ctrl Pts',(14.8887752737377,15.1623946973077,6.44711064125359));
#135034=CARTESIAN_POINT('Ctrl Pts',(14.9517118409019,14.2982097364751,6.15641520794383));
#135035=CARTESIAN_POINT('Ctrl Pts',(15.014648408066,14.0658397345017,5.27475635967888));
#135036=CARTESIAN_POINT('Ctrl Pts',(15.0775849752302,14.6744838827034,4.59588186058087));
#135037=CARTESIAN_POINT('Ctrl Pts',(15.1405215423944,15.5761868925933,4.7309753061558));
#135038=CARTESIAN_POINT('Ctrl Pts',(15.2034581095586,15.9591549090515,5.55841343936032));
#135039=CARTESIAN_POINT('Ctrl Pts',(15.2663946767228,15.4786060605264,6.33326258999341));
#135040=CARTESIAN_POINT('Ctrl Pts',(15.3293312438869,14.5671732669502,6.3579343308786));
#135041=CARTESIAN_POINT('Ctrl Pts',(15.3922678110511,14.0454097673336,5.61021696712997));
#135042=CARTESIAN_POINT('Ctrl Pts',(15.4552043782153,14.3830536444789,4.76327244425191));
#135043=CARTESIAN_POINT('Ctrl Pts',(15.5181409453795,15.2761277344769,4.57959586606118));
#135044=CARTESIAN_POINT('Ctrl Pts',(15.5810775125437,15.9206069748642,5.2245492913342));
#135045=CARTESIAN_POINT('Ctrl Pts',(15.6440140797078,15.7362735966939,6.11748804565223));
#135046=CARTESIAN_POINT('Ctrl Pts',(15.706950646872,14.8890809687434,6.45450891246436));
#135047=CARTESIAN_POINT('Ctrl Pts',(15.7698872140362,14.1417475592875,5.93219560785463));
#135048=CARTESIAN_POINT('Ctrl Pts',(15.8328237812004,14.1670896485298,5.02078121704908));
#135049=CARTESIAN_POINT('Ctrl Pts',(15.8957603483645,14.9422920245755,4.54080237434935));
#135050=CARTESIAN_POINT('Ctrl Pts',(15.9586969155287,15.7694482740449,4.92437890148916));
#135051=CARTESIAN_POINT('Ctrl Pts',(16.0216334826929,15.903878466769,5.82618095101143));
#135052=CARTESIAN_POINT('Ctrl Pts',(16.0845700498571,15.2245565370916,6.434325776769));
#135053=CARTESIAN_POINT('Ctrl Pts',(16.1475066170213,14.3430687572802,6.20130709238213));
#135054=CARTESIAN_POINT('Ctrl Pts',(16.2104431841855,14.0530091535813,5.33690912874664));
#135055=CARTESIAN_POINT('Ctrl Pts',(16.2733797513496,14.6155152868614,4.61934013328171));
#135056=CARTESIAN_POINT('Ctrl Pts',(16.3363163185138,15.5241688977606,4.6946198027566));
#135057=CARTESIAN_POINT('Ctrl Pts',(16.399252885678,15.9609188526577,5.49497465539119));
#135058=CARTESIAN_POINT('Ctrl Pts',(16.4621894528422,15.5325638354403,6.29985377205));
#135059=CARTESIAN_POINT('Ctrl Pts',(16.5251260200063,14.6247472895435,6.38463308711259));
#135060=CARTESIAN_POINT('Ctrl Pts',(16.5880625871705,14.0547667479651,5.67298668933017));
#135061=CARTESIAN_POINT('Ctrl Pts',(16.6509991543347,14.3357695998536,4.80560222423307));
#135062=CARTESIAN_POINT('Ctrl Pts',(16.7139357214989,15.2147719814151,4.56337665429964));
#135063=CARTESIAN_POINT('Ctrl Pts',(16.7768722886631,15.9004174434459,5.16438307162583));
#135064=CARTESIAN_POINT('Ctrl Pts',(16.8398088558272,15.7754267059423,6.06754182156959));
#135065=CARTESIAN_POINT('Ctrl Pts',(16.9027454229914,14.9523275922601,6.4597487371857));
#135066=CARTESIAN_POINT('Ctrl Pts',(16.9656819901556,14.1721474398201,5.98790412044679));
#135067=CARTESIAN_POINT('Ctrl Pts',(17.0286185573198,14.137274094579,5.07680464433289));
#135068=CARTESIAN_POINT('Ctrl Pts',(17.091555124484,14.8791036686173,4.54670341335277));
#135069=CARTESIAN_POINT('Ctrl Pts',(17.1544916916481,15.7297749019882,4.87484492973059));
#135070=CARTESIAN_POINT('Ctrl Pts',(17.2174282588123,15.9234376217902,5.76580683512822));
#135071=CARTESIAN_POINT('Ctrl Pts',(17.2803648259765,15.2857392617874,6.41746576335018));
#135072=CARTESIAN_POINT('Ctrl Pts',(17.3433013931407,14.3907930139337,6.24313992442123));
#135073=CARTESIAN_POINT('Ctrl Pts',(17.4062379603049,14.0443090792265,5.39977344089779));
#135074=CARTESIAN_POINT('Ctrl Pts',(17.469174527469,14.5582239035133,4.6466392995559));
#135075=CARTESIAN_POINT('Ctrl Pts',(17.5321110946332,15.4698641718634,4.66177776227094));
#135076=CARTESIAN_POINT('Ctrl Pts',(17.5950476617974,15.9584924118522,5.43155662856886));
#135077=CARTESIAN_POINT('Ctrl Pts',(17.6579842289616,15.5841969372227,6.26295845692337));
#135078=CARTESIAN_POINT('Ctrl Pts',(17.7209207961258,14.6839615201247,6.40746890094173));
#135079=CARTESIAN_POINT('Ctrl Pts',(17.7838573632899,14.0682398613808,5.73501046091577));
#135080=CARTESIAN_POINT('Ctrl Pts',(17.8467939304541,14.2913958777472,4.8509440843937));
#135081=CARTESIAN_POINT('Ctrl Pts',(17.9097304976183,15.1524538805926,4.55127530357883));
#135082=CARTESIAN_POINT('Ctrl Pts',(17.9726670647825,15.8763503464722,5.10561729226978));
#135083=CARTESIAN_POINT('Ctrl Pts',(18.0356036319466,15.8111004918114,6.01524380028187));
#135084=CARTESIAN_POINT('Ctrl Pts',(18.0985401991108,15.0159716304487,6.46056070654498));
#135085=CARTESIAN_POINT('Ctrl Pts',(18.161476766275,14.2057863984636,6.04196258174017));
#135086=CARTESIAN_POINT('Ctrl Pts',(18.2244172634697,14.111966986904,5.13361162962105));
#135087=CARTESIAN_POINT('Ctrl Pts',(18.2663789049429,14.5805463104091,4.75081963394569));
#135088=CARTESIAN_POINT('Ctrl Pts',(18.2873616906948,14.8443798014988,4.69953133716798));
#135089=CARTESIAN_POINT('Ctrl Pts',(14.1152436711209,15.3247449997639,6.16282333077395));
#135090=CARTESIAN_POINT('Ctrl Pts',(14.1362280267549,15.1062653839256,6.26987111778852));
#135091=CARTESIAN_POINT('Ctrl Pts',(14.1781912381104,14.558956154484,6.24937525158952));
#135092=CARTESIAN_POINT('Ctrl Pts',(14.2411333051872,14.1307318023153,5.54236915040796));
#135093=CARTESIAN_POINT('Ctrl Pts',(14.3040698723514,14.4870801187687,4.79782341372522));
#135094=CARTESIAN_POINT('Ctrl Pts',(14.3670064395155,15.3042421283455,4.68518325992769));
#135095=CARTESIAN_POINT('Ctrl Pts',(14.4299430066797,15.8479889005418,5.30624339897972));
#135096=CARTESIAN_POINT('Ctrl Pts',(14.4928795738439,15.6280488253434,6.10167428736234));
#135097=CARTESIAN_POINT('Ctrl Pts',(14.5558161410081,14.8428121442009,6.35545822361114));
#135098=CARTESIAN_POINT('Ctrl Pts',(14.6187527081723,14.1990237913524,5.83906482977647));
#135099=CARTESIAN_POINT('Ctrl Pts',(14.6816892753364,14.2763797399144,5.01742394112739));
#135100=CARTESIAN_POINT('Ctrl Pts',(14.7446258425006,15.0051858349026,4.63023652856724));
#135101=CARTESIAN_POINT('Ctrl Pts',(14.8075624096648,15.7293321277563,5.02609022911216));
#135102=CARTESIAN_POINT('Ctrl Pts',(14.870498976829,15.7968639087338,5.84859862167108));
#135103=CARTESIAN_POINT('Ctrl Pts',(14.9334355439932,15.1469899870644,6.35726802176666));
#135104=CARTESIAN_POINT('Ctrl Pts',(14.9963721111573,14.3647813415856,6.09414786642744));
#135105=CARTESIAN_POINT('Ctrl Pts',(15.0593086783215,14.1544538853912,5.29612290101818));
#135106=CARTESIAN_POINT('Ctrl Pts',(15.1222452454857,14.7053622398767,4.68164622477757));
#135107=CARTESIAN_POINT('Ctrl Pts',(15.1851818126499,15.5215299840022,4.80392474831775));
#135108=CARTESIAN_POINT('Ctrl Pts',(15.2481183798141,15.8681697740847,5.55287235875496));
#135109=CARTESIAN_POINT('Ctrl Pts',(15.3110549469782,15.4332056391742,6.25421956107508));
#135110=CARTESIAN_POINT('Ctrl Pts',(15.3739915141424,14.6082310756026,6.27655094832902));
#135111=CARTESIAN_POINT('Ctrl Pts',(15.4369280813066,14.1359618985248,5.59976182006737));
#135112=CARTESIAN_POINT('Ctrl Pts',(15.4998646484708,14.4415769829873,4.8331581899859));
#135113=CARTESIAN_POINT('Ctrl Pts',(15.5628012156349,15.2499343438656,4.66690511460918));
#135114=CARTESIAN_POINT('Ctrl Pts',(15.6257377827991,15.8332784848894,5.25067845948853));
#135115=CARTESIAN_POINT('Ctrl Pts',(15.6886743499633,15.6664309133739,6.0589133225873));
#135116=CARTESIAN_POINT('Ctrl Pts',(15.7516109171275,14.8996027133896,6.3639644952821));
#135117=CARTESIAN_POINT('Ctrl Pts',(15.8145474842917,14.2231611176365,5.89119766754112));
#135118=CARTESIAN_POINT('Ctrl Pts',(15.8774840514559,14.2460992642119,5.06623976105893));
#135119=CARTESIAN_POINT('Ctrl Pts',(15.94042061862,14.9477661850923,4.63179156139939));
#135120=CARTESIAN_POINT('Ctrl Pts',(16.0033571857842,15.6964586511974,4.97898213903037));
#135121=CARTESIAN_POINT('Ctrl Pts',(16.0662937529484,15.8181368378449,5.7952395279198));
#135122=CARTESIAN_POINT('Ctrl Pts',(16.1292303201126,15.2032551741499,6.34569592553222));
#135123=CARTESIAN_POINT('Ctrl Pts',(16.1921668872767,14.4053850496942,6.13478132073524));
#135124=CARTESIAN_POINT('Ctrl Pts',(16.2551034544409,14.1428404093677,5.35237987783294));
#135125=CARTESIAN_POINT('Ctrl Pts',(16.3180400216051,14.6519873866103,4.70287925306001));
#135126=CARTESIAN_POINT('Ctrl Pts',(16.3809765887693,15.4744463999053,4.77101791661106));
#135127=CARTESIAN_POINT('Ctrl Pts',(16.4439131559335,15.8697663905516,5.49545135801052));
#135128=CARTESIAN_POINT('Ctrl Pts',(16.5068497230977,15.4820449964198,6.22397989316257));
#135129=CARTESIAN_POINT('Ctrl Pts',(16.5697862902618,14.6603436444027,6.3007170688892));
#135130=CARTESIAN_POINT('Ctrl Pts',(16.632722857426,14.1444312788974,5.6565772260332));
#135131=CARTESIAN_POINT('Ctrl Pts',(16.6956594245902,14.3987782880603,4.87147258026479));
#135132=CARTESIAN_POINT('Ctrl Pts',(16.7585959917544,15.1943987783676,4.65222445220735));
#135133=CARTESIAN_POINT('Ctrl Pts',(16.8215325589185,15.8150041261129,5.19621958858164));
#135134=CARTESIAN_POINT('Ctrl Pts',(16.8844691260827,15.7018699709131,6.01370498171452));
#135135=CARTESIAN_POINT('Ctrl Pts',(16.9474056932469,14.9568497819623,6.36870727186765));
#135136=CARTESIAN_POINT('Ctrl Pts',(17.0103422604111,14.2506772750008,5.94162168803595));
#135137=CARTESIAN_POINT('Ctrl Pts',(17.0732788275753,14.2191120043925,5.11694882353618));
#135138=CARTESIAN_POINT('Ctrl Pts',(17.1362153947394,14.8905718568359,4.63713282968683));
#135139=CARTESIAN_POINT('Ctrl Pts',(17.1991519619036,15.6605486828174,4.93414694435498));
#135140=CARTESIAN_POINT('Ctrl Pts',(17.2620885290678,15.8358406175325,5.74059248180427));
#135141=CARTESIAN_POINT('Ctrl Pts',(17.325025096232,15.2586341246988,6.33043524771806));
#135142=CARTESIAN_POINT('Ctrl Pts',(17.3879616633962,14.4485821982738,6.17264590339857));
#135143=CARTESIAN_POINT('Ctrl Pts',(17.4508982305603,14.1349656213476,5.40928090097655));
#135144=CARTESIAN_POINT('Ctrl Pts',(17.5138347977245,14.6001306459849,4.72758882895156));
#135145=CARTESIAN_POINT('Ctrl Pts',(17.5767713648887,15.4252930033383,4.74129126182374));
#135146=CARTESIAN_POINT('Ctrl Pts',(17.6397079320529,15.8675701211627,5.43804914539642));
#135147=CARTESIAN_POINT('Ctrl Pts',(17.702644499217,15.5287801983009,6.19058445610023));
#135148=CARTESIAN_POINT('Ctrl Pts',(17.7655810663813,14.7139408315735,6.32138668455399));
#135149=CARTESIAN_POINT('Ctrl Pts',(17.8285176335454,14.1566263369844,5.7127174420267));
#135150=CARTESIAN_POINT('Ctrl Pts',(17.8914542007096,14.3586138433675,4.91251332573848));
#135151=CARTESIAN_POINT('Ctrl Pts',(17.9543907678738,15.1379921531166,4.64127103183461));
#135152=CARTESIAN_POINT('Ctrl Pts',(18.0173273350379,15.793220026438,5.14302831269285));
#135153=CARTESIAN_POINT('Ctrl Pts',(18.0802639022021,15.7341597526016,5.96636793438466));
#135154=CARTESIAN_POINT('Ctrl Pts',(18.1432004693663,15.014456566575,6.36944221806724));
#135155=CARTESIAN_POINT('Ctrl Pts',(18.2061370365305,14.2811252525384,5.99055218058262));
#135156=CARTESIAN_POINT('Ctrl Pts',(18.2690775337251,14.1962055210438,5.16836711595032));
#135157=CARTESIAN_POINT('Ctrl Pts',(18.3110391751983,14.6203355563376,4.82188664937422));
#135158=CARTESIAN_POINT('Ctrl Pts',(18.3320219609502,14.8591418849023,4.77546354440285));
#135159=CARTESIAN_POINT('Ctrl Pts',(13.9832500000001,15.4251191285151,6.36826222368042));
#135160=CARTESIAN_POINT('Ctrl Pts',(13.9999444295459,15.3215451468816,6.40038609166026));
#135161=CARTESIAN_POINT('Ctrl Pts',(14.0151347722421,15.2140895632333,6.41628947421468));
#135162=CARTESIAN_POINT('Ctrl Pts',(14.0464108252689,15.0135230598887,6.40808816006153));
#135163=CARTESIAN_POINT('Ctrl Pts',(14.0616867519111,14.9233916473141,6.38961563625844));
#135164=CARTESIAN_POINT('Ctrl Pts',(14.1014789163806,14.7191082827324,6.31037841140784));
#135165=CARTESIAN_POINT('Ctrl Pts',(14.122898891006,14.6299394659766,6.24441205772044));
#135166=CARTESIAN_POINT('Ctrl Pts',(14.150553159263,14.5162927313885,6.14013885201157));
#135167=CARTESIAN_POINT('Ctrl Pts',(14.162214770313,14.4710252601612,6.0877267220467));
#135168=CARTESIAN_POINT('Ctrl Pts',(14.1857737491176,14.3996118262497,5.97684797725505));
#135169=CARTESIAN_POINT('Ctrl Pts',(14.1973567639203,14.3727511830336,5.92043909160861));
#135170=CARTESIAN_POINT('Ctrl Pts',(14.2099481424296,14.3539251530524,5.86092110500077));
#135171=CARTESIAN_POINT('Origin',(18.2,15.,5.5));
#135172=CARTESIAN_POINT('',(18.3,15.,6.56675));
#135173=CARTESIAN_POINT('Origin',(18.3,15.,5.5));
#135174=CARTESIAN_POINT('Origin',(18.2,15.,6.56675));
#135175=CARTESIAN_POINT('Origin',(18.3,16.9,5.5));
#135176=CARTESIAN_POINT('',(18.3,13.1,5.5));
#135177=CARTESIAN_POINT('Origin',(18.3,15.,5.5));
#135178=CARTESIAN_POINT('Origin',(19.,15.,5.5));
#135179=CARTESIAN_POINT('',(19.,13.1165191798163,5.25));
#135180=CARTESIAN_POINT('',(19.,13.1,5.5));
#135181=CARTESIAN_POINT('Origin',(19.,15.,5.5));
#135182=CARTESIAN_POINT('',(19.,16.8834808201837,5.25));
#135183=CARTESIAN_POINT('',(19.,12.6,5.25));
#135184=CARTESIAN_POINT('',(19.,16.8834808201837,5.75));
#135185=CARTESIAN_POINT('Origin',(19.,15.,5.5));
#135186=CARTESIAN_POINT('',(19.,13.1165191798163,5.75));
#135187=CARTESIAN_POINT('',(19.,17.4,5.75));
#135188=CARTESIAN_POINT('Origin',(19.,15.,5.5));
#135189=CARTESIAN_POINT('Origin',(19.6,12.6,5.75));
#135190=CARTESIAN_POINT('',(19.2,13.1165191798163,5.75));
#135191=CARTESIAN_POINT('',(18.75,13.1165191798163,5.75));
#135192=CARTESIAN_POINT('',(19.2,16.8834808201837,5.75));
#135193=CARTESIAN_POINT('',(18.75,16.8834808201837,5.75));
#135194=CARTESIAN_POINT('',(19.6,16.4790199457749,5.75));
#135195=CARTESIAN_POINT('Ctrl Pts',(19.6,16.4790199457749,5.75));
#135196=CARTESIAN_POINT('Ctrl Pts',(19.4240571469012,16.6574585668375,5.75));
#135197=CARTESIAN_POINT('Ctrl Pts',(19.2000000000002,16.8834808201836,5.75));
#135198=CARTESIAN_POINT('',(19.6,13.5209800542251,5.75));
#135199=CARTESIAN_POINT('',(19.6,13.8,5.75));
#135200=CARTESIAN_POINT('Ctrl Pts',(19.2000000000002,13.1165191798164,5.75));
#135201=CARTESIAN_POINT('Ctrl Pts',(19.4240571469012,13.3425414331625,5.75));
#135202=CARTESIAN_POINT('Ctrl Pts',(19.6,13.5209800542251,5.75));
#135203=CARTESIAN_POINT('Origin',(19.6,17.4,5.25));
#135204=CARTESIAN_POINT('',(19.2,13.1165191798163,5.25));
#135205=CARTESIAN_POINT('',(18.75,13.1165191798163,5.25));
#135206=CARTESIAN_POINT('',(19.6,13.5209800542251,5.25));
#135207=CARTESIAN_POINT('Ctrl Pts',(19.6,13.5209800542251,5.25));
#135208=CARTESIAN_POINT('Ctrl Pts',(19.4240571469012,13.3425414331624,5.25));
#135209=CARTESIAN_POINT('Ctrl Pts',(19.2000000000002,13.1165191798164,5.25));
#135210=CARTESIAN_POINT('',(19.6,16.4790199457749,5.25));
#135211=CARTESIAN_POINT('',(19.6,16.2,5.25));
#135212=CARTESIAN_POINT('',(19.2,16.8834808201837,5.25));
#135213=CARTESIAN_POINT('Ctrl Pts',(19.2000000000002,16.8834808201836,5.25));
#135214=CARTESIAN_POINT('Ctrl Pts',(19.4240571469012,16.6574585668376,5.25));
#135215=CARTESIAN_POINT('Ctrl Pts',(19.6,16.4790199457749,5.25));
#135216=CARTESIAN_POINT('',(18.75,16.8834808201837,5.25));
#135217=CARTESIAN_POINT('Origin',(18.75,15.,5.5));
#135218=CARTESIAN_POINT('',(18.75,13.1,5.5));
#135219=CARTESIAN_POINT('Origin',(19.2,15.,5.5));
#135220=CARTESIAN_POINT('Origin',(19.2,15.,5.5));
#135221=CARTESIAN_POINT('Origin',(19.6,15.,5.5));
#135222=CARTESIAN_POINT('Origin',(19.6,15.,5.5));
#135223=CARTESIAN_POINT('Origin',(19.6,15.,5.5));
#135224=CARTESIAN_POINT('Origin',(19.6,15.,5.5));
#135225=CARTESIAN_POINT('Origin',(19.4,15.,5.5));
#135226=CARTESIAN_POINT('Origin',(14.3,15.65,5.5));
#135227=CARTESIAN_POINT('',(14.3,14.35,5.5));
#135228=CARTESIAN_POINT('Origin',(14.3,15.,5.5));
#135229=CARTESIAN_POINT('Origin',(14.125,15.,5.5));
#135230=CARTESIAN_POINT('',(14.125,14.175,5.5));
#135231=CARTESIAN_POINT('Origin',(19.4,15.,5.5));
#135266=UNCERTAINTY_MEASURE_WITH_UNIT(LENGTH_MEASURE(0.01),#135283,
'DISTANCE_ACCURACY_VALUE',
'Maximum model space distance between geometric entities at asserted c
onnectivities');
#135267=UNCERTAINTY_MEASURE_WITH_UNIT(LENGTH_MEASURE(0.01),#135283,
'DISTANCE_ACCURACY_VALUE',
'Maximum model space distance between geometric entities at asserted c
onnectivities');
#135281=(
GEOMETRIC_REPRESENTATION_CONTEXT(3)
GLOBAL_UNCERTAINTY_ASSIGNED_CONTEXT((#135266))
GLOBAL_UNIT_ASSIGNED_CONTEXT((#135283,#135285,#135286))
REPRESENTATION_CONTEXT('','3D')
);
#135282=(
GEOMETRIC_REPRESENTATION_CONTEXT(3)
GLOBAL_UNCERTAINTY_ASSIGNED_CONTEXT((#135267))
GLOBAL_UNIT_ASSIGNED_CONTEXT((#135283,#135285,#135286))
REPRESENTATION_CONTEXT('','3D')
);
#135283=(
LENGTH_UNIT()
NAMED_UNIT(*)
SI_UNIT(.MILLI.,.METRE.)
);
#135285=(
NAMED_UNIT(*)
PLANE_ANGLE_UNIT()
SI_UNIT($,.RADIAN.)
);
#135286=(
NAMED_UNIT(*)
SI_UNIT($,.STERADIAN.)
SOLID_ANGLE_UNIT()
);
#135300=SHAPE_DEFINITION_REPRESENTATION(#135314,#135349);
#135314=PRODUCT_DEFINITION_SHAPE('',$,#135364);
#135349=SHAPE_REPRESENTATION('',(#34149),#135281);
#135350=PRODUCT_DEFINITION_CONTEXT('part definition',#135394,'design');
#135364=PRODUCT_DEFINITION('2026-10-15-19-09-11-266',
'ISO 1207 - M2 x 4 - 4.8',#135378,#135350);
#135378=PRODUCT_DEFINITION_FORMATION('',$,#135409);
#135394=APPLICATION_CONTEXT(
'Core Data for Automotive Mechanical Design Process');
#135395=PRODUCT_CONTEXT('part definition',#135394,'mechanical');
#135409=PRODUCT('2026-10-15-19-09-11-266','ISO 1207 - M2 x 4 - 4.8',$,(#135395));
#135423=PRESENTATION_STYLE_ASSIGNMENT((#135437));
#135437=SURFACE_STYLE_USAGE(.BOTH.,#135451);
#135451=SURFACE_SIDE_STYLE('',(#135465));
#135465=SURFACE_STYLE_FILL_AREA(#135479);
#135479=FILL_AREA_STYLE('Opaque(203,207,213)',(#135493));
#135493=FILL_AREA_STYLE_COLOUR('Opaque(203,207,213)',#135507);
#135507=COLOUR_RGB('Opaque(203,207,213)', 0.09019608, 0.27058824, 0.51372549);
ENDSEC;
END-ISO-10303-21;
